ISO-10303-21;
HEADER;
FILE_DESCRIPTION (('STEP AP214'),
    '1' );
FILE_NAME ('Screw M5.step',
    '2026-10-29T23:46:56',
    ( '' ),
    ( '' ),
    'SwSTEP 2.0',
    'SolidWorks 2020',
    '' );
FILE_SCHEMA (( 'AUTOMOTIVE_DESIGN' ));
ENDSEC;

DATA;
#15=CARTESIAN_POINT ( 'NONE',  ( 49.15300726216835159, 22.74928388133296764, 45.65942558980532340 ) ) ;
#24=CARTESIAN_POINT ( 'NONE',  ( 46.00908685603034343, 26.23284706826093071, 44.91496614357595263 ) ) ;
#34=CARTESIAN_POINT ( 'NONE',  ( 46.96819297411687444, 27.59253733014356058, 49.54594323136014822 ) ) ;
#35=CARTESIAN_POINT ( 'NONE',  ( 49.62252444096254322, 24.84787913140503690, 48.68715535708000175 ) ) ;
#37=CARTESIAN_POINT ( 'NONE',  ( 44.79156314060809763, 22.80400562401889530, 46.92953032342012420 ) ) ;
#58=CARTESIAN_POINT ( 'NONE',  ( 44.70507715278255745, 27.74951373492759643, 46.92503878583764987 ) ) ;
#60=LINE ( 'NONE', #27627, #25175 ) ;
#65=AXIS2_PLACEMENT_3D ( 'NONE', #14177, #6132, #1197 ) ;
#67=( BOUNDED_CURVE ( )  B_SPLINE_CURVE ( 3, ( #13523, #18741, #20741, #23527 ),
 .UNSPECIFIED., .F., .F. ) 
 B_SPLINE_CURVE_WITH_KNOTS ( ( 4, 4 ),
 ( 1.099063246724957033, 1.220321128156881318 ),
 .UNSPECIFIED. ) 
 CURVE ( )  GEOMETRIC_REPRESENTATION_ITEM ( )  RATIONAL_B_SPLINE_CURVE ( ( 1.000000000000000000, 0.9987750858034805113, 0.9987750858034805113, 1.000000000000000000 ) ) 
 REPRESENTATION_ITEM ( '' )  );
#125=CARTESIAN_POINT ( 'NONE',  ( 44.70507715278255745, 28.36291119454914877, 46.92503878583765697 ) ) ;
#143=ORIENTED_EDGE ( 'NONE', *, *, #20256, .T. ) ;
#145=CARTESIAN_POINT ( 'NONE',  ( 46.44275705260056242, 23.09557481883486219, 47.38348660136355051 ) ) ;
#152=CARTESIAN_POINT ( 'NONE',  ( 45.79384627280941089, 24.97957786121582302, 49.05938063676249072 ) ) ;
#165=DIRECTION ( 'NONE',  ( 0.8907924397839086517, 1.100109291107994064E-16, -0.4544104193609905251 ) ) ;
#176=VECTOR ( 'NONE', #32272, 1000.000000000000114 ) ;
#177=VECTOR ( 'NONE', #9320, 1000.000000000000114 ) ;
#185=CARTESIAN_POINT ( 'NONE',  ( 49.49063479933183629, 26.69951373492759927, 47.17357720316391578 ) ) ;
#194=CARTESIAN_POINT ( 'NONE',  ( 48.28214861297873028, 24.78954579807170333, 49.37090702980594870 ) ) ;
#205=CARTESIAN_POINT ( 'NONE',  ( 49.62266228875127183, 24.94631262459061105, 46.45121837018842825 ) ) ;
#207=CARTESIAN_POINT ( 'NONE',  ( 48.66895200406656130, 27.18420399681022914, 44.62753372671561181 ) ) ;
#216=CARTESIAN_POINT ( 'NONE',  ( 46.00908685603034343, 25.53284706826093498, 44.91496614357595263 ) ) ;
#224=EDGE_CURVE ( 'NONE', #23081, #15904, #26859, .T. ) ;
#263=VECTOR ( 'NONE', #8856, 1000.000000000000000 ) ;
#273=DIRECTION ( 'NONE',  ( 1.234978253042719660E-16, -1.000000000000000000, -1.109335647967047851E-31 ) ) ;
#278=CARTESIAN_POINT ( 'NONE',  ( 47.40417757965286683, 23.10527845304106620, 46.57712699531703038 ) ) ;
#282=CARTESIAN_POINT ( 'NONE',  ( 48.18662509608405031, 27.19624452788248803, 49.18364984542562013 ) ) ;
#304=CARTESIAN_POINT ( 'NONE',  ( 45.37804019580246973, 22.89977464660286444, 47.76827453631080544 ) ) ;
#306=VERTEX_POINT ( 'NONE', #16918 ) ;
#309=CARTESIAN_POINT ( 'NONE',  ( 45.38854177497844944, 29.72622849631042286, 45.94041160078741370 ) ) ;
#320=ORIENTED_EDGE ( 'NONE', *, *, #9164, .F. ) ;
#323=CARTESIAN_POINT ( 'NONE',  ( 44.21498992391908445, 28.81753733014356200, 46.89958605635242606 ) ) ;
#325=CARTESIAN_POINT ( 'NONE',  ( 45.35708200440645044, 27.69118040159426286, 45.92000246470680480 ) ) ;
#350=CARTESIAN_POINT ( 'NONE',  ( 44.96133376908166213, 22.84434098701873950, 47.26233605563525941 ) ) ;
#353=CARTESIAN_POINT ( 'NONE',  ( 45.46000861347822308, 28.87287913140503548, 49.57397645940629616 ) ) ;
#366=ORIENTED_EDGE ( 'NONE', *, *, #2554, .T. ) ;
#369=CARTESIAN_POINT ( 'NONE',  ( 47.20547626766766314, 27.57451373492759572, 44.97710074790751378 ) ) ;
#386=CARTESIAN_POINT ( 'NONE',  ( 45.96182992765471909, 25.77822092656774799, 44.82232689504102296 ) ) ;
#391=DIRECTION ( 'NONE',  ( 1.234978253042719660E-16, -1.000000000000000000, -1.109335647967047851E-31 ) ) ;
#396=EDGE_CURVE ( 'NONE', #456, #16189, #14313, .T. ) ;
#398=CARTESIAN_POINT ( 'NONE',  ( 49.32483701613094240, 26.30322093266652672, 45.91328182968236860 ) ) ;
#417=VECTOR ( 'NONE', #31540, 999.9999999999998863 ) ;
#425=ORIENTED_EDGE ( 'NONE', *, *, #23403, .T. ) ;
#436=CARTESIAN_POINT ( 'NONE',  ( 47.74496780842034127, 22.93328494799376571, 45.45767897490919296 ) ) ;
#441=CARTESIAN_POINT ( 'NONE',  ( 49.49063479933183629, 25.21291119454915730, 47.17357720316391578 ) ) ;
#446=AXIS2_PLACEMENT_3D ( 'NONE', #4993, #15161, #2997 ) ;
#454=( BOUNDED_CURVE ( )  B_SPLINE_CURVE ( 2, ( #26958, #22195, #9573, #207, #14829, #27460, #32382, #4482, #2504 ),
 .UNSPECIFIED., .F., .F. ) 
 B_SPLINE_CURVE_WITH_KNOTS ( ( 3, 2, 2, 2, 3 ),
 ( 0.4642857154469869352, 0.4761904761904761640, 0.5000000000000000000, 0.5238095238095238360, 0.5357142868755583320 ),
 .UNSPECIFIED. ) 
 CURVE ( )  GEOMETRIC_REPRESENTATION_ITEM ( )  RATIONAL_B_SPLINE_CURVE ( ( 0.9330127018922200755, 0.9330127084266228721, 1.000000000000000000, 0.8660254037844388186, 1.000000000000000000, 0.8660254037844388186, 1.000000000000000000, 0.9330126953578163906, 0.9330127018922200755 ) ) 
 REPRESENTATION_ITEM ( '' )  );
#456=VERTEX_POINT ( 'NONE', #6680 ) ;
#467=CARTESIAN_POINT ( 'NONE',  ( 47.48234838051382667, 29.55343750245331336, 44.96782160785550531 ) ) ;
#469=CARTESIAN_POINT ( 'NONE',  ( 45.38854177497844944, 25.52622849631043422, 45.94041160078741370 ) ) ;
#475=LINE ( 'NONE', #30528, #22010 ) ;
#484=CARTESIAN_POINT ( 'NONE',  ( 48.18662509608405742, 25.88284706826093284, 49.18364984542562013 ) ) ;
#485=ORIENTED_EDGE ( 'NONE', *, *, #11437, .T. ) ;
#486=CYLINDRICAL_SURFACE ( 'NONE', #31413, 2.499999999999997335 ) ;
#512=CARTESIAN_POINT ( 'NONE',  ( 49.41945501136223839, 28.46454579807170759, 45.86501535757901848 ) ) ;
#514=ORIENTED_EDGE ( 'NONE', *, *, #26124, .F. ) ;
#522=EDGE_CURVE ( 'NONE', #10117, #4981, #8501, .T. ) ;
#525=VECTOR ( 'NONE', #14979, 1000.000000000000114 ) ;
#526=CARTESIAN_POINT ( 'NONE',  ( 48.22970226119645076, 23.04411657098542676, 46.95810019591398543 ) ) ;
#533=CARTESIAN_POINT ( 'NONE',  ( 45.24946171279598417, 25.70784706826093569, 47.99220971130007030 ) ) ;
#535=CARTESIAN_POINT ( 'NONE',  ( 47.20547626766766314, 28.18791119454915162, 44.97710074790751378 ) ) ;
#545=CARTESIAN_POINT ( 'NONE',  ( 45.36511207810797686, 26.63213139976340571, 45.12672418911604666 ) ) ;
#566=CARTESIAN_POINT ( 'NONE',  ( 49.73184169360587248, 24.88249584856351149, 46.46638833876414765 ) ) ;
#587=CARTESIAN_POINT ( 'NONE',  ( 47.92322045604424119, 23.24793988701932435, 47.55508673835812772 ) ) ;
#604=PLANE ( 'NONE',  #25960 ) ;
#606=AXIS2_PLACEMENT_3D ( 'NONE', #30004, #14570, #19486 ) ;
#612=DIRECTION ( 'NONE',  ( 1.234978253042719660E-16, -1.000000000000000000, -1.109335647967047851E-31 ) ) ;
#613=CARTESIAN_POINT ( 'NONE',  ( 48.78406556707242459, 22.93807716476589675, 47.13688154746046166 ) ) ;
#624=AXIS2_PLACEMENT_3D ( 'NONE', #9247, #9083, #9410 ) ;
#637=CARTESIAN_POINT ( 'NONE',  ( 48.37829923888483563, 26.05122849631043280, 45.07556196625585443 ) ) ;
#639=EDGE_LOOP ( 'NONE', ( #24316, #16511, #2227, #514, #31883, #2232, #9018, #10673 ) ) ;
#647=DIRECTION ( 'NONE',  ( 1.234978253042719660E-16, -1.000000000000000000, -1.109335647967047851E-31 ) ) ;
#654=CARTESIAN_POINT ( 'NONE',  ( 48.53603344299159517, 25.21410780737789281, 48.64505250420380378 ) ) ;
#668=CARTESIAN_POINT ( 'NONE',  ( 48.81241343884743600, 22.91413368675619111, 46.49136847324655974 ) ) ;
#670=ORIENTED_EDGE ( 'NONE', *, *, #24310, .T. ) ;
#698=CARTESIAN_POINT ( 'NONE',  ( 48.40186567930498285, 26.81618040159426641, 45.03923535223908203 ) ) ;
#723=DIRECTION ( 'NONE',  ( 1.234978253042719660E-16, -1.000000000000000000, -1.109335647967047851E-31 ) ) ;
#738=CARTESIAN_POINT ( 'NONE',  ( 47.03138641870017977, 22.86454579224779948, 49.04855133162938330 ) ) ;
#751=LINE ( 'NONE', #3040, #15627 ) ;
#758=DIRECTION ( 'NONE',  ( -0.4544104659272754088, -1.796165296417912609E-16, -0.8907924160295463967 ) ) ;
#761=CARTESIAN_POINT ( 'NONE',  ( 45.18933221474103590, 20.36454579224780304, 43.30797974740836764 ) ) ;
#762=EDGE_LOOP ( 'NONE', ( #6005, #7688, #10808, #3142 ) ) ;
#774=ORIENTED_EDGE ( 'NONE', *, *, #26425, .F. ) ;
#796=CARTESIAN_POINT ( 'NONE',  ( 45.28286642839709231, 28.44289516297709142, 47.97516931882780966 ) ) ;
#808=DIRECTION ( 'NONE',  ( 0.8643320973212949010, -0.2419218955996661480, -0.4409124878812526460 ) ) ;
#815=CARTESIAN_POINT ( 'NONE',  ( 46.99023568444673771, 26.52451373492759856, 49.12151524109405898 ) ) ;
#818=CARTESIAN_POINT ( 'NONE',  ( 46.05411555189323991, 22.80670247275590867, 45.00323677929942079 ) ) ;
#827=CARTESIAN_POINT ( 'NONE',  ( 48.01680169312755453, 22.93807716476589675, 45.63279442905645311 ) ) ;
#852=CARTESIAN_POINT ( 'NONE',  ( 45.96182992765472619, 28.57822092656774160, 44.82232689504103007 ) ) ;
#855=CARTESIAN_POINT ( 'NONE',  ( 49.41945501136223839, 28.46454579807170759, 45.86501535757901848 ) ) ;
#856=CARTESIAN_POINT ( 'NONE',  ( 47.20547626766765603, 29.58791119454915020, 44.97710074790751378 ) ) ;
#866=CARTESIAN_POINT ( 'NONE',  ( 44.21498992391908445, 26.71753733014355703, 46.89958605635242606 ) ) ;
#884=CARTESIAN_POINT ( 'NONE',  ( 47.09785597605719687, 25.16454579224780019, 47.04930799450078638 ) ) ;
#891=CARTESIAN_POINT ( 'NONE',  ( 49.40414881150629611, 22.86454579224779948, 47.16908566558144855 ) ) ;
#901=CARTESIAN_POINT ( 'NONE',  ( 49.32483701613094240, 27.70322093266652175, 45.91328182968236860 ) ) ;
#908=CARTESIAN_POINT ( 'NONE',  ( 46.53577443378190281, 23.10527845304106620, 47.02011620365084354 ) ) ;
#921=CARTESIAN_POINT ( 'NONE',  ( 49.40414881150629611, 19.96454579224779380, 47.16908566558144855 ) ) ;
#936=EDGE_CURVE ( 'NONE', #20447, #14398, #15132, .T. ) ;
#943=ORIENTED_EDGE ( 'NONE', *, *, #25202, .T. ) ;
#949=CARTESIAN_POINT ( 'NONE',  ( 48.80717017713595141, 25.87622849631043920, 48.15820438821415195 ) ) ;
#958=AXIS2_PLACEMENT_3D ( 'NONE', #20676, #5430, #2476 ) ;
#961=CARTESIAN_POINT ( 'NONE',  ( 48.99785660077486682, 22.86454579224780304, 47.79536686733754181 ) ) ;
#969=CARTESIAN_POINT ( 'NONE',  ( 48.96093869543725674, 24.86454579224779593, 50.70155699761480861 ) ) ;
#970=AXIS2_PLACEMENT_3D ( 'NONE', #17910, #29911, #17740 ) ;
#971=CARTESIAN_POINT ( 'NONE',  ( 45.96182992765471909, 25.77822092656774799, 44.82232689504102296 ) ) ;
#972=CARTESIAN_POINT ( 'NONE',  ( 48.83862994770794330, 26.64118040159426570, 48.17861352429476796 ) ) ;
#973=ORIENTED_EDGE ( 'NONE', *, *, #15561, .T. ) ;
#980=VECTOR ( 'NONE', #29388, 1000.000000000000114 ) ;
#982=EDGE_CURVE ( 'NONE', #12544, #14642, #19707, .T. ) ;
#983=CARTESIAN_POINT ( 'NONE',  ( 45.96182992765471909, 25.90087065737812466, 44.82232689504102296 ) ) ;
#991=CARTESIAN_POINT ( 'NONE',  ( 46.99747725352182925, 22.88065857334294861, 48.98207832244369087 ) ) ;
#1015=CARTESIAN_POINT ( 'NONE',  ( 48.73570333863616355, 27.12287913140504259, 44.52463952959527660 ) ) ;
#1026=EDGE_CURVE ( 'NONE', #18648, #5411, #27388, .T. ) ;
#1040=CARTESIAN_POINT ( 'NONE',  ( 47.63716429968716426, 25.51960992152948293, 49.58068632438585865 ) ) ;
#1048=VERTEX_POINT ( 'NONE', #26098 ) ;
#1069=CARTESIAN_POINT ( 'NONE',  ( 49.98072202819531640, 26.94488759933318534, 47.19902993264913960 ) ) ;
#1072=CARTESIAN_POINT ( 'NONE',  ( 48.23388202445966755, 26.82822092656774515, 49.27628909396054979 ) ) ;
#1088=CARTESIAN_POINT ( 'NONE',  ( 47.20547626766766314, 25.38791119454915801, 44.97710074790751378 ) ) ;
#1091=CARTESIAN_POINT ( 'NONE',  ( 47.63716429968715005, 28.89696019071909916, 49.58068632438585155 ) ) ;
#1097=ORIENTED_EDGE ( 'NONE', *, *, #11165, .T. ) ;
#1098=ORIENTED_EDGE ( 'NONE', *, *, #936, .F. ) ;
#1103=CIRCLE ( 'NONE', #12667, 2.499999999999997335 ) ;
#1106=ORIENTED_EDGE ( 'NONE', *, *, #28798, .F. ) ;
#1109=CARTESIAN_POINT ( 'NONE',  ( 48.33536759636189828, 22.98765316579147111, 47.85212840585852234 ) ) ;
#1116=CARTESIAN_POINT ( 'NONE',  ( 46.99218062947583974, 25.05956182964376922, 49.08406571254116102 ) ) ;
#1130=CARTESIAN_POINT ( 'NONE',  ( 48.23388214087538017, 25.42822093266651606, 49.27628903457465270 ) ) ;
#1131=CARTESIAN_POINT ( 'NONE',  ( 44.70507715278255034, 26.34951373492759430, 46.92503878583765697 ) ) ;
#1137=EDGE_LOOP ( 'NONE', ( #12110, #26077, #7283, #32320, #17994, #20024 ) ) ;
#1149=EDGE_CURVE ( 'NONE', #32468, #456, #2131, .T. ) ;
#1156=( NAMED_UNIT ( * ) SI_UNIT ( $, .STERADIAN. ) SOLID_ANGLE_UNIT ( ) );
#1167=ORIENTED_EDGE ( 'NONE', *, *, #23303, .F. ) ;
#1169=CARTESIAN_POINT ( 'NONE',  ( 49.28428300279882990, 27.64787913140504116, 48.46772541801551171 ) ) ;
#1174=EDGE_CURVE ( 'NONE', #16189, #7375, #1691, .T. ) ;
#1182=LINE ( 'NONE', #16926, #17529 ) ;
#1193=CARTESIAN_POINT ( 'NONE',  ( 48.40186567930497574, 26.72957786121581947, 45.03923535223907493 ) ) ;
#1197=DIRECTION ( 'NONE',  ( 0.4544104193609900810, 0.000000000000000000, 0.8907924397839089847 ) ) ;
#1200=CARTESIAN_POINT ( 'NONE',  ( 47.09785597605719687, 23.12036939723557083, 47.04930799450080059 ) ) ;
#1240=DIRECTION ( 'NONE',  ( -0.4544104193609990738, 0.000000000000000000, -0.8907924397839043218 ) ) ;
#1252=B_SPLINE_CURVE_WITH_KNOTS ( 'NONE', 3,
 ( #26867, #9304, #29325, #14400, #1911, #29502 ),
 .UNSPECIFIED., .F., .F.,
 ( 4, 2, 4 ),
 ( 0.000000000000000000, 0.5000000000000000000, 1.000000000000000000 ),
 .UNSPECIFIED. ) ;
#1259=CARTESIAN_POINT ( 'NONE',  ( 48.43832450663380484, 22.91413368675619111, 48.25518855289821119 ) ) ;
#1263=CARTESIAN_POINT ( 'NONE',  ( 47.20353132263855400, 28.95286309983297812, 45.01455027646041174 ) ) ;
#1268=DIRECTION ( 'NONE',  ( 1.234978253042719660E-16, -1.000000000000000000, -1.109335647967047851E-31 ) ) ;
#1301=CARTESIAN_POINT ( 'NONE',  ( 49.32483701613094240, 25.72587066347689699, 45.91328182968236860 ) ) ;
#1303=AXIS2_PLACEMENT_3D ( 'NONE', #29470, #27000, #4513 ) ;
#1331=CARTESIAN_POINT ( 'NONE',  ( 44.91142894931555674, 27.99787913140503903, 45.63089057098605394 ) ) ;
#1344=CARTESIAN_POINT ( 'NONE',  ( 46.00908685603034343, 29.73284706826092361, 44.91496614357595263 ) ) ;
#1353=CARTESIAN_POINT ( 'NONE',  ( 45.52675994804781112, 25.43420399681022914, 49.47108226228596806 ) ) ;
#1354=DIRECTION ( 'NONE',  ( 0.000000000000000000, 0.000000000000000000, 1.000000000000000000 ) ) ;
#1356=ADVANCED_FACE ( 'NONE', ( #15568 ), #5410, .T. ) ;
#1358=CARTESIAN_POINT ( 'NONE',  ( 45.24946171279598417, 28.42124452788248234, 47.99220971130007030 ) ) ;
#1373=ORIENTED_EDGE ( 'NONE', *, *, #20000, .F. ) ;
#1398=CARTESIAN_POINT ( 'NONE',  ( 45.46177120706448704, 22.89977464660286444, 46.15605224449101485 ) ) ;
#1401=CARTESIAN_POINT ( 'NONE',  ( 47.03932003404746354, 22.95310733321322161, 45.41014739348889862 ) ) ;
#1411=LINE ( 'NONE', #23580, #3582 ) ;
#1424=CARTESIAN_POINT ( 'NONE',  ( 47.09785597605719687, 24.86874180309281712, 47.04930799450078638 ) ) ;
#1428=CARTESIAN_POINT ( 'NONE',  ( 47.20353132263855400, 28.25286309983298239, 45.01455027646040463 ) ) ;
#1439=CARTESIAN_POINT ( 'NONE',  ( 49.41945501136223839, 25.66454579807171399, 45.86501535757901848 ) ) ;
#1440=CARTESIAN_POINT ( 'NONE',  ( 47.05971367727331511, 23.09557481883486574, 47.78372960763746136 ) ) ;
#1445=DIRECTION ( 'NONE',  ( 1.234978253042719660E-16, -1.000000000000000000, -1.109335647967047851E-31 ) ) ;
#1473=ORIENTED_EDGE ( 'NONE', *, *, #4176, .T. ) ;
#1476=CARTESIAN_POINT ( 'NONE',  ( 48.83059987400640978, 29.08213139976340500, 48.97189179988551899 ) ) ;
#1484=ORIENTED_EDGE ( 'NONE', *, *, #1026, .T. ) ;
#1489=CARTESIAN_POINT ( 'NONE',  ( 44.77625694075214824, 28.81454579807170546, 48.23360063142255427 ) ) ;
#1495=AXIS2_PLACEMENT_3D ( 'NONE', #13900, #4203, #4037 ) ;
#1501=CARTESIAN_POINT ( 'NONE',  ( 48.80717017713595141, 25.21952976649965805, 48.15820438821415195 ) ) ;
#1508=CARTESIAN_POINT ( 'NONE',  ( 44.21498992391908445, 26.59488759933318747, 46.89958605635244027 ) ) ;
#1515=ADVANCED_FACE ( 'NONE', ( #9644 ), #29174, .F. ) ;
#1519=CARTESIAN_POINT ( 'NONE',  ( 48.94625023931840246, 26.67124452788248945, 46.10640627770148825 ) ) ;
#1526=CYLINDRICAL_SURFACE ( 'NONE', #624, 7.999999999999999112 ) ;
#1534=EDGE_LOOP ( 'NONE', ( #7705, #28572, #22447, #27008 ) ) ;
#1559=CARTESIAN_POINT ( 'NONE',  ( 46.45846941443645761, 22.99884124225578930, 45.79590206249746132 ) ) ;
#1591=CARTESIAN_POINT ( 'NONE',  ( 45.81741271322955100, 28.54452976649965024, 49.02305402274571122 ) ) ;
#1593=ADVANCED_FACE ( 'NONE', ( #30489 ), #27398, .T. ) ;
#1605=CARTESIAN_POINT ( 'NONE',  ( 49.28428300279882990, 26.24787913140504614, 48.46772541801551171 ) ) ;
#1606=CARTESIAN_POINT ( 'NONE',  ( 46.94469835654546586, 23.12036939723557083, 47.28539358874152043 ) ) ;
#1607=CYLINDRICAL_SURFACE ( 'NONE', #24275, 2.499999999999997335 ) ;
#1638=DIRECTION ( 'NONE',  ( 0.9761574614375596592, 0.2110602665713100790, 0.05069688703093150339 ) ) ;
#1656=ADVANCED_FACE ( 'NONE', ( #14735 ), #12274, .F. ) ;
#1670=CARTESIAN_POINT ( 'NONE',  ( 45.79384627280941089, 28.56618040159425931, 49.05938063676249072 ) ) ;
#1684=CARTESIAN_POINT ( 'NONE',  ( 46.04302072787191946, 22.93328494799376571, 45.69307819878901000 ) ) ;
#1691=( BOUNDED_CURVE ( )  B_SPLINE_CURVE ( 3, ( #9357, #24286, #9522, #9195 ),
 .UNSPECIFIED., .F., .F. ) 
 B_SPLINE_CURVE_WITH_KNOTS ( ( 4, 4 ),
 ( 1.099063246724959253, 1.220321128156879542 ),
 .UNSPECIFIED. ) 
 CURVE ( )  GEOMETRIC_REPRESENTATION_ITEM ( )  RATIONAL_B_SPLINE_CURVE ( ( 1.000000000000000000, 0.9987750858034806223, 0.9987750858034806223, 1.000000000000000000 ) ) 
 REPRESENTATION_ITEM ( '' )  );
#1707=AXIS2_PLACEMENT_3D ( 'NONE', #28904, #26587, #9527 ) ;
#1711=EDGE_CURVE ( 'NONE', #26418, #21141, #17412, .T. ) ;
#1728=LINE ( 'NONE', #4849, #7403 ) ;
#1730=AXIS2_PLACEMENT_3D ( 'NONE', #27571, #5086, #25109 ) ;
#1757=CARTESIAN_POINT ( 'NONE',  ( 48.37020515026796375, 25.16454579224780019, 49.54352682589573220 ) ) ;
#1759=CARTESIAN_POINT ( 'NONE',  ( 45.28286642839709231, 26.38619643316631524, 47.97516931882780966 ) ) ;
#1765=CARTESIAN_POINT ( 'NONE',  ( 49.06626442724220283, 29.56259918706335910, 46.29368314320814193 ) ) ;
#1771=CARTESIAN_POINT ( 'NONE',  ( 46.96268396749378127, 26.83121246473837473, 49.65201805493727960 ) ) ;
#1772=CARTESIAN_POINT ( 'NONE',  ( 47.33078969507813838, 23.03451764446789696, 48.23582531347169322 ) ) ;
#1773=CYLINDRICAL_SURFACE ( 'NONE', #24803, 7.999999999999999112 ) ;
#1778=DIRECTION ( 'NONE',  ( 1.234978253042719660E-16, -1.000000000000000000, -1.109335647967047851E-31 ) ) ;
#1782=FACE_OUTER_BOUND ( 'NONE', #24200, .T. ) ;
#1788=B_SPLINE_CURVE_WITH_KNOTS ( 'NONE', 3,
 ( #12617, #7026, #17024, #27046, #12286, #14580, #22280, #32308, #9819, #4896, #14909, #8444, #20748, #23697, #13224, #23533, #25991, #18275, #23851, #28306, #5826, #26153, #21217, #6134 ),
 .UNSPECIFIED., .F., .F.,
 ( 4, 2, 2, 2, 2, 2, 2, 2, 2, 2, 2, 4 ),
 ( 1.395353767516851130E-14, 2.664078908521907074E-05, 3.996118362085184644E-05, 4.662138088866923718E-05, 5.328157815648662115E-05, 6.660197269212707436E-05, 7.992236722776753434E-05, 0.0001065631562990277190, 0.0002131263125840656791, 0.0004262526251541395124, 0.0008525052502942665790, 0.001705010500574540011 ),
 .UNSPECIFIED. ) ;
#1798=CARTESIAN_POINT ( 'NONE',  ( 46.18657129672061501, 22.93807716476589675, 45.61868866909985343 ) ) ;
#1828=VECTOR ( 'NONE', #26022, 1000.000000000000000 ) ;
#1834=CARTESIAN_POINT ( 'NONE',  ( 44.70507715278255745, 28.44951373492759217, 46.92503878583765697 ) ) ;
#1847=CARTESIAN_POINT ( 'NONE',  ( 46.27402357847488901, 23.03451764446789696, 46.16421949815220671 ) ) ;
#1850=CARTESIAN_POINT ( 'NONE',  ( 49.76180767062073329, 24.76486642951281425, 48.77751362531137147 ) ) ;
#1863=DIRECTION ( 'NONE',  ( 0.8907924397839087627, 1.100109291107993941E-16, -0.4544104193609906361 ) ) ;
#1882=CARTESIAN_POINT ( 'NONE',  ( 48.59475124299144966, 29.58954579224780090, 45.61232171765963272 ) ) ;
#1911=CARTESIAN_POINT ( 'NONE',  ( 47.25101359556892078, 23.12036939723557083, 46.81322240026007364 ) ) ;
#1914=CARTESIAN_POINT ( 'NONE',  ( 44.74832014356462651, 28.42786309983298310, 46.92728461490987257 ) ) ;
#1927=EDGE_CURVE ( 'NONE', #2146, #30019, #20527, .T. ) ;
#1928=CARTESIAN_POINT ( 'NONE',  ( 45.24946171279598417, 29.82124452788248092, 47.99220971130007030 ) ) ;
#1930=CARTESIAN_POINT ( 'NONE',  ( 46.17891025898683921, 22.93807716476589675, 48.46582155994513386 ) ) ;
#1937=CARTESIAN_POINT ( 'NONE',  ( 48.28750925852675380, 22.93328494799376571, 45.80964605384927069 ) ) ;
#1939=EDGE_LOOP ( 'NONE', ( #1484, #32183, #18857, #25866, #22142, #10442 ) ) ;
#1945=APPLICATION_CONTEXT ( 'automotive_design' ) ;
#1951=EDGE_CURVE ( 'NONE', #5630, #5136, #14433, .T. ) ;
#1960=VERTEX_POINT ( 'NONE', #8952 ) ;
#1992=CARTESIAN_POINT ( 'NONE',  ( 48.16694854572211426, 25.86119643316632022, 49.14507740233662503 ) ) ;
#2016=CYLINDRICAL_SURFACE ( 'NONE', #12424, 7.999999999999999112 ) ;
#2023=LINE ( 'NONE', #24338, #21436 ) ;
#2036=ADVANCED_FACE ( 'NONE', ( #29634 ), #2387, .F. ) ;
#2038=CARTESIAN_POINT ( 'NONE',  ( 45.96182992765471909, 27.17822092656774657, 44.82232689504102296 ) ) ;
#2091=CARTESIAN_POINT ( 'NONE',  ( 48.86248627303584158, 22.86454579224779948, 46.10725065118596433 ) ) ;
#2094=CARTESIAN_POINT ( 'NONE',  ( 44.77625694075215534, 25.31454579807171257, 48.23360063142255427 ) ) ;
#2103=CARTESIAN_POINT ( 'NONE',  ( 48.61853364894580665, 22.95310733321322161, 46.43464276236652921 ) ) ;
#2123=AXIS2_PLACEMENT_3D ( 'NONE', #10950, #5539, #28660 ) ;
#2125=DIRECTION ( 'NONE',  ( 1.234978253042719660E-16, -1.000000000000000000, -1.109335647967047851E-31 ) ) ;
#2126=CARTESIAN_POINT ( 'NONE',  ( 45.45050395073641170, 20.53597436367637030, 46.96375251515745930 ) ) ;
#2131=LINE ( 'NONE', #11662, #2854 ) ;
#2137=LINE ( 'NONE', #17223, #18878 ) ;
#2138=CARTESIAN_POINT ( 'NONE',  ( 48.83862994770794330, 27.95457786121581734, 48.17861352429476796 ) ) ;
#2146=VERTEX_POINT ( 'NONE', #28616 ) ;
#2154=CARTESIAN_POINT ( 'NONE',  ( 49.28428300279882990, 26.24787913140504614, 48.46772541801551171 ) ) ;
#2164=CARTESIAN_POINT ( 'NONE',  ( 46.99023568444673060, 25.12451373492760354, 49.12151524109405898 ) ) ;
#2171=FACE_OUTER_BOUND ( 'NONE', #29334, .T. ) ;
#2176=( BOUNDED_CURVE ( )  B_SPLINE_CURVE ( 2, ( #16600, #11860, #28765, #1508, #31877, #18903, #26621, #21353, #31399 ),
 .UNSPECIFIED., .F., .F. ) 
 B_SPLINE_CURVE_WITH_KNOTS ( ( 3, 2, 2, 2, 3 ),
 ( 0.2499999988387273664, 0.2619047619047618625, 0.2857142857142856984, 0.3095238095238095344, 0.3214285702672988188 ),
 .UNSPECIFIED. ) 
 CURVE ( )  GEOMETRIC_REPRESENTATION_ITEM ( )  RATIONAL_B_SPLINE_CURVE ( ( 0.9330127018922199644, 0.9330126953578159466, 1.000000000000000000, 0.8660254037844387076, 1.000000000000000000, 0.8660254037844387076, 1.000000000000000000, 0.9330127084266226500, 0.9330127018922199644 ) ) 
 REPRESENTATION_ITEM ( '' )  );
#2190=ORIENTED_EDGE ( 'NONE', *, *, #7437, .T. ) ;
#2192=CARTESIAN_POINT ( 'NONE',  ( 49.40414881150629611, 22.86454579224779948, 47.16908566558144855 ) ) ;
#2198=CARTESIAN_POINT ( 'NONE',  ( 44.85846160380767600, 29.33657771061399089, 47.75346028685437005 ) ) ;
#2200=VERTEX_POINT ( 'NONE', #20416 ) ;
#2210=DIRECTION ( 'NONE',  ( 1.234978253042719660E-16, -1.000000000000000000, -1.109335647967047851E-31 ) ) ;
#2221=EDGE_CURVE ( 'NONE', #19350, #26434, #20578, .T. ) ;
#2227=ORIENTED_EDGE ( 'NONE', *, *, #224, .T. ) ;
#2232=ORIENTED_EDGE ( 'NONE', *, *, #29944, .F. ) ;
#2237=ORIENTED_EDGE ( 'NONE', *, *, #16879, .F. ) ;
#2262=CARTESIAN_POINT ( 'NONE',  ( 49.49063479933183629, 28.71291119454914664, 47.17357720316391578 ) ) ;
#2269=DIRECTION ( 'NONE',  ( 0.8907924160295465077, 1.100109261771873178E-16, -0.4544104659272754643 ) ) ;
#2281=VECTOR ( 'NONE', #28156, 1000.000000000000000 ) ;
#2289=CARTESIAN_POINT ( 'NONE',  ( 49.19517401419062708, 26.30920399681023270, 48.40991706654173754 ) ) ;
#2290=CARTESIAN_POINT ( 'NONE',  ( 48.91284552371730143, 29.49289516297709213, 46.12344667017377020 ) ) ;
#2300=CARTESIAN_POINT ( 'NONE',  ( 45.35708200440645044, 28.30457786121581876, 45.92000246470680480 ) ) ;
#2302=VERTEX_POINT ( 'NONE', #10339 ) ;
#2315=ORIENTED_EDGE ( 'NONE', *, *, #2221, .T. ) ;
#2326=CARTESIAN_POINT ( 'NONE',  ( 44.70507715278255745, 27.04951373492760069, 46.92503878583765697 ) ) ;
#2343=CARTESIAN_POINT ( 'NONE',  ( 48.28214861297873739, 25.48954579807170262, 49.37090702980594159 ) ) ;
#2359=CARTESIAN_POINT ( 'NONE',  ( 48.40186567930498285, 29.61618040159425647, 45.03923535223908203 ) ) ;
#2365=CARTESIAN_POINT ( 'NONE',  ( 45.06051016020553135, 29.34935871078510061, 48.15932322090515783 ) ) ;
#2387=PLANE ( 'NONE',  #11604 ) ;
#2394=ORIENTED_EDGE ( 'NONE', *, *, #12400, .T. ) ;
#2409=ORIENTED_EDGE ( 'NONE', *, *, #31113, .F. ) ;
#2415=CARTESIAN_POINT ( 'NONE',  ( 49.64105649875294546, 24.93604219378083187, 46.47965702198763438 ) ) ;
#2429=CARTESIAN_POINT ( 'NONE',  ( 45.24946171279598417, 27.72124452788248661, 47.99220971130007030 ) ) ;
#2445=ADVANCED_FACE ( 'NONE', ( #28546 ), #31168, .F. ) ;
#2455=CARTESIAN_POINT ( 'NONE',  ( 49.49063479933183629, 25.91291119454915304, 47.17357720316391578 ) ) ;
#2457=ORIENTED_EDGE ( 'NONE', *, *, #2724, .T. ) ;
#2472=EDGE_LOOP ( 'NONE', ( #26108, #20058 ) ) ;
#2473=CARTESIAN_POINT ( 'NONE',  ( 44.70507715278255034, 27.04951373492759714, 46.92503878583765697 ) ) ;
#2476=DIRECTION ( 'NONE',  ( 0.4544104193609915243, 0.000000000000000000, 0.8907924397839082076 ) ) ;
#2482=CARTESIAN_POINT ( 'NONE',  ( 49.64623691886138346, 24.93450097658724118, 46.50278401396133177 ) ) ;
#2483=CARTESIAN_POINT ( 'NONE',  ( 48.66895200406656130, 27.88420399681022488, 44.62753372671561181 ) ) ;
#2489=CARTESIAN_POINT ( 'NONE',  ( 45.36511207810797686, 27.20948166895303189, 45.12672418911604666 ) ) ;
#2501=CARTESIAN_POINT ( 'NONE',  ( 44.79156314060809763, 19.96454579224779380, 46.92953032342012420 ) ) ;
#2504=CARTESIAN_POINT ( 'NONE',  ( 48.23388202445966044, 26.95087065737812182, 49.27628909396054979 ) ) ;
#2511=CARTESIAN_POINT ( 'NONE',  ( 46.04844006429464542, 19.96454579224779380, 44.99211097489548905 ) ) ;
#2512=CARTESIAN_POINT ( 'NONE',  ( 49.49063479933183629, 28.09951373492759430, 47.17357720316391578 ) ) ;
#2516=CARTESIAN_POINT ( 'NONE',  ( 45.14219408817155710, 29.35362821189650617, 48.28978332510292404 ) ) ;
#2523=ADVANCED_FACE ( 'NONE', ( #11948 ), #1607, .T. ) ;
#2531=CARTESIAN_POINT ( 'NONE',  ( 45.96182992765471909, 15.77906836436399374, 44.82232689504101586 ) ) ;
#2554=EDGE_CURVE ( 'NONE', #15510, #16262, #29519, .T. ) ;
#2567=DIRECTION ( 'NONE',  ( 0.4544104193609917464, 0.000000000000000000, 0.8907924397839080966 ) ) ;
#2583=CARTESIAN_POINT ( 'NONE',  ( 49.49063479933183629, 28.01291119454915091, 47.17357720316391578 ) ) ;
#2611=CARTESIAN_POINT ( 'NONE',  ( 49.06491948623858690, 22.86454579224779948, 46.50408568885027449 ) ) ;
#2612=CARTESIAN_POINT ( 'NONE',  ( 47.20353132263855400, 28.90956182964375643, 45.01455027646041174 ) ) ;
#2613=AXIS2_PLACEMENT_3D ( 'NONE', #25201, #15511, #27987 ) ;
#2634=CARTESIAN_POINT ( 'NONE',  ( 48.94625023931840246, 28.85784706826092716, 46.10640627770150246 ) ) ;
#2637=DIRECTION ( 'NONE',  ( 0.4544104193609900810, 0.000000000000000000, 0.8907924397839089847 ) ) ;
#2638=ADVANCED_FACE ( 'NONE', ( #11791 ), #1773, .F. ) ;
#2649=CARTESIAN_POINT ( 'NONE',  ( 45.24946171279598417, 25.70784706826093569, 47.99220971130007030 ) ) ;
#2651=ORIENTED_EDGE ( 'NONE', *, *, #31061, .T. ) ;
#2654=CARTESIAN_POINT ( 'NONE',  ( 47.63716429968716426, 26.21960992152948577, 49.58068632438585865 ) ) ;
#2660=FACE_OUTER_BOUND ( 'NONE', #20395, .T. ) ;
#2680=CARTESIAN_POINT ( 'NONE',  ( 46.00908685603034343, 26.93284706826093355, 44.91496614357595263 ) ) ;
#2681=AXIS2_PLACEMENT_3D ( 'NONE', #3297, #30398, #3129 ) ;
#2724=EDGE_CURVE ( 'NONE', #11490, #28677, #15920, .T. ) ;
#2730=CARTESIAN_POINT ( 'NONE',  ( 47.63716429968715715, 26.09696019071910200, 49.58068632438583734 ) ) ;
#2751=CARTESIAN_POINT ( 'NONE',  ( 48.94625023931840957, 26.67124452788248945, 46.10640627770150246 ) ) ;
#2756=VERTEX_POINT ( 'NONE', #30009 ) ;
#2766=B_SPLINE_SURFACE_WITH_KNOTS ( 'NONE', 3, 3, ( 
 ( #18342, #13593, #31313, #10819, #31155, #18178 ),
 ( #21281, #11290, #13442, #18501, #23753, #18659 ),
 ( #28531, #28205, #6195, #11138, #6048, #23597 ),
 ( #16047, #10973, #8814, #1109, #13287, #1259 ),
 ( #8668, #5722, #25743, #26217, #3252, #30833 ),
 ( #21119, #28373, #5563, #15727, #20652, #13118 ) ),
 .UNSPECIFIED., .F., .F., .F.,
 ( 4, 2, 4 ),
 ( 4, 2, 4 ),
 ( 0.000000000000000000, 0.5000000000000000000, 1.000000000000000000 ),
 ( 0.000000000000000000, 0.5000000000000000000, 1.000000000000000000 ),
 .UNSPECIFIED. ) ;
#2769=CARTESIAN_POINT ( 'NONE',  ( 46.52714753771119405, 23.10527865767145173, 47.18627808671003265 ) ) ;
#2775=CARTESIAN_POINT ( 'NONE',  ( 48.89639543821420631, 22.86454579224779948, 46.17372366037167097 ) ) ;
#2776=CARTESIAN_POINT ( 'NONE',  ( 45.24946171279598417, 26.32124452788248803, 47.99220971130007030 ) ) ;
#2791=CARTESIAN_POINT ( 'NONE',  ( 47.63716429968716426, 29.01960992152946872, 49.58068632438585155 ) ) ;
#2793=CARTESIAN_POINT ( 'NONE',  ( 48.94625023931840246, 29.55784706826092645, 46.10640627770150246 ) ) ;
#2794=CONICAL_SURFACE ( 'NONE', #6443, 1.799999999999998490, 0.7853981633974489451 ) ;
#2817=CARTESIAN_POINT ( 'NONE',  ( 45.41164638504195494, 22.93807716476589675, 46.96173444154113241 ) ) ;
#2821=CARTESIAN_POINT ( 'NONE',  ( 49.41945501136223839, 29.16454579807170688, 45.86501535757901848 ) ) ;
#2833=CARTESIAN_POINT ( 'NONE',  ( 45.35708200440645044, 26.29118040159426428, 45.92000246470679770 ) ) ;
#2839=ORIENTED_EDGE ( 'NONE', *, *, #30504, .T. ) ;
#2854=VECTOR ( 'NONE', #1638, 999.9999999999997726 ) ;
#2861=AXIS2_PLACEMENT_3D ( 'NONE', #25544, #273, #20453 ) ;
#2863=DIRECTION ( 'NONE',  ( -0.8907924397839087627, -1.100109291107994187E-16, 0.4544104193609907472 ) ) ;
#2887=CARTESIAN_POINT ( 'NONE',  ( 48.23388202445966755, 26.82822092656774515, 49.27628909396054979 ) ) ;
#2902=CARTESIAN_POINT ( 'NONE',  ( 47.86364407361583062, 22.99884124225578930, 45.86888002329718717 ) ) ;
#2905=CARTESIAN_POINT ( 'NONE',  ( 46.99023568444673060, 27.13791119454915446, 49.12151524109405898 ) ) ;
#2926=ADVANCED_FACE ( 'NONE', ( #29150 ), #9614, .T. ) ;
#2930=CARTESIAN_POINT ( 'NONE',  ( 46.99023568444673060, 26.43791119454915517, 49.12151524109405898 ) ) ;
#2939=CARTESIAN_POINT ( 'NONE',  ( 47.88116631533108603, 22.93807716476589675, 45.54480264941530265 ) ) ;
#2949=DIRECTION ( 'NONE',  ( 1.234978253042719660E-16, -1.000000000000000000, -1.109335647967047851E-31 ) ) ;
#2988=CARTESIAN_POINT ( 'NONE',  ( 49.49063479933183629, 26.69951373492759927, 47.17357720316391578 ) ) ;
#2989=CARTESIAN_POINT ( 'NONE',  ( 48.18662509608405031, 29.29624452788248234, 49.18364984542562013 ) ) ;
#2997=DIRECTION ( 'NONE',  ( 0.4544104193609911913, 0.000000000000000000, 0.8907924397839085406 ) ) ;
#3000=CARTESIAN_POINT ( 'NONE',  ( 47.63716429968716426, 26.91960992152948151, 49.58068632438585865 ) ) ;
#3003=VERTEX_POINT ( 'NONE', #14222 ) ;
#3018=CARTESIAN_POINT ( 'NONE',  ( 49.73084373776887901, 24.88948912900243116, 46.55219242998139606 ) ) ;
#3038=CARTESIAN_POINT ( 'NONE',  ( 49.98072202819531640, 27.64488759933318818, 47.19902993264913960 ) ) ;
#3040=CARTESIAN_POINT ( 'NONE',  ( 48.23388202445966755, 15.77906836436399374, 49.27628909396055690 ) ) ;
#3044=DIRECTION ( 'NONE',  ( -0.8907924160295463967, -1.100109261771873301E-16, 0.4544104659272754088 ) ) ;
#3051=FACE_OUTER_BOUND ( 'NONE', #24335, .T. ) ;
#3058=LINE ( 'NONE', #23093, #26228 ) ;
#3064=CARTESIAN_POINT ( 'NONE',  ( 45.96182992765472619, 28.00087065737811898, 44.82232689504102296 ) ) ;
#3084=CARTESIAN_POINT ( 'NONE',  ( 48.80717017713595141, 28.67622849631042570, 48.15820438821415195 ) ) ;
#3099=CARTESIAN_POINT ( 'NONE',  ( 45.79384627280941800, 25.76618040159426926, 49.05938063676250493 ) ) ;
#3101=DIRECTION ( 'NONE',  ( 0.4544104193609903586, 0.000000000000000000, 0.8907924397839087627 ) ) ;
#3115=CARTESIAN_POINT ( 'NONE',  ( 48.55603101936429056, 22.91413368675619111, 45.98877541807350156 ) ) ;
#3129=DIRECTION ( 'NONE',  ( 0.4544104193609900810, 0.000000000000000000, 0.8907924397839089847 ) ) ;
#3131=CARTESIAN_POINT ( 'NONE',  ( 48.46535932150934656, 28.28954579807170688, 49.73005965046827015 ) ) ;
#3136=CARTESIAN_POINT ( 'NONE',  ( 47.35966831703180446, 25.13711290387551855, 44.54181020796264079 ) ) ;
#3142=ORIENTED_EDGE ( 'NONE', *, *, #26856, .T. ) ;
#3146=CARTESIAN_POINT ( 'NONE',  ( 47.20547626766766314, 28.27451373492759501, 44.97710074790751378 ) ) ;
#3148=CARTESIAN_POINT ( 'NONE',  ( 44.70507715278255745, 29.76291119454914380, 46.92503878583764987 ) ) ;
#3161=CARTESIAN_POINT ( 'NONE',  ( 46.48525799733394592, 23.04411619146717882, 47.99360027521537830 ) ) ;
#3181=CARTESIAN_POINT ( 'NONE',  ( 49.72060376828096651, 24.89739800709606499, 46.58538876707991960 ) ) ;
#3190=CARTESIAN_POINT ( 'NONE',  ( 48.77568013947721681, 22.93807716476589675, 47.29834112010470903 ) ) ;
#3206=CARTESIAN_POINT ( 'NONE',  ( 45.44030796846719511, 22.86454579224779948, 45.92951929762858043 ) ) ;
#3219=CARTESIAN_POINT ( 'NONE',  ( 46.20008674485251987, 20.53597436367637030, 48.43317895773266457 ) ) ;
#3222=ORIENTED_EDGE ( 'NONE', *, *, #24187, .F. ) ;
#3225=CARTESIAN_POINT ( 'NONE',  ( 45.37383841111020644, 22.88065857334295217, 47.92876263475718446 ) ) ;
#3230=CARTESIAN_POINT ( 'NONE',  ( 47.09785597605719687, 23.12036939723557083, 47.04930799450080059 ) ) ;
#3238=ORIENTED_EDGE ( 'NONE', *, *, #31675, .F. ) ;
#3252=CARTESIAN_POINT ( 'NONE',  ( 48.56989418307995976, 22.92747281079970634, 48.00427463845466036 ) ) ;
#3253=DIRECTION ( 'NONE',  ( -1.234978253042719660E-16, 1.000000000000000000, 1.109335647967047851E-31 ) ) ;
#3255=CARTESIAN_POINT ( 'NONE',  ( 49.44739180854976013, 25.23456182964376993, 47.17133137409169308 ) ) ;
#3262=CARTESIAN_POINT ( 'NONE',  ( 49.76180767062073329, 24.76486642951281780, 48.77751362531136436 ) ) ;
#3272=CARTESIAN_POINT ( 'NONE',  ( 48.01680169312755453, 22.93807716476589675, 45.63279442905645311 ) ) ;
#3273=CARTESIAN_POINT ( 'NONE',  ( 45.79384627280941800, 26.46618040159426499, 49.05938063676250493 ) ) ;
#3283=VERTEX_POINT ( 'NONE', #26155 ) ;
#3291=CARTESIAN_POINT ( 'NONE',  ( 48.15316146078545501, 22.93807716476589320, 48.40645952689865084 ) ) ;
#3297=CARTESIAN_POINT ( 'NONE',  ( 47.09785597605719687, 24.76454579224779806, 47.04930799450078638 ) ) ;
#3315=CARTESIAN_POINT ( 'NONE',  ( 47.23302798462060537, 29.28121246473837047, 44.44659793406428605 ) ) ;
#3316=CARTESIAN_POINT ( 'NONE',  ( 49.49063479933183629, 28.71291119454914664, 47.17357720316391578 ) ) ;
#3327=VECTOR ( 'NONE', #5269, 999.9999999999998863 ) ;
#3339=ADVANCED_FACE ( 'NONE', ( #13058 ), #4378, .F. ) ;
#3342=CARTESIAN_POINT ( 'NONE',  ( 46.77981311948828846, 23.11533908250407165, 46.84298161117587966 ) ) ;
#3367=CARTESIAN_POINT ( 'NONE',  ( 47.22751897799751220, 27.11988759933318960, 44.55267275764142454 ) ) ;
#3381=ORIENTED_EDGE ( 'NONE', *, *, #25020, .F. ) ;
#3386=CARTESIAN_POINT ( 'NONE',  ( 48.94625023931840957, 25.97124452788249371, 46.10640627770150246 ) ) ;
#3390=CARTESIAN_POINT ( 'NONE',  ( 47.09785597605719687, 15.77906836436399374, 47.04930799450078638 ) ) ;
#3413=CYLINDRICAL_SURFACE ( 'NONE', #26900, 2.499999999999997335 ) ;
#3415=CARTESIAN_POINT ( 'NONE',  ( 44.74832014356462651, 28.38456182964376495, 46.92728461490987257 ) ) ;
#3426=CARTESIAN_POINT ( 'NONE',  ( 48.35473289974375177, 22.86454579224779948, 45.11188864597616544 ) ) ;
#3438=ADVANCED_FACE ( 'NONE', ( #11714 ), #16616, .F. ) ;
#3458=CARTESIAN_POINT ( 'NONE',  ( 46.37506696020427910, 29.22387735013030152, 44.70869714466342515 ) ) ;
#3474=CARTESIAN_POINT ( 'NONE',  ( 47.23302798462060537, 28.58121246473837118, 44.44659793406428605 ) ) ;
#3484=CARTESIAN_POINT ( 'NONE',  ( 44.87087493598345134, 26.77587066347689415, 48.18533415931919706 ) ) ;
#3491=DIRECTION ( 'NONE',  ( 1.234978253042719660E-16, -1.000000000000000000, -1.109335647967047851E-31 ) ) ;
#3497=CARTESIAN_POINT ( 'NONE',  ( 48.40186567930498285, 29.52957786121581663, 45.03923535223908203 ) ) ;
#3510=LINE ( 'NONE', #891, #2281 ) ;
#3511=VERTEX_POINT ( 'NONE', #3833 ) ;
#3530=CARTESIAN_POINT ( 'NONE',  ( 45.84097905237065618, 19.96454579224779380, 48.98672734302541443 ) ) ;
#3539=CARTESIAN_POINT ( 'NONE',  ( 46.04844006429464542, 22.80400562401889530, 44.99211097489548905 ) ) ;
#3545=CARTESIAN_POINT ( 'NONE',  ( 49.49063479933183629, 25.91291119454915304, 47.17357720316391578 ) ) ;
#3566=FACE_OUTER_BOUND ( 'NONE', #20244, .T. ) ;
#3570=CARTESIAN_POINT ( 'NONE',  ( 48.37829923888483563, 25.35122849631043351, 45.07556196625585443 ) ) ;
#3577=CIRCLE ( 'NONE', #26122, 4.200000000000000178 ) ;
#3582=VECTOR ( 'NONE', #13741, 1000.000000000000227 ) ;
#3583=CARTESIAN_POINT ( 'NONE',  ( 46.04844006429464542, 22.86454579224779948, 44.99211097489548905 ) ) ;
#3593=CARTESIAN_POINT ( 'NONE',  ( 47.54376155772514778, 23.10527865767145528, 46.66768365041815514 ) ) ;
#3613=CARTESIAN_POINT ( 'NONE',  ( 47.86511985000206693, 22.93807716476589320, 48.55339511290479493 ) ) ;
#3635=CARTESIAN_POINT ( 'NONE',  ( 49.98072202819531640, 28.34488759933318747, 47.19902993264913960 ) ) ;
#3638=CARTESIAN_POINT ( 'NONE',  ( 45.24946171279598417, 25.00784706826093640, 47.99220971130007030 ) ) ;
#3664=CARTESIAN_POINT ( 'NONE',  ( 48.94625023931840246, 28.07124452788248803, 46.10640627770149536 ) ) ;
#3671=CARTESIAN_POINT ( 'NONE',  ( 49.68665970317314873, 24.91671509559730069, 46.58149026817019944 ) ) ;
#3690=CARTESIAN_POINT ( 'NONE',  ( 48.04075769285628894, 25.18284706826092290, 48.89770225776209145 ) ) ;
#3698=ORIENTED_EDGE ( 'NONE', *, *, #20818, .F. ) ;
#3710=ADVANCED_FACE ( 'NONE', ( #8406, #30895 ), #11037, .F. ) ;
#3711=CARTESIAN_POINT ( 'NONE',  ( 48.18662509608405031, 25.79624452788248945, 49.18364984542562013 ) ) ;
#3712=EDGE_CURVE ( 'NONE', #24927, #14398, #16156, .T. ) ;
#3736=CARTESIAN_POINT ( 'NONE',  ( 45.81741271322955100, 29.24452976649964597, 49.02305402274571122 ) ) ;
#3756=CARTESIAN_POINT ( 'NONE',  ( 47.40417757965286683, 23.10527845304106620, 46.57712699531703038 ) ) ;
#3758=EDGE_LOOP ( 'NONE', ( #26479, #12252, #8267 ) ) ;
#3762=CARTESIAN_POINT ( 'NONE',  ( 48.35473289974373756, 19.96454579224779380, 45.11188864597615833 ) ) ;
#3766=CARTESIAN_POINT ( 'NONE',  ( 48.28750925852675380, 22.93328494799376571, 45.80964605384927069 ) ) ;
#3771=ORIENTED_EDGE ( 'NONE', *, *, #2724, .F. ) ;
#3780=CARTESIAN_POINT ( 'NONE',  ( 48.40423897560355471, 29.16454579224780019, 44.91779129072006072 ) ) ;
#3795=CARTESIAN_POINT ( 'NONE',  ( 49.28428300279882990, 28.34787913140504045, 48.46772541801551171 ) ) ;
#3806=CARTESIAN_POINT ( 'NONE',  ( 45.24946171279598417, 29.20784706826092503, 47.99220971130007030 ) ) ;
#3818=CARTESIAN_POINT ( 'NONE',  ( 48.74520800137798204, 20.53597436367637030, 47.13486347384411346 ) ) ;
#3826=CARTESIAN_POINT ( 'NONE',  ( 47.20547626766764893, 26.08791119454915730, 44.97710074790751378 ) ) ;
#3833=CARTESIAN_POINT ( 'NONE',  ( 48.35473289974373756, 22.80400562401889530, 45.11188864597615833 ) ) ;
#3841=CARTESIAN_POINT ( 'NONE',  ( 47.96808403254358666, 29.45344092395630753, 49.08756527095943056 ) ) ;
#3842=VERTEX_POINT ( 'NONE', #22161 ) ;
#3894=CARTESIAN_POINT ( 'NONE',  ( 46.95686452149019630, 22.86454579224779948, 49.04468102550210773 ) ) ;
#3897=CARTESIAN_POINT ( 'NONE',  ( 48.91284552371730143, 28.83619643316631453, 46.12344667017377020 ) ) ;
#3906=CARTESIAN_POINT ( 'NONE',  ( 48.73570333863616355, 25.72287913140504756, 44.52463952959527660 ) ) ;
#3920=CARTESIAN_POINT ( 'NONE',  ( 47.22751897799751220, 25.71988759933319102, 44.55267275764142454 ) ) ;
#3931=EDGE_CURVE ( 'NONE', #4981, #14884, #8218, .T. ) ;
#3949=CARTESIAN_POINT ( 'NONE',  ( 49.54111243405073139, 29.13489273995354267, 47.87666846268844267 ) ) ;
#3951=ORIENTED_EDGE ( 'NONE', *, *, #31908, .F. ) ;
#3958=CARTESIAN_POINT ( 'NONE',  ( 48.96852009960340268, 19.86454579224779948, 46.09504611384270589 ) ) ;
#3962=CARTESIAN_POINT ( 'NONE',  ( 44.09250526802607340, 27.35621246473837331, 46.89322480343881949 ) ) ;
#3973=CARTESIAN_POINT ( 'NONE',  ( 47.20547626766766314, 28.27451373492759501, 44.97710074790751378 ) ) ;
#3979=MECHANICAL_DESIGN_GEOMETRIC_PRESENTATION_REPRESENTATION('',(#24430),#21804);
#3986=CARTESIAN_POINT ( 'NONE',  ( 49.49063479933183629, 25.91291119454916014, 47.17357720316391578 ) ) ;
#4000=EDGE_CURVE ( 'NONE', #23526, #19268, #475, .T. ) ;
#4020=EDGE_LOOP ( 'NONE', ( #12850, #30333, #22793, #3771 ) ) ;
#4027=CARTESIAN_POINT ( 'NONE',  ( 47.17436303681730436, 22.98765316579147466, 45.57618128815960290 ) ) ;
#4037=DIRECTION ( 'NONE',  ( 0.4544104193609903586, 0.000000000000000000, 0.8907924397839087627 ) ) ;
#4053=CARTESIAN_POINT ( 'NONE',  ( 48.16694854572211426, 27.26119643316631880, 49.14507740233662503 ) ) ;
#4063=CARTESIAN_POINT ( 'NONE',  ( 50.10320668408830613, 24.90621246473838468, 47.20539118556276037 ) ) ;
#4064=CARTESIAN_POINT ( 'NONE',  ( 46.59799852009219734, 22.98879437201065912, 48.43017694493634195 ) ) ;
#4083=ORIENTED_EDGE ( 'NONE', *, *, #20853, .T. ) ;
#4084=LINE ( 'NONE', #31347, #263 ) ;
#4099=CARTESIAN_POINT ( 'NONE',  ( 49.59034552300744281, 29.16454579224780019, 47.24294646780535345 ) ) ;
#4102=EDGE_LOOP ( 'NONE', ( #22436, #25184, #20452, #30552 ) ) ;
#4129=CARTESIAN_POINT ( 'NONE',  ( 46.99023568444673060, 27.92451373492759714, 49.12151524109405898 ) ) ;
#4131=DIRECTION ( 'NONE',  ( 1.234978253042719660E-16, -1.000000000000000000, -1.109335647967047851E-31 ) ) ;
#4145=CARTESIAN_POINT ( 'NONE',  ( 44.26921014953015288, 25.23153309617947926, 48.49225502104211927 ) ) ;
#4161=VERTEX_POINT ( 'NONE', #12609 ) ;
#4165=VECTOR ( 'NONE', #31582, 1000.000000000000000 ) ;
#4173=CARTESIAN_POINT ( 'NONE',  ( 48.05211795450447454, 25.13954579807170120, 48.91997206816282784 ) ) ;
#4174=CARTESIAN_POINT ( 'NONE',  ( 48.23388202445966755, 29.05087065737811969, 49.27628909396056400 ) ) ;
#4176=EDGE_CURVE ( 'NONE', #3842, #3511, #29596, .T. ) ;
#4178=VERTEX_POINT ( 'NONE', #31967 ) ;
#4180=ORIENTED_EDGE ( 'NONE', *, *, #17896, .T. ) ;
#4203=DIRECTION ( 'NONE',  ( 1.234978253042719660E-16, -1.000000000000000000, -1.109335647967047851E-31 ) ) ;
#4226=CARTESIAN_POINT ( 'NONE',  ( 46.99218062947583974, 29.30286309983297954, 49.08406571254116102 ) ) ;
#4239=CARTESIAN_POINT ( 'NONE',  ( 44.09250526802607340, 28.05621246473836905, 46.89322480343881949 ) ) ;
#4240=CARTESIAN_POINT ( 'NONE',  ( 47.57660806753134608, 22.93328494799376216, 48.69940892914074482 ) ) ;
#4244=CARTESIAN_POINT ( 'NONE',  ( 49.40414881150628901, 22.86454579224779948, 47.16908566558146987 ) ) ;
#4283=ORIENTED_EDGE ( 'NONE', *, *, #26524, .T. ) ;
#4297=CARTESIAN_POINT ( 'NONE',  ( 48.18662509608405031, 27.98284706826092716, 49.18364984542562013 ) ) ;
#4298=EDGE_CURVE ( 'NONE', #10117, #14884, #25873, .T. ) ;
#4328=CARTESIAN_POINT ( 'NONE',  ( 48.94625023931840246, 29.55784706826092645, 46.10640627770150246 ) ) ;
#4329=DIRECTION ( 'NONE',  ( 0.4441739386572013393, 0.2110602665713099402, 0.8707256032141217350 ) ) ;
#4332=CARTESIAN_POINT ( 'NONE',  ( 45.32865359766977775, 29.36272681631152182, 48.52962753590826850 ) ) ;
#4377=EDGE_LOOP ( 'NONE', ( #27224, #28856, #6580, #19903 ) ) ;
#4378=TOROIDAL_SURFACE ( 'NONE', #19035, 2.799999999999998490, 0.2999999999999999334 ) ;
#4383=CARTESIAN_POINT ( 'NONE',  ( 45.81741271322955100, 27.84452976649965450, 49.02305402274571122 ) ) ;
#4394=CARTESIAN_POINT ( 'NONE',  ( 47.23302798462060537, 25.78121246473837758, 44.44659793406428605 ) ) ;
#4396=CARTESIAN_POINT ( 'NONE',  ( 47.00684970613776414, 22.92747281079970278, 48.80161379910075681 ) ) ;
#4399=EDGE_LOOP ( 'NONE', ( #16639, #14822, #774, #8017 ) ) ;
#4404=CARTESIAN_POINT ( 'NONE',  ( 48.15507178867567717, 22.98879437201065912, 46.03001840850954807 ) ) ;
#4406=VERTEX_POINT ( 'NONE', #921 ) ;
#4461=CARTESIAN_POINT ( 'NONE',  ( 48.83862994770794330, 29.44118040159425931, 48.17861352429476796 ) ) ;
#4470=CYLINDRICAL_SURFACE ( 'NONE', #5281, 7.999999999999999112 ) ;
#4472=DIRECTION ( 'NONE',  ( 1.234978253042719660E-16, -1.000000000000000000, -1.109335647967047851E-31 ) ) ;
#4479=CARTESIAN_POINT ( 'NONE',  ( 45.91356333913565635, 25.13954579807170475, 44.72770895919563117 ) ) ;
#4482=CARTESIAN_POINT ( 'NONE',  ( 48.83059987400640978, 26.98213139976341068, 48.97189179988551899 ) ) ;
#4486=CARTESIAN_POINT ( 'NONE',  ( 49.40414881150629611, 22.86454579224779948, 47.16908566558144855 ) ) ;
#4495=ORIENTED_EDGE ( 'NONE', *, *, #32399, .F. ) ;
#4496=CARTESIAN_POINT ( 'NONE',  ( 44.78102299139906251, 29.29862254614766925, 46.54638771186188961 ) ) ;
#4497=ORIENTED_EDGE ( 'NONE', *, *, #20853, .F. ) ;
#4513=DIRECTION ( 'NONE',  ( -0.5442436726714893203, -6.721291001053903893E-17, 0.8389271868029124501 ) ) ;
#4518=DIRECTION ( 'NONE',  ( 0.4544104193609913023, 0.000000000000000000, 0.8907924397839084296 ) ) ;
#4520=ORIENTED_EDGE ( 'NONE', *, *, #17116, .T. ) ;
#4556=CARTESIAN_POINT ( 'NONE',  ( 49.41945501136223839, 26.36454579807171328, 45.86501535757901848 ) ) ;
#4557=CARTESIAN_POINT ( 'NONE',  ( 46.93112133629608707, 23.10527865767144817, 47.61204104636720302 ) ) ;
#4562=CARTESIAN_POINT ( 'NONE',  ( 47.86364407361583062, 22.99884124225578930, 45.86888002329718717 ) ) ;
#4579=CARTESIAN_POINT ( 'NONE',  ( 49.32483701613094240, 26.42587066347689984, 45.91328182968236860 ) ) ;
#4593=CARTESIAN_POINT ( 'NONE',  ( 49.49063479933183629, 29.41291119454914593, 47.17357720316391578 ) ) ;
#4598=LINE ( 'NONE', #24458, #980 ) ;
#4602=LINE ( 'NONE', #3958, #417 ) ;
#4618=CARTESIAN_POINT ( 'NONE',  ( 46.99023568444673060, 25.82451373492759927, 49.12151524109405898 ) ) ;
#4638=CARTESIAN_POINT ( 'NONE',  ( 44.43390428149366755, 25.11486642951281212, 45.32110236369020839 ) ) ;
#4649=VERTEX_POINT ( 'NONE', #31769 ) ;
#4655=CARTESIAN_POINT ( 'NONE',  ( 45.86052195822112765, 29.24126980604143355, 44.96013611432259438 ) ) ;
#4664=( BOUNDED_CURVE ( )  B_SPLINE_CURVE ( 3, ( #22093, #6681, #32124, #3894 ),
 .UNSPECIFIED., .F., .F. ) 
 B_SPLINE_CURVE_WITH_KNOTS ( ( 4, 4 ),
 ( 5.062864179022701805, 5.184122060454623870 ),
 .UNSPECIFIED. ) 
 CURVE ( )  GEOMETRIC_REPRESENTATION_ITEM ( )  RATIONAL_B_SPLINE_CURVE ( ( 1.000000000000000000, 0.9987750858034806223, 0.9987750858034806223, 1.000000000000000000 ) ) 
 REPRESENTATION_ITEM ( '' )  );
#4667=EDGE_CURVE ( 'NONE', #13719, #306, #1728, .T. ) ;
#4670=LINE ( 'NONE', #2531, #6566 ) ;
#4693=ORIENTED_EDGE ( 'NONE', *, *, #6115, .F. ) ;
#4723=CARTESIAN_POINT ( 'NONE',  ( 48.14727188781975542, 19.96454579224779380, 49.10650501410607660 ) ) ;
#4724=CARTESIAN_POINT ( 'NONE',  ( 44.70507715278255745, 26.26291119454915801, 46.92503878583765697 ) ) ;
#4745=CARTESIAN_POINT ( 'NONE',  ( 46.20089404322238380, 22.99884124225578574, 48.14463855678482673 ) ) ;
#4748=VECTOR ( 'NONE', #18074, 999.9999999999998863 ) ;
#4754=CARTESIAN_POINT ( 'NONE',  ( 49.23437818303271030, 22.84434098701873594, 46.83627993336631334 ) ) ;
#4756=CARTESIAN_POINT ( 'NONE',  ( 45.28286642839709231, 29.84289516297709710, 47.97516931882780966 ) ) ;
#4766=CARTESIAN_POINT ( 'NONE',  ( 48.83862994770795041, 25.85457786121582302, 48.17861352429476085 ) ) ;
#4787=CARTESIAN_POINT ( 'NONE',  ( 48.18662509608405031, 25.88284706826093284, 49.18364984542562013 ) ) ;
#4791=CARTESIAN_POINT ( 'NONE',  ( 48.23388202445966755, 27.52822092656774089, 49.27628909396054979 ) ) ;
#4817=CARTESIAN_POINT ( 'NONE',  ( 47.20547626766766314, 28.97451373492759430, 44.97710074790751378 ) ) ;
#4849=CARTESIAN_POINT ( 'NONE',  ( 48.14727188781975542, 22.86454579224779948, 49.10650501410607660 ) ) ;
#4868=( BOUNDED_CURVE ( )  B_SPLINE_CURVE ( 3, ( #31263, #28789, #16145, #21548 ),
 .UNSPECIFIED., .F., .F. ) 
 B_SPLINE_CURVE_WITH_KNOTS ( ( 4, 4 ),
 ( 5.062864179022703581, 5.184122060454621206 ),
 .UNSPECIFIED. ) 
 CURVE ( )  GEOMETRIC_REPRESENTATION_ITEM ( )  RATIONAL_B_SPLINE_CURVE ( ( 1.000000000000000000, 0.9987750858034806223, 0.9987750858034806223, 1.000000000000000000 ) ) 
 REPRESENTATION_ITEM ( '' )  );
#4890=CARTESIAN_POINT ( 'NONE',  ( 48.94625023931840246, 28.07124452788248803, 46.10640627770150246 ) ) ;
#4896=CARTESIAN_POINT ( 'NONE',  ( 47.12654256966948907, 29.60334677283180582, 44.98830670686451327 ) ) ;
#4898=ORIENTED_EDGE ( 'NONE', *, *, #23574, .T. ) ;
#4917=CARTESIAN_POINT ( 'NONE',  ( 48.83059987400640978, 26.28213139976340784, 48.97189179988551899 ) ) ;
#4918=CARTESIAN_POINT ( 'NONE',  ( 46.99218062947583974, 29.25956182964375429, 49.08406571254116102 ) ) ;
#4920=VERTEX_POINT ( 'NONE', #26316 ) ;
#4928=CARTESIAN_POINT ( 'NONE',  ( 45.79384627280941800, 25.67957786121582231, 49.05938063676250493 ) ) ;
#4937=CARTESIAN_POINT ( 'NONE',  ( 49.49063479933183629, 29.49951373492759288, 47.17357720316391578 ) ) ;
#4938=EDGE_LOOP ( 'NONE', ( #4980, #27231, #29317, #19712 ) ) ;
#4953=CARTESIAN_POINT ( 'NONE',  ( 47.22751897799751220, 27.94253733014356200, 44.55267275764142454 ) ) ;
#4959=DIRECTION ( 'NONE',  ( -0.9986540920324801229, -1.233316085972235080E-16, -0.05186525298099629866 ) ) ;
#4967=ORIENTED_EDGE ( 'NONE', *, *, #12361, .T. ) ;
#4972=CARTESIAN_POINT ( 'NONE',  ( 49.50463956150868228, 24.97506988763833036, 46.15219500445987677 ) ) ;
#4973=CARTESIAN_POINT ( 'NONE',  ( 45.47421713364555274, 22.88065857334294861, 45.99599230681428708 ) ) ;
#4980=ORIENTED_EDGE ( 'NONE', *, *, #14575, .F. ) ;
#4981=VERTEX_POINT ( 'NONE', #32058 ) ;
#4983=DIRECTION ( 'NONE',  ( 1.234978253042719660E-16, -1.000000000000000000, -1.109335647967047851E-31 ) ) ;
#4993=CARTESIAN_POINT ( 'NONE',  ( 47.09785597605719687, 24.86454579224779593, 47.04930799450078638 ) ) ;
#5038=EDGE_LOOP ( 'NONE', ( #16945, #11537, #670 ) ) ;
#5052=CARTESIAN_POINT ( 'NONE',  ( 45.33610888377108239, 19.86454579224779948, 45.90639628189065746 ) ) ;
#5055=CARTESIAN_POINT ( 'NONE',  ( 48.83862994770794330, 29.35457786121581591, 48.17861352429476796 ) ) ;
#5063=VERTEX_POINT ( 'NONE', #20374 ) ;
#5072=CARTESIAN_POINT ( 'NONE',  ( 45.97377588299919893, 23.04411619146718238, 46.99092872297675427 ) ) ;
#5078=CARTESIAN_POINT ( 'NONE',  ( 46.02876340639226527, 28.96789516297709355, 44.95353858666495483 ) ) ;
#5086=DIRECTION ( 'NONE',  ( 0.4441739386572013948, 0.2110602665713099679, 0.8707256032141218460 ) ) ;
#5108=CARTESIAN_POINT ( 'NONE',  ( 49.65101332465108186, 24.93501648625822398, 46.52608845888364186 ) ) ;
#5109=CARTESIAN_POINT ( 'NONE',  ( 48.94625023931840957, 26.75784706826093284, 46.10640627770150246 ) ) ;
#5114=CARTESIAN_POINT ( 'NONE',  ( 46.96819297411687444, 27.46988759933318747, 49.54594323136014822 ) ) ;
#5123=FACE_OUTER_BOUND ( 'NONE', #6689, .T. ) ;
#5125=B_SPLINE_SURFACE_WITH_KNOTS ( 'NONE', 3, 3, ( 
 ( #10634, #20625, #278, #30651, #2902, #10304 ),
 ( #28019, #8316, #20290, #12931, #28345, #30322 ),
 ( #7836, #27860, #15382, #25388, #22919, #436 ),
 ( #10464, #11112, #31608, #4027, #21408, #16499 ),
 ( #1559, #26351, #18476, #1401, #21095, #13890 ),
 ( #14048, #8954, #18786, #6169, #19110, #16175 ) ),
 .UNSPECIFIED., .F., .F., .F.,
 ( 4, 2, 4 ),
 ( 4, 2, 4 ),
 ( 0.000000000000000000, 0.5000000000000000000, 1.000000000000000000 ),
 ( 0.000000000000000000, 0.5000000000000000000, 1.000000000000000000 ),
 .UNSPECIFIED. ) ;
#5136=VERTEX_POINT ( 'NONE', #4973 ) ;
#5142=CARTESIAN_POINT ( 'NONE',  ( 48.94625023931840957, 27.45784706826093213, 46.10640627770150246 ) ) ;
#5147=CARTESIAN_POINT ( 'NONE',  ( 45.99596926870651004, 19.86454579224779948, 44.88925112391522987 ) ) ;
#5153=ORIENTED_EDGE ( 'NONE', *, *, #16441, .T. ) ;
#5154=DIRECTION ( 'NONE',  ( -0.8907924397839087627, -1.100109291107994187E-16, 0.4544104193609907472 ) ) ;
#5183=ORIENTED_EDGE ( 'NONE', *, *, #11051, .F. ) ;
#5192=AXIS2_PLACEMENT_3D ( 'NONE', #27291, #29593, #24834 ) ;
#5194=CARTESIAN_POINT ( 'NONE',  ( 45.52675994804781112, 26.01155426599985532, 49.47108226228597516 ) ) ;
#5205=CARTESIAN_POINT ( 'NONE',  ( 46.27991722120741258, 29.86454579224779948, 45.44588160288975587 ) ) ;
#5215=CARTESIAN_POINT ( 'NONE',  ( 48.18662509608405031, 27.89624452788248377, 49.18364984542562013 ) ) ;
#5218=ORIENTED_EDGE ( 'NONE', *, *, #2554, .F. ) ;
#5233=ADVANCED_FACE ( 'NONE', ( #18833 ), #13777, .F. ) ;
#5235=CARTESIAN_POINT ( 'NONE',  ( 46.53577443378190281, 23.10527845304106620, 47.02011620365084354 ) ) ;
#5241=CARTESIAN_POINT ( 'NONE',  ( 49.32738855505253639, 29.28333847617543739, 46.19910593250668285 ) ) ;
#5242=CARTESIAN_POINT ( 'NONE',  ( 48.23388202445966044, 26.25087065737812253, 49.27628909396054979 ) ) ;
#5243=CARTESIAN_POINT ( 'NONE',  ( 45.24946171279598417, 25.62124452788248874, 47.99220971130007030 ) ) ;
#5253=CARTESIAN_POINT ( 'NONE',  ( 48.40186567930497574, 25.32957786121582444, 45.03923535223908203 ) ) ;
#5256=CARTESIAN_POINT ( 'NONE',  ( 48.77917452769285944, 20.36454579224779948, 50.34524002170125101 ) ) ;
#5261=CARTESIAN_POINT ( 'NONE',  ( 46.99023568444673060, 27.92451373492759714, 49.12151524109405898 ) ) ;
#5264=LINE ( 'NONE', #25288, #21429 ) ;
#5269=DIRECTION ( 'NONE',  ( 0.5319835227803600963, -0.2110602665713099124, -0.8200287161831869565 ) ) ;
#5280=CARTESIAN_POINT ( 'NONE',  ( 45.24946171279598417, 26.40784706826093498, 47.99220971130007030 ) ) ;
#5281=AXIS2_PLACEMENT_3D ( 'NONE', #32373, #22184, #12355 ) ;
#5291=CARTESIAN_POINT ( 'NONE',  ( 45.39590889550878927, 22.93328494799376571, 47.28470721838063184 ) ) ;
#5311=CARTESIAN_POINT ( 'NONE',  ( 45.79384627280941089, 27.16618040159427139, 49.05938063676249072 ) ) ;
#5326=CARTESIAN_POINT ( 'NONE',  ( 45.82550680184641578, 25.16454579224780019, 44.55508916310584056 ) ) ;
#5336=ORIENTED_EDGE ( 'NONE', *, *, #6185, .T. ) ;
#5337=CARTESIAN_POINT ( 'NONE',  ( 45.96182992765471909, 26.60087065737812040, 44.82232689504102296 ) ) ;
#5358=ORIENTED_EDGE ( 'NONE', *, *, #15588, .T. ) ;
#5359=EDGE_CURVE ( 'NONE', #10117, #6715, #29772, .T. ) ;
#5366=B_SPLINE_CURVE_WITH_KNOTS ( 'NONE', 3,
 ( #30805, #18000, #12933, #30168, #5870, #3225 ),
 .UNSPECIFIED., .F., .F.,
 ( 4, 2, 4 ),
 ( 0.000000000000000000, 0.5000000000000000000, 1.000000000000000000 ),
 .UNSPECIFIED. ) ;
#5383=CARTESIAN_POINT ( 'NONE',  ( 45.35708200440645044, 28.30457786121581876, 45.92000246470679770 ) ) ;
#5396=EDGE_CURVE ( 'NONE', #3842, #29156, #30011, .T. ) ;
#5397=TOROIDAL_SURFACE ( 'NONE', #11694, 3.700000000000000178, 0.5000000000000002220 ) ;
#5398=VERTEX_POINT ( 'NONE', #17185 ) ;
#5400=CARTESIAN_POINT ( 'NONE',  ( 45.57717830316858709, 22.95310733321322161, 47.66397322663508618 ) ) ;
#5407=CARTESIAN_POINT ( 'NONE',  ( 44.70507715278255745, 26.96291119454915375, 46.92503878583765697 ) ) ;
#5408=ORIENTED_EDGE ( 'NONE', *, *, #14575, .T. ) ;
#5410=CYLINDRICAL_SURFACE ( 'NONE', #27380, 2.499999999999997335 ) ;
#5411=VERTEX_POINT ( 'NONE', #7362 ) ;
#5415=CARTESIAN_POINT ( 'NONE',  ( 48.01680169312755453, 22.93807716476589675, 45.63279442905645311 ) ) ;
#5422=EDGE_CURVE ( 'NONE', #13542, #19007, #25076, .T. ) ;
#5426=CARTESIAN_POINT ( 'NONE',  ( 49.49063479933183629, 27.39951373492759856, 47.17357720316391578 ) ) ;
#5430=DIRECTION ( 'NONE',  ( 1.234978253042719660E-16, -1.000000000000000000, -1.109335647967047851E-31 ) ) ;
#5433=AXIS2_PLACEMENT_3D ( 'NONE', #3426, #23294, #808 ) ;
#5436=ORIENTED_EDGE ( 'NONE', *, *, #29023, .T. ) ;
#5447=ADVANCED_FACE ( 'NONE', ( #7027 ), #23263, .T. ) ;
#5456=CARTESIAN_POINT ( 'NONE',  ( 44.09250526802607340, 28.75621246473837189, 46.89322480343881949 ) ) ;
#5472=CARTESIAN_POINT ( 'NONE',  ( 48.94625023931840246, 28.85784706826092716, 46.10640627770150246 ) ) ;
#5473=CARTESIAN_POINT ( 'NONE',  ( 46.00908685603034343, 28.24624452788248163, 44.91496614357594552 ) ) ;
#5508=CARTESIAN_POINT ( 'NONE',  ( 48.23388202445966044, 28.92822092656773947, 49.27628909396054979 ) ) ;
#5523=CARTESIAN_POINT ( 'NONE',  ( 45.69268131687783807, 22.99884124225578574, 46.97633003370108185 ) ) ;
#5539=DIRECTION ( 'NONE',  ( 1.234978253042719660E-16, -1.000000000000000000, -1.109335647967047851E-31 ) ) ;
#5542=( BOUNDED_CURVE ( )  B_SPLINE_CURVE ( 2, ( #983, #28406, #28564, #18689, #1301, #11007, #11325, #30711, #28716 ),
 .UNSPECIFIED., .F., .F. ) 
 B_SPLINE_CURVE_WITH_KNOTS ( ( 3, 2, 2, 2, 3 ),
 ( 0.7500000011612726336, 0.7619047619047618625, 0.7857142857142856984, 0.8095238095238095344, 0.8214285725898440305 ),
 .UNSPECIFIED. ) 
 CURVE ( )  GEOMETRIC_REPRESENTATION_ITEM ( )  RATIONAL_B_SPLINE_CURVE ( ( 0.9330127018922200755, 0.9330127084266227611, 1.000000000000000000, 0.8660254037844388186, 1.000000000000000000, 0.8660254037844388186, 1.000000000000000000, 0.9330126953578163906, 0.9330127018922200755 ) ) 
 REPRESENTATION_ITEM ( '' )  );
#5551=AXIS2_PLACEMENT_3D ( 'NONE', #15171, #25183, #18424 ) ;
#5552=CARTESIAN_POINT ( 'NONE',  ( 48.23388202445966044, 28.35087065737811685, 49.27628909396054979 ) ) ;
#5563=CARTESIAN_POINT ( 'NONE',  ( 48.76626135000090301, 22.93328494799376216, 47.45974698848920781 ) ) ;
#5565=CARTESIAN_POINT ( 'NONE',  ( 48.80717017713595141, 27.27622849631043067, 48.15820438821415195 ) ) ;
#5575=CARTESIAN_POINT ( 'NONE',  ( 47.74496780842034127, 22.93328494799376571, 45.45767897490919296 ) ) ;
#5576=CARTESIAN_POINT ( 'NONE',  ( 48.94625023931840246, 25.27124452788249442, 46.10640627770148825 ) ) ;
#5582=CARTESIAN_POINT ( 'NONE',  ( 45.35708200440645044, 26.29118040159426428, 45.92000246470680480 ) ) ;
#5598=ORIENTED_EDGE ( 'NONE', *, *, #14122, .F. ) ;
#5604=CARTESIAN_POINT ( 'NONE',  ( 45.00053793792376666, 27.35920399681022630, 45.68869892245983522 ) ) ;
#5605=CARTESIAN_POINT ( 'NONE',  ( 44.79156314060809763, 22.86454579224779948, 46.92953032342012420 ) ) ;
#5610=CARTESIAN_POINT ( 'NONE',  ( 46.96268396749378127, 28.93121246473836905, 49.65201805493727960 ) ) ;
#5615=CARTESIAN_POINT ( 'NONE',  ( 49.03322279537384532, 25.03300763406332408, 45.41163724378073852 ) ) ;
#5623=CARTESIAN_POINT ( 'NONE',  ( 49.49063479933183629, 28.79951373492759359, 47.17357720316391578 ) ) ;
#5624=B_SPLINE_CURVE_WITH_KNOTS ( 'NONE', 3,
 ( #20355, #30384, #668, #12992, #27922, #28245 ),
 .UNSPECIFIED., .F., .F.,
 ( 4, 2, 4 ),
 ( 0.000000000000000000, 0.5000000000000000000, 1.000000000000000000 ),
 .UNSPECIFIED. ) ;
#5625=CARTESIAN_POINT ( 'NONE',  ( 46.99023568444673060, 28.53791119454914949, 49.12151524109405898 ) ) ;
#5626=CARTESIAN_POINT ( 'NONE',  ( 46.04844006429464542, 22.86454579224779948, 44.99211097489548905 ) ) ;
#5629=ADVANCED_FACE ( 'NONE', ( #26197 ), #26683, .T. ) ;
#5630=VERTEX_POINT ( 'NONE', #14224 ) ;
#5655=CARTESIAN_POINT ( 'NONE',  ( 49.73127130660545703, 24.88724468661089873, 46.52306240693558692 ) ) ;
#5656=DIRECTION ( 'NONE',  ( 1.234978253042719660E-16, -1.000000000000000000, -1.109335647967047851E-31 ) ) ;
#5669=EDGE_CURVE ( 'NONE', #4920, #5411, #1411, .T. ) ;
#5684=CYLINDRICAL_SURFACE ( 'NONE', #7050, 2.749999999999998224 ) ;
#5719=( GEOMETRIC_REPRESENTATION_CONTEXT ( 3 ) GLOBAL_UNCERTAINTY_ASSIGNED_CONTEXT ( ( #13746 ) ) GLOBAL_UNIT_ASSIGNED_CONTEXT ( ( #18023, #22455, #7867 ) ) REPRESENTATION_CONTEXT ( 'NONE', 'WORKASPACE' ) );
#5722=CARTESIAN_POINT ( 'NONE',  ( 48.49492103495406070, 22.99884124225578574, 47.27843453342132563 ) ) ;
#5723=SHAPE_REPRESENTATION ( 'Screw M5', ( #8172 ), #22330 ) ;
#5724=CARTESIAN_POINT ( 'NONE',  ( 48.23388214087538728, 15.77906836436399374, 49.27628903457465270 ) ) ;
#5726=CARTESIAN_POINT ( 'NONE',  ( 46.02876340639226527, 25.46789516297710065, 44.95353858666495483 ) ) ;
#5777=ORIENTED_EDGE ( 'NONE', *, *, #20000, .T. ) ;
#5790=AXIS2_PLACEMENT_3D ( 'NONE', #9450, #31931, #4518 ) ;
#5791=CARTESIAN_POINT ( 'NONE',  ( 44.70507715278255745, 28.44951373492759217, 46.92503878583765697 ) ) ;
#5795=CARTESIAN_POINT ( 'NONE',  ( 48.40186567930498285, 28.12957786121581805, 45.03923535223908203 ) ) ;
#5818=CARTESIAN_POINT ( 'NONE',  ( 46.45846941443645761, 22.99884124225578930, 45.79590206249746132 ) ) ;
#5820=CIRCLE ( 'NONE', #2681, 4.200000000000000178 ) ;
#5821=CARTESIAN_POINT ( 'NONE',  ( 45.23477325667712989, 24.76454579224779806, 43.39705899138675704 ) ) ;
#5826=CARTESIAN_POINT ( 'NONE',  ( 47.76133520913771235, 29.61346213614034895, 45.10342086390699734 ) ) ;
#5827=CARTESIAN_POINT ( 'NONE',  ( 49.73059755354898215, 24.88073588970408423, 46.43791210414119064 ) ) ;
#5849=CARTESIAN_POINT ( 'NONE',  ( 49.32483701613094240, 27.00322093266652601, 45.91328182968236860 ) ) ;
#5862=DIRECTION ( 'NONE',  ( -0.05186525298099804726, -2.168404344971009854E-16, 0.9986540920324800119 ) ) ;
#5864=DIRECTION ( 'NONE',  ( -0.4544104193609905806, -5.611869858668446909E-17, -0.8907924397839086517 ) ) ;
#5866=ORIENTED_EDGE ( 'NONE', *, *, #14122, .T. ) ;
#5870=CARTESIAN_POINT ( 'NONE',  ( 45.50623141997586174, 22.89977464660286444, 48.01957109218837871 ) ) ;
#5880=ORIENTED_EDGE ( 'NONE', *, *, #4176, .F. ) ;
#5893=CARTESIAN_POINT ( 'NONE',  ( 46.99218062947583974, 27.85956182964376282, 49.08406571254116102 ) ) ;
#5894=ORIENTED_EDGE ( 'NONE', *, *, #22486, .T. ) ;
#5901=FACE_OUTER_BOUND ( 'NONE', #32292, .T. ) ;
#5919=( BOUNDED_CURVE ( )  B_SPLINE_CURVE ( 2, ( #5552, #17527, #20302, #25402, #25558, #17683, #22439, #7364, #3064 ),
 .UNSPECIFIED., .F., .F. ) 
 B_SPLINE_CURVE_WITH_KNOTS ( ( 3, 2, 2, 2, 3 ),
 ( 0.2500000011612727446, 0.2619047619047619180, 0.2857142857142856984, 0.3095238095238095344, 0.3214285725898440860 ),
 .UNSPECIFIED. ) 
 CURVE ( )  GEOMETRIC_REPRESENTATION_ITEM ( )  RATIONAL_B_SPLINE_CURVE ( ( 0.9330127018922200755, 0.9330127084266233162, 1.000000000000000000, 0.8660254037844388186, 1.000000000000000000, 0.8660254037844388186, 1.000000000000000000, 0.9330126953578159466, 0.9330127018922200755 ) ) 
 REPRESENTATION_ITEM ( '' )  );
#5927=CARTESIAN_POINT ( 'NONE',  ( 47.28715512441527125, 22.91889071986277671, 48.84357536195264515 ) ) ;
#5936=LINE ( 'NONE', #8869, #16264 ) ;
#5955=ADVANCED_FACE ( 'NONE', ( #30458 ), #22735, .T. ) ;
#5956=CARTESIAN_POINT ( 'NONE',  ( 48.46535932150934656, 28.98954579807170617, 49.73005965046827015 ) ) ;
#5977=DIRECTION ( 'NONE',  ( 1.000000000000000000, 0.000000000000000000, 0.000000000000000000 ) ) ;
#6001=DIRECTION ( 'NONE',  ( 1.234978253042719660E-16, -1.000000000000000000, -1.109335647967047851E-31 ) ) ;
#6005=ORIENTED_EDGE ( 'NONE', *, *, #16642, .T. ) ;
#6023=CARTESIAN_POINT ( 'NONE',  ( 48.18662509608405031, 25.09624452788249371, 49.18364984542562013 ) ) ;
#6045=EDGE_LOOP ( 'NONE', ( #2651, #32227, #8094 ) ) ;
#6048=CARTESIAN_POINT ( 'NONE',  ( 48.04379483844901699, 22.98879437201065912, 48.17263172485531442 ) ) ;
#6050=CARTESIAN_POINT ( 'NONE',  ( 45.28286642839709231, 27.74289516297709568, 47.97516931882780966 ) ) ;
#6052=VERTEX_POINT ( 'NONE', #26158 ) ;
#6071=LINE ( 'NONE', #818, #29815 ) ;
#6087=CARTESIAN_POINT ( 'NONE',  ( 48.72149481846882679, 22.88065857334295217, 48.10262368218729279 ) ) ;
#6103=CARTESIAN_POINT ( 'NONE',  ( 45.46000861347822308, 29.57287913140503832, 49.57397645940629616 ) ) ;
#6115=EDGE_CURVE ( 'NONE', #24091, #24927, #6139, .T. ) ;
#6119=CARTESIAN_POINT ( 'NONE',  ( 46.94469835654546586, 23.12036939723557083, 47.28539358874152043 ) ) ;
#6132=DIRECTION ( 'NONE',  ( 1.234978253042719660E-16, -1.000000000000000000, -1.109335647967047851E-31 ) ) ;
#6134=CARTESIAN_POINT ( 'NONE',  ( 48.59475124299144966, 29.58954579224780090, 45.61232171765963272 ) ) ;
#6139=LINE ( 'NONE', #25996, #4165 ) ;
#6160=CARTESIAN_POINT ( 'NONE',  ( 45.41164638504195494, 22.93807716476589675, 46.96173444154113241 ) ) ;
#6169=CARTESIAN_POINT ( 'NONE',  ( 46.90849534498374140, 22.91413368675619111, 45.25622507561872965 ) ) ;
#6176=CARTESIAN_POINT ( 'NONE',  ( 47.65993751833249092, 23.10527845304106620, 47.07849978535075053 ) ) ;
#6185=EDGE_CURVE ( 'NONE', #17767, #25543, #2023, .T. ) ;
#6193=ADVANCED_FACE ( 'NONE', ( #11717 ), #32067, .F. ) ;
#6195=CARTESIAN_POINT ( 'NONE',  ( 47.71481260072994246, 23.09557481883486929, 47.44955100077470433 ) ) ;
#6198=CARTESIAN_POINT ( 'NONE',  ( 48.37829923888483563, 27.45122849631043138, 45.07556196625585443 ) ) ;
#6209=FACE_OUTER_BOUND ( 'NONE', #17779, .T. ) ;
#6220=AXIS2_PLACEMENT_3D ( 'NONE', #14136, #11501, #8563 ) ;
#6221=LINE ( 'NONE', #16223, #20558 ) ;
#6224=CARTESIAN_POINT ( 'NONE',  ( 46.00908685603033632, 26.93284706826093000, 44.91496614357595263 ) ) ;
#6228=EDGE_CURVE ( 'NONE', #4161, #4920, #9748, .T. ) ;
#6250=ADVANCED_FACE ( 'NONE', ( #6787 ), #26234, .T. ) ;
#6263=CARTESIAN_POINT ( 'NONE',  ( 49.28428300279882990, 26.94787913140504543, 48.46772541801551171 ) ) ;
#6270=ORIENTED_EDGE ( 'NONE', *, *, #9227, .T. ) ;
#6273=CARTESIAN_POINT ( 'NONE',  ( 48.37829923888483563, 25.39452976649965876, 45.07556196625585443 ) ) ;
#6274=VECTOR ( 'NONE', #3491, 1000.000000000000000 ) ;
#6285=CARTESIAN_POINT ( 'NONE',  ( 44.87087493598345134, 25.37587066347689913, 48.18533415931919706 ) ) ;
#6286=CARTESIAN_POINT ( 'NONE',  ( 0.000000000000000000, 0.000000000000000000, 0.000000000000000000 ) ) ;
#6290=CARTESIAN_POINT ( 'NONE',  ( 45.79384627280941089, 27.77957786121581663, 49.05938063676250493 ) ) ;
#6295=( BOUNDED_CURVE ( )  B_SPLINE_CURVE ( 2, ( #23394, #20921, #8768, #3038, #901, #10617, #20606, #10927, #18460 ),
 .UNSPECIFIED., .F., .T. ) 
 B_SPLINE_CURVE_WITH_KNOTS ( ( 3, 2, 2, 2, 3 ),
 ( 0.4642857131244416125, 0.4761904761904761640, 0.5000000000000000000, 0.5238095238095238360, 0.5357142845530131758 ),
 .UNSPECIFIED. ) 
 CURVE ( )  GEOMETRIC_REPRESENTATION_ITEM ( )  RATIONAL_B_SPLINE_CURVE ( ( 0.9330127018922199644, 0.9330126953578159466, 1.000000000000000000, 0.8660254037844387076, 1.000000000000000000, 0.8660254037844387076, 1.000000000000000000, 0.9330127084266224280, 0.9330127018922200755 ) ) 
 REPRESENTATION_ITEM ( '' )  );
#6309=VECTOR ( 'NONE', #30634, 1000.000000000000114 ) ;
#6329=CARTESIAN_POINT ( 'NONE',  ( 45.41164638504195494, 22.93807716476589675, 46.96173444154113241 ) ) ;
#6365=CARTESIAN_POINT ( 'NONE',  ( 47.20353132263855400, 26.85286309983298025, 45.01455027646041174 ) ) ;
#6367=ORIENTED_EDGE ( 'NONE', *, *, #26978, .T. ) ;
#6376=CARTESIAN_POINT ( 'NONE',  ( 44.09250526802607340, 27.35621246473837331, 46.89322480343881949 ) ) ;
#6377=CARTESIAN_POINT ( 'NONE',  ( 48.89639543821420631, 22.86454579224779948, 46.17372366037167097 ) ) ;
#6405=EDGE_CURVE ( 'NONE', #28677, #11490, #3577, .T. ) ;
#6412=CARTESIAN_POINT ( 'NONE',  ( 48.23388202445966755, 15.77906836436399374, 49.27628909396055690 ) ) ;
#6422=EDGE_LOOP ( 'NONE', ( #24764, #11832 ) ) ;
#6428=CARTESIAN_POINT ( 'NONE',  ( 45.46000861347822308, 28.87287913140503548, 49.57397645940629616 ) ) ;
#6438=CARTESIAN_POINT ( 'NONE',  ( 48.37829923888483563, 26.09452976649965450, 45.07556196625585443 ) ) ;
#6443=AXIS2_PLACEMENT_3D ( 'NONE', #20493, #30520, #13121 ) ;
#6446=EDGE_CURVE ( 'NONE', #15214, #18631, #29260, .T. ) ;
#6456=CARTESIAN_POINT ( 'NONE',  ( 47.20547626766765603, 28.18791119454915162, 44.97710074790751378 ) ) ;
#6472=CARTESIAN_POINT ( 'NONE',  ( 47.53612098953208687, 29.43843285659984943, 49.23711617065869461 ) ) ;
#6485=ADVANCED_FACE ( 'NONE', ( #14956 ), #25443, .F. ) ;
#6521=EDGE_CURVE ( 'NONE', #26418, #10913, #6071, .T. ) ;
#6528=CARTESIAN_POINT ( 'NONE',  ( 45.28286642839709231, 29.88619643316631524, 47.97516931882780966 ) ) ;
#6537=CARTESIAN_POINT ( 'NONE',  ( 45.46000861347822308, 26.77287913140504116, 49.57397645940629616 ) ) ;
#6544=DIRECTION ( 'NONE',  ( 0.2029548553014545453, 0.9702957262759968060, 0.1316644609608131067 ) ) ;
#6549=CARTESIAN_POINT ( 'NONE',  ( 48.82187354100420151, 22.88065857334294861, 46.16985335424440251 ) ) ;
#6553=EDGE_LOOP ( 'NONE', ( #30381, #20640, #5436, #425 ) ) ;
#6565=AXIS2_PLACEMENT_3D ( 'NONE', #10747, #7792, #13047 ) ;
#6566=VECTOR ( 'NONE', #2210, 1000.000000000000000 ) ;
#6577=CYLINDRICAL_SURFACE ( 'NONE', #7488, 2.499999999999997335 ) ;
#6580=ORIENTED_EDGE ( 'NONE', *, *, #10696, .F. ) ;
#6590=CARTESIAN_POINT ( 'NONE',  ( 47.23302798462060537, 27.18121246473837616, 44.44659793406428605 ) ) ;
#6601=CARTESIAN_POINT ( 'NONE',  ( 46.00908685603034343, 28.33284706826092503, 44.91496614357594552 ) ) ;
#6615=CARTESIAN_POINT ( 'NONE',  ( 45.64903328369346269, 22.95310733321322161, 46.28042130680973543 ) ) ;
#6616=CARTESIAN_POINT ( 'NONE',  ( 46.99023568444674481, 25.73791119454915588, 49.12151524109405898 ) ) ;
#6621=ORIENTED_EDGE ( 'NONE', *, *, #23574, .F. ) ;
#6623=CARTESIAN_POINT ( 'NONE',  ( 46.33059210211230550, 22.93807716476589675, 45.54522087609679204 ) ) ;
#6629=LINE ( 'NONE', #19082, #19372 ) ;
#6631=CARTESIAN_POINT ( 'NONE',  ( 46.47461290750400309, 22.93807716476589675, 45.47175308309371644 ) ) ;
#6641=B_SPLINE_CURVE_WITH_KNOTS ( 'NONE', 3,
 ( #7702, #18344, #25744, #30676, #27723, #5241, #15250, #8190, #17871, #8036, #8343, #27889, #25260, #467, #18024, #28374 ),
 .UNSPECIFIED., .F., .F.,
 ( 4, 2, 2, 2, 2, 2, 2, 4 ),
 ( 0.000000000000000000, 0.0004663348940371102379, 0.0009326697880742204757, 0.001399004682111330659, 0.001865339576148440951, 0.002798009364222690375, 0.003264344258259825604, 0.003730679152296960399 ),
 .UNSPECIFIED. ) ;
#6654=DIRECTION ( 'NONE',  ( 0.4544104193609903586, 0.000000000000000000, 0.8907924397839088737 ) ) ;
#6665=ORIENTED_EDGE ( 'NONE', *, *, #4667, .T. ) ;
#6680=CARTESIAN_POINT ( 'NONE',  ( 45.37383841111020644, 22.88065857334295217, 47.92876263475718446 ) ) ;
#6681=CARTESIAN_POINT ( 'NONE',  ( 46.21408258523083390, 22.84434098701873239, 49.00610453205841566 ) ) ;
#6684=CARTESIAN_POINT ( 'NONE',  ( 44.74832014356462651, 27.72786309983298025, 46.92728461490987257 ) ) ;
#6689=EDGE_LOOP ( 'NONE', ( #18251, #8301, #10419, #5218 ) ) ;
#6694=CARTESIAN_POINT ( 'NONE',  ( 49.28428300279882990, 26.94787913140504543, 48.46772541801551171 ) ) ;
#6695=CARTESIAN_POINT ( 'NONE',  ( 46.33206787849857022, 22.99884124225578574, 48.22973596570440691 ) ) ;
#6701=FACE_OUTER_BOUND ( 'NONE', #4938, .T. ) ;
#6715=VERTEX_POINT ( 'NONE', #16548 ) ;
#6716=CARTESIAN_POINT ( 'NONE',  ( 47.23884743062419744, 22.86454579224779948, 45.05393496349946503 ) ) ;
#6722=CARTESIAN_POINT ( 'NONE',  ( 46.04302072787191946, 22.93328494799376571, 45.69307819878901000 ) ) ;
#6733=FILL_AREA_STYLE_COLOUR ( '', #9232 ) ;
#6745=CARTESIAN_POINT ( 'NONE',  ( 45.46000861347822308, 26.07287913140504543, 49.57397645940629616 ) ) ;
#6757=CARTESIAN_POINT ( 'NONE',  ( 47.22751897799751220, 28.64253733014355774, 44.55267275764142454 ) ) ;
#6758=CARTESIAN_POINT ( 'NONE',  ( 45.35708200440645044, 27.69118040159425931, 45.92000246470679770 ) ) ;
#6769=( BOUNDED_CURVE ( )  B_SPLINE_CURVE ( 2, ( #7430, #12518, #34, #7587, #17585, #27601, #5604, #25941, #20855 ),
 .UNSPECIFIED., .F., .F. ) 
 B_SPLINE_CURVE_WITH_KNOTS ( ( 3, 2, 2, 2, 3 ),
 ( 0.3928571440184155938, 0.4047619047619047672, 0.4285714285714285476, 0.4523809523809523836, 0.4642857154469869352 ),
 .UNSPECIFIED. ) 
 CURVE ( )  GEOMETRIC_REPRESENTATION_ITEM ( )  RATIONAL_B_SPLINE_CURVE ( ( 0.9330127018922200755, 0.9330127084266233162, 1.000000000000000000, 0.8660254037844388186, 1.000000000000000000, 0.8660254037844388186, 1.000000000000000000, 0.9330126953578159466, 0.9330127018922200755 ) ) 
 REPRESENTATION_ITEM ( '' )  );
#6787=FACE_OUTER_BOUND ( 'NONE', #10979, .T. ) ;
#6803=DIRECTION ( 'NONE',  ( -0.4544104659272507063, 0.000000000000000000, -0.8907924160295589422 ) ) ;
#6805=AXIS2_PLACEMENT_3D ( 'NONE', #14582, #1445, #24584 ) ;
#6847=DIRECTION ( 'NONE',  ( -1.234978253042719660E-16, 1.000000000000000000, 1.109335647967047851E-31 ) ) ;
#6852=CARTESIAN_POINT ( 'NONE',  ( 44.74832014356462651, 26.32786309983298878, 46.92728461490987257 ) ) ;
#6866=CARTESIAN_POINT ( 'NONE',  ( 46.96268396749378127, 24.73121246473838042, 49.65201805493727960 ) ) ;
#6867=CARTESIAN_POINT ( 'NONE',  ( 46.45074414369405957, 22.93328494799376571, 48.64093701409239401 ) ) ;
#6874=DIRECTION ( 'NONE',  ( 0.9986540920324801229, 1.233316085972235327E-16, 0.05186525298099653458 ) ) ;
#6891=DIRECTION ( 'NONE',  ( -0.5442436726714893203, -6.721291001053903893E-17, 0.8389271868029124501 ) ) ;
#6901=EDGE_CURVE ( 'NONE', #12307, #5411, #15740, .T. ) ;
#6903=SURFACE_STYLE_FILL_AREA ( #29384 ) ;
#6922=CARTESIAN_POINT ( 'NONE',  ( 48.94625023931840246, 28.85784706826092716, 46.10640627770150246 ) ) ;
#6935=B_SPLINE_SURFACE_WITH_KNOTS ( 'NONE', 3, 3, ( 
 ( #14094, #1606, #22111, #21624, #6695, #1930 ),
 ( #27043, #24415, #4557, #24089, #21455, #19490 ),
 ( #14576, #29344, #1440, #26883, #4064, #6867 ),
 ( #29518, #11947, #1772, #31656, #32143, #29183 ),
 ( #29678, #7184, #26719, #14257, #4396, #7023 ),
 ( #16693, #17181, #4240, #24253, #31972, #24579 ) ),
 .UNSPECIFIED., .F., .F., .F.,
 ( 4, 2, 4 ),
 ( 4, 2, 4 ),
 ( 0.000000000000000000, 0.5000000000000000000, 1.000000000000000000 ),
 ( 0.000000000000000000, 0.5000000000000000000, 1.000000000000000000 ),
 .UNSPECIFIED. ) ;
#6939=CARTESIAN_POINT ( 'NONE',  ( 45.86034435575247414, 22.98765316579147111, 46.24648758314307173 ) ) ;
#6940=CARTESIAN_POINT ( 'NONE',  ( 44.41710432008958520, 25.31454579807170191, 48.41681133995267317 ) ) ;
#6952=CARTESIAN_POINT ( 'NONE',  ( 45.24946171279598417, 29.20784706826092503, 47.99220971130007030 ) ) ;
#6962=EDGE_CURVE ( 'NONE', #24589, #4920, #4868, .T. ) ;
#7006=CARTESIAN_POINT ( 'NONE',  ( 46.98893894479710553, 19.86454579224779948, 49.14648158776898867 ) ) ;
#7010=CARTESIAN_POINT ( 'NONE',  ( 45.81741271322955100, 25.00122849631043565, 49.02305402274571122 ) ) ;
#7017=CARTESIAN_POINT ( 'NONE',  ( 47.09785597605719687, 25.16454579224780019, 47.04930799450078638 ) ) ;
#7022=CARTESIAN_POINT ( 'NONE',  ( 49.41945501136223839, 27.06454579807170902, 45.86501535757901848 ) ) ;
#7023=CARTESIAN_POINT ( 'NONE',  ( 46.86059137560834387, 22.89977464660286444, 48.89819542093576388 ) ) ;
#7026=CARTESIAN_POINT ( 'NONE',  ( 47.16329704288476421, 29.59056480653310217, 44.97634117946077481 ) ) ;
#7027=FACE_OUTER_BOUND ( 'NONE', #19247, .T. ) ;
#7036=EDGE_CURVE ( 'NONE', #13067, #25764, #18002, .T. ) ;
#7050=AXIS2_PLACEMENT_3D ( 'NONE', #18302, #10294, #2567 ) ;
#7056=VERTEX_POINT ( 'NONE', #7288 ) ;
#7066=CARTESIAN_POINT ( 'NONE',  ( 49.00637973737335074, 24.76454579224779806, 50.79063624159320511 ) ) ;
#7074=CARTESIAN_POINT ( 'NONE',  ( 49.41945501136223839, 25.66454579807171044, 45.86501535757901848 ) ) ;
#7086=CARTESIAN_POINT ( 'NONE',  ( 45.24946171279598417, 27.10784706826093071, 47.99220971130007030 ) ) ;
#7101=CARTESIAN_POINT ( 'NONE',  ( 45.45032030167665482, 22.91413368675619111, 46.31675765204602868 ) ) ;
#7103=CARTESIAN_POINT ( 'NONE',  ( 46.93316184409368930, 25.34819976284614640, 50.22046065185270436 ) ) ;
#7114=CARTESIAN_POINT ( 'NONE',  ( 45.35708200440645044, 29.09118040159425789, 45.92000246470679770 ) ) ;
#7173=VERTEX_POINT ( 'NONE', #5147 ) ;
#7182=CARTESIAN_POINT ( 'NONE',  ( 46.72376704384358703, 22.91413368675619111, 48.81312807415246624 ) ) ;
#7183=CARTESIAN_POINT ( 'NONE',  ( 48.18662509608405031, 26.49624452788248874, 49.18364984542562013 ) ) ;
#7184=CARTESIAN_POINT ( 'NONE',  ( 47.59795910211924763, 22.99884124225578219, 48.37376509570535887 ) ) ;
#7190=ORIENTED_EDGE ( 'NONE', *, *, #11165, .F. ) ;
#7204=CARTESIAN_POINT ( 'NONE',  ( 46.48525799733394592, 23.04411619146717882, 47.99360027521537830 ) ) ;
#7211=CARTESIAN_POINT ( 'NONE',  ( 46.99023568444673060, 25.03791119454915659, 49.12151524109405898 ) ) ;
#7224=CARTESIAN_POINT ( 'NONE',  ( 49.49063479933183629, 28.01291119454915091, 47.17357720316391578 ) ) ;
#7236=CARTESIAN_POINT ( 'NONE',  ( 48.80698780008784610, 29.57276968525846073, 45.83340656927448009 ) ) ;
#7238=ORIENTED_EDGE ( 'NONE', *, *, #24722, .T. ) ;
#7245=ORIENTED_EDGE ( 'NONE', *, *, #23027, .T. ) ;
#7250=CARTESIAN_POINT ( 'NONE',  ( 49.64105649875294546, 24.93604219378083542, 46.47965702198763438 ) ) ;
#7271=CARTESIAN_POINT ( 'NONE',  ( 49.62252444096254322, 24.84787913140503690, 48.68715535708000886 ) ) ;
#7283=ORIENTED_EDGE ( 'NONE', *, *, #19049, .T. ) ;
#7287=CARTESIAN_POINT ( 'NONE',  ( 47.19823469859255738, 22.88065857334294861, 45.11653766655789610 ) ) ;
#7288=CARTESIAN_POINT ( 'NONE',  ( 48.23388202445966044, 28.92822092656773947, 49.27628909396054979 ) ) ;
#7293=VERTEX_POINT ( 'NONE', #29551 ) ;
#7319=AXIS2_PLACEMENT_3D ( 'NONE', #32390, #1863, #29270 ) ;
#7344=DIRECTION ( 'NONE',  ( 0.4544104193609912468, 5.611869858668455538E-17, 0.8907924397839084296 ) ) ;
#7351=CARTESIAN_POINT ( 'NONE',  ( 48.40186567930498285, 26.72957786121581947, 45.03923535223908203 ) ) ;
#7362=CARTESIAN_POINT ( 'NONE',  ( 48.72149481846882679, 22.88065857334295217, 48.10262368218729279 ) ) ;
#7364=CARTESIAN_POINT ( 'NONE',  ( 45.36511207810799107, 28.03213139976340429, 45.12672418911605376 ) ) ;
#7375=VERTEX_POINT ( 'NONE', #29575 ) ;
#7377=CARTESIAN_POINT ( 'NONE',  ( 45.68457171659533600, 22.99884124225578574, 47.13247861182188103 ) ) ;
#7378=VECTOR ( 'NONE', #30858, 999.9999999999998863 ) ;
#7387=CARTESIAN_POINT ( 'NONE',  ( 46.99023568444673060, 27.13791119454915446, 49.12151524109405898 ) ) ;
#7395=FACE_OUTER_BOUND ( 'NONE', #4102, .T. ) ;
#7397=CARTESIAN_POINT ( 'NONE',  ( 45.24946171279598417, 27.02124452788248732, 47.99220971130007740 ) ) ;
#7403=VECTOR ( 'NONE', #11745, 1000.000000000000114 ) ;
#7405=ORIENTED_EDGE ( 'NONE', *, *, #15588, .F. ) ;
#7420=CARTESIAN_POINT ( 'NONE',  ( 45.79384627280941089, 25.76618040159426570, 49.05938063676249072 ) ) ;
#7427=B_SPLINE_CURVE_WITH_KNOTS ( 'NONE', 3,
 ( #613, #20947, #16026, #6176, #26194, #3230 ),
 .UNSPECIFIED., .F., .F.,
 ( 4, 2, 4 ),
 ( 0.000000000000000000, 0.5000000000000000000, 1.000000000000000000 ),
 .UNSPECIFIED. ) ;
#7430=CARTESIAN_POINT ( 'NONE',  ( 48.23388202445966044, 27.65087065737811756, 49.27628909396056400 ) ) ;
#7437=EDGE_CURVE ( 'NONE', #11362, #25360, #13869, .T. ) ;
#7451=CARTESIAN_POINT ( 'NONE',  ( 46.00908685603034343, 29.73284706826092361, 44.91496614357595263 ) ) ;
#7454=AXIS2_PLACEMENT_3D ( 'NONE', #1424, #6847, #19133 ) ;
#7478=DIRECTION ( 'NONE',  ( 0.03667427209081842304, 0.7071067811865463515, -0.7061550805358625116 ) ) ;
#7488=AXIS2_PLACEMENT_3D ( 'NONE', #11337, #9033, #29382 ) ;
#7490=PRODUCT ( 'Screw M5', 'Screw M5', '', ( #12815 ) ) ;
#7517=PLANE ( 'NONE',  #606 ) ;
#7519=CARTESIAN_POINT ( 'NONE',  ( 46.99023568444673060, 28.53791119454914949, 49.12151524109405898 ) ) ;
#7526=DIRECTION ( 'NONE',  ( -0.4544104659272780733, 0.000000000000000000, -0.8907924160295450644 ) ) ;
#7544=CARTESIAN_POINT ( 'NONE',  ( 45.78383729499237376, 22.98765316579147111, 47.71961428948426231 ) ) ;
#7549=CARTESIAN_POINT ( 'NONE',  ( 48.40186567930498285, 25.32957786121582089, 45.03923535223908203 ) ) ;
#7552=DIRECTION ( 'NONE',  ( 0.4544104193609903586, 0.000000000000000000, 0.8907924397839087627 ) ) ;
#7568=DIRECTION ( 'NONE',  ( 0.4544104193609905806, 5.611869858668446909E-17, 0.8907924397839086517 ) ) ;
#7580=CARTESIAN_POINT ( 'NONE',  ( 48.18662509608405031, 27.28284706826093142, 49.18364984542562013 ) ) ;
#7587=CARTESIAN_POINT ( 'NONE',  ( 45.52675994804781112, 27.53420399681022346, 49.47108226228596806 ) ) ;
#7610=CARTESIAN_POINT ( 'NONE',  ( 48.94625023931840957, 26.75784706826093284, 46.10640627770150246 ) ) ;
#7661=CARTESIAN_POINT ( 'NONE',  ( 45.36511207810798396, 25.80948166895303686, 45.12672418911604666 ) ) ;
#7670=ORIENTED_EDGE ( 'NONE', *, *, #14719, .F. ) ;
#7683=CARTESIAN_POINT ( 'NONE',  ( 46.99747725352182925, 22.88065857334294861, 48.98207832244369087 ) ) ;
#7684=CARTESIAN_POINT ( 'NONE',  ( 46.00908685603034343, 29.64624452788248021, 44.91496614357595263 ) ) ;
#7688=ORIENTED_EDGE ( 'NONE', *, *, #21881, .T. ) ;
#7698=CARTESIAN_POINT ( 'NONE',  ( 47.09785597605719687, 23.12036939723557083, 47.04930799450080059 ) ) ;
#7702=CARTESIAN_POINT ( 'NONE',  ( 49.59034552300744281, 29.16454579224780019, 47.24294646780535345 ) ) ;
#7704=CARTESIAN_POINT ( 'NONE',  ( 46.00908685603034343, 26.14624452788249087, 44.91496614357595263 ) ) ;
#7705=ORIENTED_EDGE ( 'NONE', *, *, #12356, .T. ) ;
#7710=CARTESIAN_POINT ( 'NONE',  ( 47.09785597605719687, 23.12036939723557083, 47.04930799450080059 ) ) ;
#7731=VECTOR ( 'NONE', #25305, 1000.000000000000000 ) ;
#7737=CARTESIAN_POINT ( 'NONE',  ( 48.18662509608405031, 26.58284706826093213, 49.18364984542562013 ) ) ;
#7743=CARTESIAN_POINT ( 'NONE',  ( 48.23388202445966044, 26.25087065737812253, 49.27628909396054979 ) ) ;
#7751=CARTESIAN_POINT ( 'NONE',  ( 44.77625694075214824, 29.51454579807170120, 48.23360063142255427 ) ) ;
#7754=ORIENTED_EDGE ( 'NONE', *, *, #18245, .F. ) ;
#7769=CARTESIAN_POINT ( 'NONE',  ( 48.18662509608405031, 25.88284706826093284, 49.18364984542562013 ) ) ;
#7777=DIRECTION ( 'NONE',  ( 0.4544104193609903586, 0.000000000000000000, 0.8907924397839087627 ) ) ;
#7792=DIRECTION ( 'NONE',  ( 1.234978253042719660E-16, -1.000000000000000000, -1.109335647967047851E-31 ) ) ;
#7836=CARTESIAN_POINT ( 'NONE',  ( 46.84209603737756566, 23.10527845304106620, 46.54793520446708044 ) ) ;
#7841=CARTESIAN_POINT ( 'NONE',  ( 47.20547626766766314, 27.48791119454915233, 44.97710074790751378 ) ) ;
#7847=DIRECTION ( 'NONE',  ( 1.234978253042719660E-16, -1.000000000000000000, -1.109335647967047851E-31 ) ) ;
#7861=CARTESIAN_POINT ( 'NONE',  ( 46.35959775518843173, 23.04411657098542676, 47.91207660486297470 ) ) ;
#7867=( NAMED_UNIT ( * ) SI_UNIT ( $, .STERADIAN. ) SOLID_ANGLE_UNIT ( ) );
#7871=CARTESIAN_POINT ( 'NONE',  ( 48.37829923888483563, 29.55122849631042570, 45.07556196625585443 ) ) ;
#7887=CARTESIAN_POINT ( 'NONE',  ( 45.96182992765472619, 28.70087065737811827, 44.82232689504103007 ) ) ;
#7889=CARTESIAN_POINT ( 'NONE',  ( 48.40186567930497574, 27.51618040159426570, 45.03923535223907493 ) ) ;
#7901=ORIENTED_EDGE ( 'NONE', *, *, #1927, .F. ) ;
#7905=EDGE_CURVE ( 'NONE', #3283, #7173, #31270, .T. ) ;
#7912=CARTESIAN_POINT ( 'NONE',  ( 45.36511207810798396, 25.93213139976340997, 45.12672418911605376 ) ) ;
#7917=CARTESIAN_POINT ( 'NONE',  ( 45.13079246587579973, 22.86454579224779948, 47.59453030015130537 ) ) ;
#7921=CARTESIAN_POINT ( 'NONE',  ( 47.23302798462060537, 29.28121246473837047, 44.44659793406428605 ) ) ;
#7924=ORIENTED_EDGE ( 'NONE', *, *, #6901, .T. ) ;
#7927=CARTESIAN_POINT ( 'NONE',  ( 49.40052002316441104, 24.99301497605546629, 45.93418205075561644 ) ) ;
#7932=CARTESIAN_POINT ( 'NONE',  ( 47.66856441440319969, 23.10527865767145528, 46.91233790229156853 ) ) ;
#7937=CARTESIAN_POINT ( 'NONE',  ( 48.94625023931840957, 25.35784706826093426, 46.10640627770150246 ) ) ;
#7939=CARTESIAN_POINT ( 'NONE',  ( 46.00908685603034343, 29.64624452788248021, 44.91496614357595263 ) ) ;
#7964=CARTESIAN_POINT ( 'NONE',  ( 47.17209261226641104, 29.58954579224849368, 44.97563639035409011 ) ) ;
#7981=EDGE_CURVE ( 'NONE', #25543, #19007, #6295, .T. ) ;
#7985=VECTOR ( 'NONE', #6874, 1000.000000000000114 ) ;
#7992=CARTESIAN_POINT ( 'NONE',  ( 48.05211795450447454, 25.13954579807170120, 48.91997206816282784 ) ) ;
#8017=ORIENTED_EDGE ( 'NONE', *, *, #31304, .F. ) ;
#8036=CARTESIAN_POINT ( 'NONE',  ( 48.64577015523532566, 29.40030387703340864, 45.36886888450657551 ) ) ;
#8038=CARTESIAN_POINT ( 'NONE',  ( 48.80717017713595141, 27.97622849631043351, 48.15820438821415195 ) ) ;
#8039=VERTEX_POINT ( 'NONE', #2038 ) ;
#8043=DIRECTION ( 'NONE',  ( -0.4544104193609908027, -5.611869858668450607E-17, -0.8907924397839086517 ) ) ;
#8086=ORIENTED_EDGE ( 'NONE', *, *, #23084, .T. ) ;
#8093=DIRECTION ( 'NONE',  ( 1.234978253042719660E-16, -1.000000000000000000, -1.170965406187439618E-31 ) ) ;
#8094=ORIENTED_EDGE ( 'NONE', *, *, #26409, .T. ) ;
#8097=CARTESIAN_POINT ( 'NONE',  ( 48.18662509608405031, 27.98284706826092716, 49.18364984542562013 ) ) ;
#8107=CARTESIAN_POINT ( 'NONE',  ( 45.52675994804781112, 26.83420399681022772, 49.47108226228596806 ) ) ;
#8125=CARTESIAN_POINT ( 'NONE',  ( 48.83059987400640267, 26.15948166895303473, 48.97189179988551899 ) ) ;
#8172=AXIS2_PLACEMENT_3D ( 'NONE', #6286, #1354, #5977 ) ;
#8190=CARTESIAN_POINT ( 'NONE',  ( 49.07982864979221205, 29.33081545780508392, 45.80760694353075735 ) ) ;
#8192=CARTESIAN_POINT ( 'NONE',  ( 47.20353132263855400, 26.80956182964376566, 45.01455027646041174 ) ) ;
#8209=CARTESIAN_POINT ( 'NONE',  ( 44.70507715278255034, 25.64951373492759856, 46.92503878583767118 ) ) ;
#8210=EDGE_LOOP ( 'NONE', ( #29395, #11555, #5777, #16565, #485, #28106, #8240 ) ) ;
#8213=EDGE_CURVE ( 'NONE', #2756, #23081, #10828, .T. ) ;
#8218=( BOUNDED_CURVE ( )  B_SPLINE_CURVE ( 2, ( #31006, #22951, #10504, #3262, #20327 ),
 .UNSPECIFIED., .F., .F. ) 
 B_SPLINE_CURVE_WITH_KNOTS ( ( 3, 2, 3 ),
 ( 0.7671007452297479157, 0.8333333333333333703, 1.000000000000000000 ),
 .UNSPECIFIED. ) 
 CURVE ( )  GEOMETRIC_REPRESENTATION_ITEM ( )  RATIONAL_B_SPLINE_CURVE ( ( 0.9358335845890755067, 0.9467590945150633486, 1.000000000000000000, 0.8660254037844387076, 1.000000000000000000 ) ) 
 REPRESENTATION_ITEM ( '' )  );
#8219=ORIENTED_EDGE ( 'NONE', *, *, #18335, .T. ) ;
#8223=CARTESIAN_POINT ( 'NONE',  ( 49.19517401419062708, 27.70920399681022772, 48.40991706654173754 ) ) ;
#8231=CARTESIAN_POINT ( 'NONE',  ( 48.43931949325730812, 22.91889071986277671, 48.25583407606420394 ) ) ;
#8239=CARTESIAN_POINT ( 'NONE',  ( 48.73570333863616355, 29.22287913140504045, 44.52463952959527660 ) ) ;
#8240=ORIENTED_EDGE ( 'NONE', *, *, #5359, .F. ) ;
#8251=CARTESIAN_POINT ( 'NONE',  ( 49.49063479933183629, 25.99951373492759643, 47.17357720316391578 ) ) ;
#8253=CARTESIAN_POINT ( 'NONE',  ( 45.35708200440645044, 29.00457786121581805, 45.92000246470679770 ) ) ;
#8263=CARTESIAN_POINT ( 'NONE',  ( 46.96819297411687444, 26.89253733014356129, 49.54594323136014822 ) ) ;
#8264=CARTESIAN_POINT ( 'NONE',  ( 46.79153437246152691, 23.10527845304106265, 47.52148899368456370 ) ) ;
#8267=ORIENTED_EDGE ( 'NONE', *, *, #5396, .T. ) ;
#8275=CARTESIAN_POINT ( 'NONE',  ( 46.58637386172244277, 23.04411619146718238, 46.04663644226216945 ) ) ;
#8301=ORIENTED_EDGE ( 'NONE', *, *, #4000, .F. ) ;
#8309=CARTESIAN_POINT ( 'NONE',  ( 48.04075769285628894, 25.18284706826092645, 48.89770225776209145 ) ) ;
#8316=CARTESIAN_POINT ( 'NONE',  ( 47.11751843720308841, 23.11533908250407165, 46.67071160955749320 ) ) ;
#8320=CARTESIAN_POINT ( 'NONE',  ( 46.99023568444673060, 25.73791119454915588, 49.12151524109405898 ) ) ;
#8343=CARTESIAN_POINT ( 'NONE',  ( 48.37591806664303107, 29.43873978692154481, 45.20163774776087706 ) ) ;
#8347=CARTESIAN_POINT ( 'NONE',  ( 46.99218062947583974, 26.45956182964376424, 49.08406571254116102 ) ) ;
#8363=CARTESIAN_POINT ( 'NONE',  ( 48.83862994770795041, 25.94118040159426641, 48.17861352429476085 ) ) ;
#8367=AXIS2_PLACEMENT_3D ( 'NONE', #7992, #3044, #758 ) ;
#8374=ORIENTED_EDGE ( 'NONE', *, *, #5422, .F. ) ;
#8380=CARTESIAN_POINT ( 'NONE',  ( 48.23388202445966044, 27.65087065737811756, 49.27628909396056400 ) ) ;
#8406=FACE_OUTER_BOUND ( 'NONE', #2472, .T. ) ;
#8411=CARTESIAN_POINT ( 'NONE',  ( 49.41945501136223839, 29.16454579807170688, 45.86501535757901848 ) ) ;
#8416=EDGE_CURVE ( 'NONE', #25372, #19042, #9662, .T. ) ;
#8437=CARTESIAN_POINT ( 'NONE',  ( 46.53577443378190281, 23.10527845304106620, 47.02011620365084354 ) ) ;
#8444=CARTESIAN_POINT ( 'NONE',  ( 47.14013642192045239, 29.60499367036002738, 44.99018544319649493 ) ) ;
#8445=CARTESIAN_POINT ( 'NONE',  ( 49.66977585544405827, 24.86874180309281712, 46.07579470028509405 ) ) ;
#8447=EDGE_CURVE ( 'NONE', #4649, #3283, #1182, .T. ) ;
#8454=CARTESIAN_POINT ( 'NONE',  ( 48.76626135000090301, 22.93328494799376216, 47.45974698848920781 ) ) ;
#8479=LINE ( 'NONE', #3219, #1828 ) ;
#8487=EDGE_LOOP ( 'NONE', ( #19293, #20432, #2394, #11194 ) ) ;
#8498=UNCERTAINTY_MEASURE_WITH_UNIT (LENGTH_MEASURE( 1.000000000000000082E-05 ), #19687, 'distance_accuracy_value', 'NONE');
#8501=CIRCLE ( 'NONE', #7454, 2.749999999999998224 ) ;
#8512=CARTESIAN_POINT ( 'NONE',  ( 47.20353132263855400, 26.10956182964376637, 45.01455027646041174 ) ) ;
#8526=CARTESIAN_POINT ( 'NONE',  ( 48.51114023551905063, 22.99884124225578574, 46.96613737717972725 ) ) ;
#8538=ADVANCED_FACE ( 'NONE', ( #26300 ), #9387, .T. ) ;
#8563=DIRECTION ( 'NONE',  ( 0.4544104193609905806, 5.611869858668446909E-17, 0.8907924397839086517 ) ) ;
#8570=CARTESIAN_POINT ( 'NONE',  ( 44.77625694075214824, 30.21454579807170049, 48.23360063142255427 ) ) ;
#8615=ORIENTED_EDGE ( 'NONE', *, *, #18335, .F. ) ;
#8646=CARTESIAN_POINT ( 'NONE',  ( 48.83862994770794330, 25.15457786121582373, 48.17861352429476796 ) ) ;
#8668=CARTESIAN_POINT ( 'NONE',  ( 48.50303063523655567, 22.99884124225578574, 47.12228595530052644 ) ) ;
#8672=CARTESIAN_POINT ( 'NONE',  ( 48.91284552371730143, 26.69289516297710563, 46.12344667017377020 ) ) ;
#8685=ORIENTED_EDGE ( 'NONE', *, *, #30357, .F. ) ;
#8690=CARTESIAN_POINT ( 'NONE',  ( 49.19517401419062708, 25.48655426599986384, 48.40991706654173754 ) ) ;
#8694=CARTESIAN_POINT ( 'NONE',  ( 48.23388202445966755, 26.12822092656774586, 49.27628909396054979 ) ) ;
#8706=CARTESIAN_POINT ( 'NONE',  ( 47.57707823921868595, 22.93807716476589320, 48.70033069891094613 ) ) ;
#8726=CARTESIAN_POINT ( 'NONE',  ( 48.46535932150934656, 28.28954579807170688, 49.73005965046827015 ) ) ;
#8732=CARTESIAN_POINT ( 'NONE',  ( 45.35708200440645044, 29.79118040159425718, 45.92000246470679770 ) ) ;
#8745=CARTESIAN_POINT ( 'NONE',  ( 45.52675994804781112, 28.11155426599984963, 49.47108226228597516 ) ) ;
#8749=CARTESIAN_POINT ( 'NONE',  ( 46.00908685603033632, 26.84624452788248661, 44.91496614357595263 ) ) ;
#8750=CYLINDRICAL_SURFACE ( 'NONE', #65, 4.200000000000000178 ) ;
#8754=DIRECTION ( 'NONE',  ( 0.4544104193609912468, 5.611869858668455538E-17, 0.8907924397839084296 ) ) ;
#8762=ORIENTED_EDGE ( 'NONE', *, *, #25202, .F. ) ;
#8768=CARTESIAN_POINT ( 'NONE',  ( 49.19517401419062708, 27.58655426599985816, 48.40991706654173754 ) ) ;
#8777=CYLINDRICAL_SURFACE ( 'NONE', #31681, 2.499999999999997335 ) ;
#8814=CARTESIAN_POINT ( 'NONE',  ( 48.24187697582666345, 23.03451764446790051, 47.44084013591611892 ) ) ;
#8817=CARTESIAN_POINT ( 'NONE',  ( 49.44739180854976013, 28.07786309983298523, 47.17133137409169308 ) ) ;
#8825=CARTESIAN_POINT ( 'NONE',  ( 49.23380989124830620, 29.53436827284168231, 47.10497933316898411 ) ) ;
#8850=VECTOR ( 'NONE', #19472, 1000.000000000000114 ) ;
#8856=DIRECTION ( 'NONE',  ( 1.234978253042719660E-16, -1.000000000000000000, -1.109335647967047851E-31 ) ) ;
#8869=CARTESIAN_POINT ( 'NONE',  ( 45.96182992765471909, 15.77906836436399374, 44.82232689504101586 ) ) ;
#8884=CARTESIAN_POINT ( 'NONE',  ( 44.77625694075214824, 26.71454579807170759, 48.23360063142255427 ) ) ;
#8895=CARTESIAN_POINT ( 'NONE',  ( 49.98072202819530219, 28.46753733014355703, 47.19902993264913960 ) ) ;
#8896=CARTESIAN_POINT ( 'NONE',  ( 46.99023568444673060, 28.62451373492759643, 49.12151524109405898 ) ) ;
#8901=CARTESIAN_POINT ( 'NONE',  ( 47.16432553341419975, 22.86454579224779948, 45.05006465737218235 ) ) ;
#8911=CARTESIAN_POINT ( 'NONE',  ( 45.79384627280941089, 27.07957786121582444, 49.05938063676250493 ) ) ;
#8918=DIRECTION ( 'NONE',  ( -0.5442436726714893203, -1.289618226626749726E-16, 0.8389271868029124501 ) ) ;
#8952=CARTESIAN_POINT ( 'NONE',  ( 48.23388202445966755, 25.55087065737811969, 49.27628909396054979 ) ) ;
#8954=CARTESIAN_POINT ( 'NONE',  ( 46.47461290750400309, 22.93807716476589675, 45.47175308309371644 ) ) ;
#8971=ORIENTED_EDGE ( 'NONE', *, *, #25730, .T. ) ;
#8985=CARTESIAN_POINT ( 'NONE',  ( 48.80717017713595141, 28.71952976649964739, 48.15820438821415195 ) ) ;
#8997=CARTESIAN_POINT ( 'NONE',  ( 48.73570333863616355, 26.42287913140504330, 44.52463952959527660 ) ) ;
#9018=ORIENTED_EDGE ( 'NONE', *, *, #522, .F. ) ;
#9033=DIRECTION ( 'NONE',  ( 1.234978253042719660E-16, -1.000000000000000000, -1.109335647967047851E-31 ) ) ;
#9050=CARTESIAN_POINT ( 'NONE',  ( 49.41945501136223839, 27.76454579807170830, 45.86501535757901848 ) ) ;
#9057=CARTESIAN_POINT ( 'NONE',  ( 48.23388202445966044, 28.35087065737811685, 49.27628909396054979 ) ) ;
#9058=CARTESIAN_POINT ( 'NONE',  ( 48.94625023931840246, 28.15784706826092787, 46.10640627770150246 ) ) ;
#9062=AXIS2_PLACEMENT_3D ( 'NONE', #12431, #29992, #27030 ) ;
#9069=CARTESIAN_POINT ( 'NONE',  ( 48.23388202445966044, 28.22822092656774373, 49.27628909396054979 ) ) ;
#9071=VECTOR ( 'NONE', #20429, 1000.000000000000114 ) ;
#9076=CARTESIAN_POINT ( 'NONE',  ( 48.83862994770794330, 29.35457786121581591, 48.17861352429476796 ) ) ;
#9083=DIRECTION ( 'NONE',  ( -0.4441739386571982307, 0.2110602665713104398, -0.8707256032141232893 ) ) ;
#9118=CARTESIAN_POINT ( 'NONE',  ( 46.33059210211230550, 22.93807716476589675, 45.54522087609679204 ) ) ;
#9145=CARTESIAN_POINT ( 'NONE',  ( 46.02876340639226527, 29.01119643316631524, 44.95353858666495483 ) ) ;
#9151=FACE_OUTER_BOUND ( 'NONE', #1534, .T. ) ;
#9158=CARTESIAN_POINT ( 'NONE',  ( 50.10320668408830613, 27.00621246473837544, 47.20539118556276037 ) ) ;
#9164=EDGE_CURVE ( 'NONE', #15510, #19268, #24607, .T. ) ;
#9172=CARTESIAN_POINT ( 'NONE',  ( 47.99481790889201704, 22.99884124225578930, 45.95397743221676023 ) ) ;
#9195=CARTESIAN_POINT ( 'NONE',  ( 45.84097905237065618, 22.80400562401890241, 48.98672734302541443 ) ) ;
#9201=SURFACE_SIDE_STYLE ('',( #6903 ) ) ;
#9224=CARTESIAN_POINT ( 'NONE',  ( 45.35708200440645044, 29.09118040159425789, 45.92000246470679770 ) ) ;
#9227=EDGE_CURVE ( 'NONE', #3003, #23526, #20165, .T. ) ;
#9232=COLOUR_RGB ( '',0.7921568627450980005, 0.8196078431372548767, 0.9333333333333333481 ) ;
#9233=PLANE ( 'NONE',  #16534 ) ;
#9247=CARTESIAN_POINT ( 'NONE',  ( 47.37433252627624825, 14.98691807112499141, 47.59129209129815763 ) ) ;
#9254=CARTESIAN_POINT ( 'NONE',  ( 47.05339576314583638, 22.89977464660286444, 45.18578914680342251 ) ) ;
#9260=EDGE_CURVE ( 'NONE', #5063, #19350, #6641, .T. ) ;
#9263=EDGE_CURVE ( 'NONE', #6715, #11279, #18179, .T. ) ;
#9269=ORIENTED_EDGE ( 'NONE', *, *, #29204, .T. ) ;
#9300=ORIENTED_EDGE ( 'NONE', *, *, #12086, .F. ) ;
#9301=CIRCLE ( 'NONE', #13001, 0.04999999999999768518 ) ;
#9304=CARTESIAN_POINT ( 'NONE',  ( 47.86364407361583062, 22.99884124225578930, 45.86888002329718717 ) ) ;
#9307=CARTESIAN_POINT ( 'NONE',  ( 44.74832014356462651, 27.02786309983298452, 46.92728461490987257 ) ) ;
#9313=CARTESIAN_POINT ( 'NONE',  ( 49.18002788330665709, 29.51722998668063624, 47.59998504452501322 ) ) ;
#9318=CARTESIAN_POINT ( 'NONE',  ( 47.23302798462060537, 27.88121246473837544, 44.44659793406428605 ) ) ;
#9319=FACE_OUTER_BOUND ( 'NONE', #4377, .T. ) ;
#9320=DIRECTION ( 'NONE',  ( 0.4544104193609908027, 5.611869858668450607E-17, 0.8907924397839086517 ) ) ;
#9336=VERTEX_POINT ( 'NONE', #13594 ) ;
#9357=CARTESIAN_POINT ( 'NONE',  ( 45.33322567907855927, 22.86454579224779948, 47.99136533781562974 ) ) ;
#9374=CARTESIAN_POINT ( 'NONE',  ( 49.41945501136223839, 26.36454579807171328, 45.86501535757901848 ) ) ;
#9385=CARTESIAN_POINT ( 'NONE',  ( 48.18662509608405031, 29.38284706826092574, 49.18364984542562013 ) ) ;
#9387=CYLINDRICAL_SURFACE ( 'NONE', #16991, 2.499999999999997335 ) ;
#9390=B_SPLINE_CURVE_WITH_KNOTS ( 'NONE', 3,
 ( #12690, #22678, #17747, #5291, #15297, #2817 ),
 .UNSPECIFIED., .F., .F.,
 ( 4, 2, 4 ),
 ( 0.000000000000000000, 0.5000000000000000000, 1.000000000000000000 ),
 .UNSPECIFIED. ) ;
#9394=CARTESIAN_POINT ( 'NONE',  ( 47.09785597605719687, 15.77906836436399374, 47.04930799450078638 ) ) ;
#9400=ORIENTED_EDGE ( 'NONE', *, *, #12686, .T. ) ;
#9401=CARTESIAN_POINT ( 'NONE',  ( 45.47421713364555274, 22.88065857334294861, 45.99599230681428708 ) ) ;
#9410=DIRECTION ( 'NONE',  ( -0.09590798424311161585, -0.9774730502038649904, -0.1880108898004995421 ) ) ;
#9415=CARTESIAN_POINT ( 'NONE',  ( 46.99023568444673060, 29.32451373492759217, 49.12151524109405898 ) ) ;
#9428=AXIS2_PLACEMENT_3D ( 'NONE', #4486, #21540, #8918 ) ;
#9450=CARTESIAN_POINT ( 'NONE',  ( 47.09785597605719687, 24.86454579224779593, 47.04930799450078638 ) ) ;
#9478=CARTESIAN_POINT ( 'NONE',  ( 44.74832014356462651, 29.82786309983297812, 46.92728461490987257 ) ) ;
#9491=CARTESIAN_POINT ( 'NONE',  ( 50.10320668408830613, 27.70621246473837118, 47.20539118556276037 ) ) ;
#9515=AXIS2_PLACEMENT_3D ( 'NONE', #19150, #1268, #16685 ) ;
#9522=CARTESIAN_POINT ( 'NONE',  ( 45.67120842389707747, 22.84434098701873594, 48.65392161081025790 ) ) ;
#9527=DIRECTION ( 'NONE',  ( -0.4544104193609908027, 6.737912671758736131E-17, -0.8907924397839086517 ) ) ;
#9539=EDGE_CURVE ( 'NONE', #2200, #10117, #23819, .T. ) ;
#9548=LINE ( 'NONE', #15, #3327 ) ;
#9554=CARTESIAN_POINT ( 'NONE',  ( 47.20547626766766314, 26.17451373492760069, 44.97710074790751378 ) ) ;
#9568=CARTESIAN_POINT ( 'NONE',  ( 45.68651739446661963, 22.98879437201065912, 46.64337703648620703 ) ) ;
#9573=CARTESIAN_POINT ( 'NONE',  ( 47.22751897799751220, 27.24253733014356271, 44.55267275764142454 ) ) ;
#9575=ORIENTED_EDGE ( 'NONE', *, *, #28830, .T. ) ;
#9614=CYLINDRICAL_SURFACE ( 'NONE', #21686, 2.499999999999997335 ) ;
#9630=ADVANCED_FACE ( 'NONE', ( #10453 ), #5684, .F. ) ;
#9644=FACE_OUTER_BOUND ( 'NONE', #21802, .T. ) ;
#9650=CARTESIAN_POINT ( 'NONE',  ( 46.86059137560834387, 22.89977464660286444, 48.89819542093576388 ) ) ;
#9651=CARTESIAN_POINT ( 'NONE',  ( 47.20547626766765603, 29.58791119454915020, 44.97710074790751378 ) ) ;
#9662=( BOUNDED_CURVE ( )  B_SPLINE_CURVE ( 2, ( #20569, #3000, #8263, #8107, #3484, #866, #23025, #545, #28130 ),
 .UNSPECIFIED., .F., .F. ) 
 B_SPLINE_CURVE_WITH_KNOTS ( ( 3, 2, 2, 2, 3 ),
 ( 0.5357142868755583320, 0.5476190476190476719, 0.5714285714285713969, 0.5952380952380952328, 0.6071428583041297289 ),
 .UNSPECIFIED. ) 
 CURVE ( )  GEOMETRIC_REPRESENTATION_ITEM ( )  RATIONAL_B_SPLINE_CURVE ( ( 0.9330127018922200755, 0.9330127084266224280, 1.000000000000000000, 0.8660254037844388186, 1.000000000000000000, 0.8660254037844388186, 1.000000000000000000, 0.9330126953578163906, 0.9330127018922200755 ) ) 
 REPRESENTATION_ITEM ( '' )  );
#9680=CARTESIAN_POINT ( 'NONE',  ( 48.40186567930498285, 26.02957786121582373, 45.03923535223908203 ) ) ;
#9692=CARTESIAN_POINT ( 'NONE',  ( 45.24946171279598417, 27.72124452788248661, 47.99220971130007740 ) ) ;
#9701=CARTESIAN_POINT ( 'NONE',  ( 48.59475124299144255, 29.58954579224780090, 45.61232171765963272 ) ) ;
#9705=CARTESIAN_POINT ( 'NONE',  ( 44.09250526802607340, 26.65621246473837402, 46.89322480343881949 ) ) ;
#9728=DIRECTION ( 'NONE',  ( -0.4544104193609908027, -5.611869858668450607E-17, -0.8907924397839086517 ) ) ;
#9748=LINE ( 'NONE', #2192, #15698 ) ;
#9785=LINE ( 'NONE', #12908, #9071 ) ;
#9801=PLANE ( 'NONE',  #9062 ) ;
#9807=CARTESIAN_POINT ( 'NONE',  ( 46.04844006429465253, 22.86454579224779948, 44.99211097489548905 ) ) ;
#9814=CARTESIAN_POINT ( 'NONE',  ( 45.79384627280941089, 28.47957786121581591, 49.05938063676249072 ) ) ;
#9819=CARTESIAN_POINT ( 'NONE',  ( 47.12239238930854413, 29.59960605238285680, 44.98451356130378542 ) ) ;
#9821=ADVANCED_FACE ( 'NONE', ( #30962 ), #8777, .T. ) ;
#9834=CARTESIAN_POINT ( 'NONE',  ( 45.69268131687783807, 22.99884124225578574, 46.97633003370108185 ) ) ;
#9840=CARTESIAN_POINT ( 'NONE',  ( 49.44739180854976013, 29.43456182964375856, 47.17133137409169308 ) ) ;
#9851=CARTESIAN_POINT ( 'NONE',  ( 46.99023568444673060, 27.83791119454915375, 49.12151524109405898 ) ) ;
#9852=EDGE_CURVE ( 'NONE', #25360, #22418, #13027, .T. ) ;
#9856=CARTESIAN_POINT ( 'NONE',  ( 45.36511207810799107, 28.73213139976340713, 45.12672418911605376 ) ) ;
#9861=CARTESIAN_POINT ( 'NONE',  ( 47.20547626766765603, 28.27451373492759501, 44.97710074790751378 ) ) ;
#9864=CARTESIAN_POINT ( 'NONE',  ( 48.46535932150934656, 25.48954579807171328, 49.73005965046827015 ) ) ;
#9874=CARTESIAN_POINT ( 'NONE',  ( 49.49063479933183629, 25.29951373492760069, 47.17357720316391578 ) ) ;
#9893=LINE ( 'NONE', #14825, #17190 ) ;
#9898=ORIENTED_EDGE ( 'NONE', *, *, #15958, .T. ) ;
#9913=ORIENTED_EDGE ( 'NONE', *, *, #9263, .T. ) ;
#9921=EDGE_LOOP ( 'NONE', ( #21493, #2190, #15148, #23125, #29047 ) ) ;
#9962=CARTESIAN_POINT ( 'NONE',  ( 48.40423897560355471, 29.16454579224780019, 44.91779129072006072 ) ) ;
#9978=CARTESIAN_POINT ( 'NONE',  ( 45.24946171279598417, 28.42124452788248590, 47.99220971130007030 ) ) ;
#10001=CARTESIAN_POINT ( 'NONE',  ( 45.91943065483079778, 23.03451764446789696, 47.32022353109342561 ) ) ;
#10009=CARTESIAN_POINT ( 'NONE',  ( 49.49063479933183629, 26.61291119454915588, 47.17357720316391578 ) ) ;
#10023=EDGE_LOOP ( 'NONE', ( #366, #19407, #22453, #31264, #31257, #7238 ) ) ;
#10029=VECTOR ( 'NONE', #647, 1000.000000000000000 ) ;
#10030=ORIENTED_EDGE ( 'NONE', *, *, #29521, .T. ) ;
#10040=EDGE_CURVE ( 'NONE', #17834, #21141, #11022, .T. ) ;
#10043=CARTESIAN_POINT ( 'NONE',  ( 48.40186567930498285, 26.11618040159426357, 45.03923535223908203 ) ) ;
#10053=CARTESIAN_POINT ( 'NONE',  ( 45.41653742442152719, 20.36454579224779948, 43.75337596730032175 ) ) ;
#10060=CARTESIAN_POINT ( 'NONE',  ( 45.84097905237065618, 22.86454579224779948, 48.98672734302541443 ) ) ;
#10076=CARTESIAN_POINT ( 'NONE',  ( 45.35708200440645044, 26.99118040159426357, 45.92000246470679770 ) ) ;
#10117=VERTEX_POINT ( 'NONE', #30562 ) ;
#10143=CARTESIAN_POINT ( 'NONE',  ( 48.40186567930498285, 28.12957786121581805, 45.03923535223908203 ) ) ;
#10163=CARTESIAN_POINT ( 'NONE',  ( 46.33206787849857022, 22.99884124225578574, 48.22973596570440691 ) ) ;
#10172=CARTESIAN_POINT ( 'NONE',  ( 48.83862994770794330, 27.25457786121581805, 48.17861352429476796 ) ) ;
#10182=CARTESIAN_POINT ( 'NONE',  ( 45.35708200440645044, 25.50457786121582515, 45.92000246470680480 ) ) ;
#10186=DIRECTION ( 'NONE',  ( -0.4544104193609937448, 0.000000000000000000, -0.8907924397839072084 ) ) ;
#10187=CARTESIAN_POINT ( 'NONE',  ( 48.23388202445966044, 29.05087065737811969, 49.27628909396056400 ) ) ;
#10190=CARTESIAN_POINT ( 'NONE',  ( 48.40186567930497574, 28.21618040159426499, 45.03923535223908203 ) ) ;
#10204=CARTESIAN_POINT ( 'NONE',  ( 46.00908685603034343, 25.53284706826093498, 44.91496614357595263 ) ) ;
#10223=CARTESIAN_POINT ( 'NONE',  ( 48.28307451434712760, 25.08930407213309977, 44.81510409515678361 ) ) ;
#10227=ORIENTED_EDGE ( 'NONE', *, *, #12686, .F. ) ;
#10236=CARTESIAN_POINT ( 'NONE',  ( 47.20547626766766314, 25.47451373492760140, 44.97710074790751378 ) ) ;
#10257=ORIENTED_EDGE ( 'NONE', *, *, #8447, .T. ) ;
#10294=DIRECTION ( 'NONE',  ( 1.234978253042719660E-16, -1.000000000000000000, -1.109335647967047851E-31 ) ) ;
#10304=CARTESIAN_POINT ( 'NONE',  ( 48.01680169312756874, 22.93807716476589675, 45.63279442905646022 ) ) ;
#10308=CARTESIAN_POINT ( 'NONE',  ( 49.49063479933183629, 26.61291119454915588, 47.17357720316391578 ) ) ;
#10324=CARTESIAN_POINT ( 'NONE',  ( 45.37383841111020644, 22.88065857334295217, 47.92876263475718446 ) ) ;
#10330=CARTESIAN_POINT ( 'NONE',  ( 45.35708200440645044, 26.20457786121582444, 45.92000246470679770 ) ) ;
#10339=CARTESIAN_POINT ( 'NONE',  ( 46.17891025898683921, 22.93807716476589675, 48.46582155994513386 ) ) ;
#10346=CARTESIAN_POINT ( 'NONE',  ( 48.18662509608405031, 28.68284706826093000, 49.18364984542562013 ) ) ;
#10357=VERTEX_POINT ( 'NONE', #7710 ) ;
#10373=CARTESIAN_POINT ( 'NONE',  ( 45.29931651390019454, 22.86454579224779948, 47.92489232862990889 ) ) ;
#10381=CARTESIAN_POINT ( 'NONE',  ( 49.65101332465108186, 24.93501648625822398, 46.52608845888364186 ) ) ;
#10386=CARTESIAN_POINT ( 'NONE',  ( 48.22193606911519481, 23.04411619146717882, 47.10768726602483980 ) ) ;
#10391=CARTESIAN_POINT ( 'NONE',  ( 46.99023568444673060, 28.62451373492759643, 49.12151524109405898 ) ) ;
#10393=CARTESIAN_POINT ( 'NONE',  ( 48.83862994770794330, 28.65457786121581663, 48.17861352429476796 ) ) ;
#10407=AXIS2_PLACEMENT_3D ( 'NONE', #25651, #20396, #7777 ) ;
#10419=ORIENTED_EDGE ( 'NONE', *, *, #32056, .F. ) ;
#10427=CARTESIAN_POINT ( 'NONE',  ( 48.66895200406656841, 26.36155426599985674, 44.62753372671560470 ) ) ;
#10433=DIRECTION ( 'NONE',  ( 1.234978253042719660E-16, -1.000000000000000000, -1.109335647967047851E-31 ) ) ;
#10442=ORIENTED_EDGE ( 'NONE', *, *, #15354, .T. ) ;
#10453=FACE_OUTER_BOUND ( 'NONE', #18636, .T. ) ;
#10464=CARTESIAN_POINT ( 'NONE',  ( 46.58637386172244277, 23.04411619146718238, 46.04663644226216945 ) ) ;
#10470=CARTESIAN_POINT ( 'NONE',  ( 45.79384627280941089, 24.97957786121582302, 49.05938063676249072 ) ) ;
#10472=CARTESIAN_POINT ( 'NONE',  ( 47.09785597605719687, 20.36454579224780304, 47.04930799450078638 ) ) ;
#10476=AXIS2_PLACEMENT_3D ( 'NONE', #25799, #8093, #26115 ) ;
#10496=CARTESIAN_POINT ( 'NONE',  ( 48.37829923888483563, 28.15122849631042712, 45.07556196625585443 ) ) ;
#10504=CARTESIAN_POINT ( 'NONE',  ( 49.84415473660248352, 24.82319976284615137, 47.19193729663540893 ) ) ;
#10507=CARTESIAN_POINT ( 'NONE',  ( 47.47194490827082092, 22.91413368675619111, 45.28548791484912783 ) ) ;
#10512=VECTOR ( 'NONE', #19396, 999.9999999999998863 ) ;
#10517=DIRECTION ( 'NONE',  ( 1.234978253042719660E-16, -1.000000000000000000, -1.109335647967047851E-31 ) ) ;
#10550=CARTESIAN_POINT ( 'NONE',  ( 50.10320668408830613, 28.40621246473837402, 47.20539118556276037 ) ) ;
#10560=CARTESIAN_POINT ( 'NONE',  ( 48.79245099466763946, 22.93807716476589675, 46.97542197481624271 ) ) ;
#10564=CARTESIAN_POINT ( 'NONE',  ( 45.24946171279598417, 27.10784706826093071, 47.99220971130007030 ) ) ;
#10566=CARTESIAN_POINT ( 'NONE',  ( 48.18662509608405031, 27.89624452788248377, 49.18364984542562013 ) ) ;
#10596=CARTESIAN_POINT ( 'NONE',  ( 48.23388202445966044, 26.12822092656774586, 49.27628909396054979 ) ) ;
#10610=VECTOR ( 'NONE', #19933, 1000.000000000000000 ) ;
#10617=CARTESIAN_POINT ( 'NONE',  ( 48.66895200406656841, 27.76155426599985176, 44.62753372671560470 ) ) ;
#10631=DIRECTION ( 'NONE',  ( -1.234978253042719660E-16, 1.000000000000000000, 1.170965406187439618E-31 ) ) ;
#10632=CARTESIAN_POINT ( 'NONE',  ( 45.64214785356322324, 22.86454579224779593, 45.61839217665156809 ) ) ;
#10634=CARTESIAN_POINT ( 'NONE',  ( 47.09785597605719687, 23.12036939723557083, 47.04930799450080059 ) ) ;
#10652=ADVANCED_FACE ( 'NONE', ( #14740 ), #7517, .F. ) ;
#10668=CARTESIAN_POINT ( 'NONE',  ( 49.44739180854976013, 25.93456182964376566, 47.17133137409169308 ) ) ;
#10673=ORIENTED_EDGE ( 'NONE', *, *, #9539, .F. ) ;
#10676=CARTESIAN_POINT ( 'NONE',  ( 46.76672225489305390, 14.98691807112499141, 47.55973575893985839 ) ) ;
#10678=CARTESIAN_POINT ( 'NONE',  ( 45.24946171279598417, 25.62124452788248874, 47.99220971130007740 ) ) ;
#10696=EDGE_CURVE ( 'NONE', #18648, #10357, #27265, .T. ) ;
#10723=CARTESIAN_POINT ( 'NONE',  ( 48.83862994770794330, 28.04118040159426428, 48.17861352429476796 ) ) ;
#10724=CARTESIAN_POINT ( 'NONE',  ( 45.79384627280941089, 29.17957786121581165, 49.05938063676249072 ) ) ;
#10747=CARTESIAN_POINT ( 'NONE',  ( 47.09785597605719687, 19.86454579224779948, 47.04930799450078638 ) ) ;
#10749=CARTESIAN_POINT ( 'NONE',  ( 47.09785597605719687, 23.12036939723557083, 47.04930799450080059 ) ) ;
#10774=EDGE_CURVE ( 'NONE', #2302, #456, #5366, .T. ) ;
#10798=EDGE_LOOP ( 'NONE', ( #13447, #30164, #15207, #19498 ) ) ;
#10806=CIRCLE ( 'NONE', #25915, 0.4999999999999988343 ) ;
#10808=ORIENTED_EDGE ( 'NONE', *, *, #13669, .T. ) ;
#10813=ORIENTED_EDGE ( 'NONE', *, *, #29615, .F. ) ;
#10819=CARTESIAN_POINT ( 'NONE',  ( 47.60933809039193676, 23.04411619146718238, 48.05197954673941751 ) ) ;
#10822=CARTESIAN_POINT ( 'NONE',  ( 48.91284552371730143, 27.39289516297709426, 46.12344667017377020 ) ) ;
#10828=CIRCLE ( 'NONE', #16560, 0.3000000000000017653 ) ;
#10834=ORIENTED_EDGE ( 'NONE', *, *, #15281, .F. ) ;
#10840=CARTESIAN_POINT ( 'NONE',  ( 47.20547626766764893, 25.47451373492760140, 44.97710074790751378 ) ) ;
#10845=CYLINDRICAL_SURFACE ( 'NONE', #1730, 7.999999999999999112 ) ;
#10850=ORIENTED_EDGE ( 'NONE', *, *, #396, .T. ) ;
#10851=CARTESIAN_POINT ( 'NONE',  ( 48.68948053213853910, 22.89977464660286444, 46.07904489681320115 ) ) ;
#10867=CARTESIAN_POINT ( 'NONE',  ( 47.12319097693831793, 23.24793988701932079, 46.08163201552200405 ) ) ;
#10880=CARTESIAN_POINT ( 'NONE',  ( 44.77625694075214824, 28.11454579807170617, 48.23360063142255427 ) ) ;
#10881=CARTESIAN_POINT ( 'NONE',  ( 45.35708200440645044, 27.60457786121581947, 45.92000246470679770 ) ) ;
#10900=CARTESIAN_POINT ( 'NONE',  ( 46.31918597887777622, 22.99884124225578930, 45.86695323169868033 ) ) ;
#10913=VERTEX_POINT ( 'NONE', #9118 ) ;
#10916=CARTESIAN_POINT ( 'NONE',  ( 47.09785597605719687, 15.77906836436399374, 47.04930799450078638 ) ) ;
#10921=ORIENTED_EDGE ( 'NONE', *, *, #22486, .F. ) ;
#10927=CARTESIAN_POINT ( 'NONE',  ( 46.55854765242722948, 27.84696019071910555, 44.51792966461572831 ) ) ;
#10939=CARTESIAN_POINT ( 'NONE',  ( 46.49024570467398121, 14.98691807112498964, 47.01775166214249424 ) ) ;
#10950=CARTESIAN_POINT ( 'NONE',  ( 47.09785597605719687, 29.86454579224779948, 47.04930799450078638 ) ) ;
#10973=CARTESIAN_POINT ( 'NONE',  ( 48.21416462065301545, 23.04411657098542321, 47.25727406314477008 ) ) ;
#10976=CARTESIAN_POINT ( 'NONE',  ( 48.16694854572211426, 25.81789516297710207, 49.14507740233662503 ) ) ;
#10979=EDGE_LOOP ( 'NONE', ( #30626, #4497, #943, #26818, #18126, #20314, #25103, #22210, #24276, #27130, #10834, #16903, #22311, #10227, #10921, #13227 ) ) ;
#10994=CARTESIAN_POINT ( 'NONE',  ( 48.66895200406656841, 25.66155426599986100, 44.62753372671560470 ) ) ;
#10995=CARTESIAN_POINT ( 'NONE',  ( 47.20547626766765603, 26.87451373492759643, 44.97710074790751378 ) ) ;
#11007=CARTESIAN_POINT ( 'NONE',  ( 49.98072202819530219, 25.66753733014356342, 47.19902993264913960 ) ) ;
#11008=CIRCLE ( 'NONE', #2613, 2.800000000000002043 ) ;
#11022=LINE ( 'NONE', #5605, #18090 ) ;
#11026=( NAMED_UNIT ( * ) PLANE_ANGLE_UNIT ( ) SI_UNIT ( $, .RADIAN. ) );
#11037=PLANE ( 'NONE',  #10476 ) ;
#11041=CARTESIAN_POINT ( 'NONE',  ( 49.41945501136223839, 27.06454579807170902, 45.86501535757901848 ) ) ;
#11043=AXIS2_PLACEMENT_3D ( 'NONE', #26844, #21746, #1240 ) ;
#11051=EDGE_CURVE ( 'NONE', #2200, #2756, #21505, .T. ) ;
#11065=CARTESIAN_POINT ( 'NONE',  ( 46.96819297411687444, 28.16988759933318676, 49.54594323136014822 ) ) ;
#11112=CARTESIAN_POINT ( 'NONE',  ( 46.71980555233013632, 23.04411657098542676, 45.97857331549464277 ) ) ;
#11117=ORIENTED_EDGE ( 'NONE', *, *, #25020, .T. ) ;
#11138=CARTESIAN_POINT ( 'NONE',  ( 47.92168837363949052, 23.03451764446790051, 47.93439649084938736 ) ) ;
#11141=CARTESIAN_POINT ( 'NONE',  ( 47.20353132263855400, 28.20956182964376069, 45.01455027646040463 ) ) ;
#11158=CARTESIAN_POINT ( 'NONE',  ( 48.94625023931840246, 25.35784706826093426, 46.10640627770148825 ) ) ;
#11165=EDGE_CURVE ( 'NONE', #20447, #24091, #18263, .T. ) ;
#11181=CARTESIAN_POINT ( 'NONE',  ( 47.62434977220233634, 29.18891845522693274, 44.62129988634950450 ) ) ;
#11191=( BOUNDED_CURVE ( )  B_SPLINE_CURVE ( 3, ( #37, #350, #7917, #10373 ),
 .UNSPECIFIED., .F., .F. ) 
 B_SPLINE_CURVE_WITH_KNOTS ( ( 4, 4 ),
 ( 5.062864179022702693, 5.184122060454624759 ),
 .UNSPECIFIED. ) 
 CURVE ( )  GEOMETRIC_REPRESENTATION_ITEM ( )  RATIONAL_B_SPLINE_CURVE ( ( 1.000000000000000000, 0.9987750858034806223, 0.9987750858034806223, 1.000000000000000000 ) ) 
 REPRESENTATION_ITEM ( '' )  );
#11194=ORIENTED_EDGE ( 'NONE', *, *, #15234, .F. ) ;
#11196=CARTESIAN_POINT ( 'NONE',  ( 49.41945501136223839, 29.86454579807170262, 45.86501535757901848 ) ) ;
#11204=CARTESIAN_POINT ( 'NONE',  ( 48.66895200406656130, 28.58420399681022062, 44.62753372671561181 ) ) ;
#11218=ORIENTED_EDGE ( 'NONE', *, *, #1174, .F. ) ;
#11220=CARTESIAN_POINT ( 'NONE',  ( 45.35708200440645044, 29.00457786121581805, 45.92000246470680480 ) ) ;
#11231=B_SPLINE_CURVE_WITH_KNOTS ( 'NONE', 3,
 ( #25433, #22804, #10507, #5575, #2939, #5415 ),
 .UNSPECIFIED., .F., .F.,
 ( 4, 2, 4 ),
 ( 0.000000000000000000, 0.5000000000000000000, 1.000000000000000000 ),
 .UNSPECIFIED. ) ;
#11279=VERTEX_POINT ( 'NONE', #17508 ) ;
#11290=CARTESIAN_POINT ( 'NONE',  ( 47.41589883262609817, 23.11533908250407165, 47.25563437782572151 ) ) ;
#11294=CARTESIAN_POINT ( 'NONE',  ( 45.28286642839709231, 27.78619643316631738, 47.97516931882780966 ) ) ;
#11300=CARTESIAN_POINT ( 'NONE',  ( 49.01277441251810529, 29.50101108909405667, 48.06976730914941243 ) ) ;
#11325=CARTESIAN_POINT ( 'NONE',  ( 49.19517401419062708, 25.60920399681023341, 48.40991706654173754 ) ) ;
#11337=CARTESIAN_POINT ( 'NONE',  ( 47.09785597605719687, 15.77906836436399374, 47.04930799450078638 ) ) ;
#11353=CARTESIAN_POINT ( 'NONE',  ( 50.10320668408830613, 27.70621246473837118, 47.20539118556276037 ) ) ;
#11361=CARTESIAN_POINT ( 'NONE',  ( 46.00908685603034343, 29.03284706826092787, 44.91496614357595263 ) ) ;
#11362=VERTEX_POINT ( 'NONE', #2415 ) ;
#11372=CARTESIAN_POINT ( 'NONE',  ( 48.23388202445966044, 28.22822092656774373, 49.27628909396054979 ) ) ;
#11375=CARTESIAN_POINT ( 'NONE',  ( 48.18662509608405031, 29.29624452788248234, 49.18364984542562013 ) ) ;
#11385=LINE ( 'NONE', #14183, #30926 ) ;
#11412=CARTESIAN_POINT ( 'NONE',  ( 45.47421713364555274, 22.88065857334294861, 45.99599230681428708 ) ) ;
#11422=ORIENTED_EDGE ( 'NONE', *, *, #1149, .F. ) ;
#11427=ORIENTED_EDGE ( 'NONE', *, *, #12241, .F. ) ;
#11430=ORIENTED_EDGE ( 'NONE', *, *, #6115, .T. ) ;
#11437=EDGE_CURVE ( 'NONE', #22710, #11279, #18145, .T. ) ;
#11441=LINE ( 'NONE', #7006, #8850 ) ;
#11444=CARTESIAN_POINT ( 'NONE',  ( 48.16694854572211426, 26.56119643316631951, 49.14507740233662503 ) ) ;
#11456=CARTESIAN_POINT ( 'NONE',  ( 48.46535932150934656, 25.48954579807171328, 49.73005965046827015 ) ) ;
#11463=CARTESIAN_POINT ( 'NONE',  ( 47.09785597605719687, 29.16454579224780019, 47.04930799450078638 ) ) ;
#11469=EDGE_LOOP ( 'NONE', ( #22524, #29133, #24942, #15017, #11422, #3381 ) ) ;
#11490=VERTEX_POINT ( 'NONE', #761 ) ;
#11500=AXIS2_PLACEMENT_3D ( 'NONE', #10916, #10433, #25365 ) ;
#11501=DIRECTION ( 'NONE',  ( 1.234978253042719660E-16, -1.000000000000000000, -1.170965406187439618E-31 ) ) ;
#11507=CARTESIAN_POINT ( 'NONE',  ( 48.73570333863616355, 29.92287913140503619, 44.52463952959527660 ) ) ;
#11517=CARTESIAN_POINT ( 'NONE',  ( 47.20547626766765603, 29.67451373492759004, 44.97710074790751378 ) ) ;
#11537=ORIENTED_EDGE ( 'NONE', *, *, #5669, .T. ) ;
#11539=CARTESIAN_POINT ( 'NONE',  ( 45.41164638504195494, 22.93807716476589675, 46.96173444154113241 ) ) ;
#11540=CARTESIAN_POINT ( 'NONE',  ( 45.24946171279598417, 26.32124452788248803, 47.99220971130008451 ) ) ;
#11555=ORIENTED_EDGE ( 'NONE', *, *, #30698, .T. ) ;
#11589=VERTEX_POINT ( 'NONE', #1882 ) ;
#11604=AXIS2_PLACEMENT_3D ( 'NONE', #14700, #7478, #17137 ) ;
#11614=CARTESIAN_POINT ( 'NONE',  ( 48.16694854572211426, 27.96119643316631453, 49.14507740233662503 ) ) ;
#11626=CARTESIAN_POINT ( 'NONE',  ( 44.91142894931555674, 25.89787913140504472, 45.63089057098605394 ) ) ;
#11631=DIRECTION ( 'NONE',  ( -0.3935310072385434510, 0.5000000000000004441, -0.7714488617801033010 ) ) ;
#11636=CARTESIAN_POINT ( 'NONE',  ( 48.48814272641119061, 22.95310733321322161, 46.17903408117996378 ) ) ;
#11655=CARTESIAN_POINT ( 'NONE',  ( 45.96182992765471909, 28.57822092656774160, 44.82232689504102296 ) ) ;
#11662=CARTESIAN_POINT ( 'NONE',  ( 47.07252097517607581, 23.24793988701932079, 48.01698397347956870 ) ) ;
#11682=CARTESIAN_POINT ( 'NONE',  ( 44.91142894931555674, 26.59787913140504401, 45.63089057098605394 ) ) ;
#11689=CARTESIAN_POINT ( 'NONE',  ( 45.04270468994605636, 22.74928388133296764, 48.43919039919626357 ) ) ;
#11692=CARTESIAN_POINT ( 'NONE',  ( 45.24946171279598417, 27.80784706826093000, 47.99220971130007030 ) ) ;
#11694=AXIS2_PLACEMENT_3D ( 'NONE', #28220, #13453, #25587 ) ;
#11705=CARTESIAN_POINT ( 'NONE',  ( 47.63716429968715715, 28.19696019071910342, 49.58068632438583734 ) ) ;
#11708=CARTESIAN_POINT ( 'NONE',  ( 48.34748475735720774, 25.40653309617948352, 49.49898713858203791 ) ) ;
#11714=FACE_OUTER_BOUND ( 'NONE', #11882, .T. ) ;
#11717=FACE_OUTER_BOUND ( 'NONE', #30779, .T. ) ;
#11725=B_SPLINE_CURVE_WITH_KNOTS ( 'NONE', 3,
 ( #6623, #13697, #31578, #14180, #16615, #1200 ),
 .UNSPECIFIED., .F., .F.,
 ( 4, 2, 4 ),
 ( 0.000000000000000000, 0.5000000000000000000, 1.000000000000000000 ),
 .UNSPECIFIED. ) ;
#11745=DIRECTION ( 'NONE',  ( -0.9986540920324801229, -6.158269594508763597E-17, -0.05186525298099636111 ) ) ;
#11764=AXIS2_PLACEMENT_3D ( 'NONE', #1757, #29503, #14401 ) ;
#11775=CARTESIAN_POINT ( 'NONE',  ( 48.37829923888483563, 28.19452976649965237, 45.07556196625585443 ) ) ;
#11783=CARTESIAN_POINT ( 'NONE',  ( 49.22880864277328072, 29.52863415674993064, 47.27039427357411938 ) ) ;
#11788=CARTESIAN_POINT ( 'NONE',  ( 50.10320668408830613, 25.60621246473838042, 47.20539118556276037 ) ) ;
#11791=FACE_OUTER_BOUND ( 'NONE', #4399, .T. ) ;
#11801=CARTESIAN_POINT ( 'NONE',  ( 45.84097905237065618, 22.86454579224779948, 48.98672734302541443 ) ) ;
#11821=CARTESIAN_POINT ( 'NONE',  ( 45.61530479625130852, 22.89977464660286444, 45.91938710987583505 ) ) ;
#11832=ORIENTED_EDGE ( 'NONE', *, *, #6446, .F. ) ;
#11842=CARTESIAN_POINT ( 'NONE',  ( 48.73570333863616355, 26.42287913140504330, 44.52463952959527660 ) ) ;
#11851=CARTESIAN_POINT ( 'NONE',  ( 45.38854177497844944, 26.26952976649965876, 45.94041160078741370 ) ) ;
#11860=CARTESIAN_POINT ( 'NONE',  ( 45.36511207810799107, 26.50948166895304325, 45.12672418911606087 ) ) ;
#11880=EDGE_LOOP ( 'NONE', ( #27640, #4180, #20386, #19073 ) ) ;
#11881=CARTESIAN_POINT ( 'NONE',  ( 45.11371142117359057, 29.27222086838446202, 45.70422120043853909 ) ) ;
#11882=EDGE_LOOP ( 'NONE', ( #30505, #13915, #14275, #26679, #22550, #15492 ) ) ;
#11930=EDGE_CURVE ( 'NONE', #6715, #23081, #1103, .T. ) ;
#11934=CARTESIAN_POINT ( 'NONE',  ( 46.02876340639226527, 26.91119643316632093, 44.95353858666495483 ) ) ;
#11946=CARTESIAN_POINT ( 'NONE',  ( 48.73570333863616355, 27.12287913140504259, 44.52463952959527660 ) ) ;
#11947=CARTESIAN_POINT ( 'NONE',  ( 47.47590639978425031, 23.04411657098542321, 48.12004267350693709 ) ) ;
#11948=FACE_OUTER_BOUND ( 'NONE', #17033, .T. ) ;
#11955=CARTESIAN_POINT ( 'NONE',  ( 48.55603101936429056, 22.91413368675619111, 45.98877541807350156 ) ) ;
#11960=ORIENTED_EDGE ( 'NONE', *, *, #17634, .T. ) ;
#12011=CARTESIAN_POINT ( 'NONE',  ( 44.74832014356462651, 25.62786309983298949, 46.92728461490987257 ) ) ;
#12015=EDGE_CURVE ( 'NONE', #1960, #30715, #26422, .T. ) ;
#12036=EDGE_CURVE ( 'NONE', #19007, #24927, #14068, .T. ) ;
#12040=CARTESIAN_POINT ( 'NONE',  ( 45.79384627280941089, 29.26618040159425860, 49.05938063676249072 ) ) ;
#12073=AXIS2_PLACEMENT_3D ( 'NONE', #17426, #22507, #9728 ) ;
#12086=EDGE_CURVE ( 'NONE', #7375, #23526, #22188, .T. ) ;
#12093=CIRCLE ( 'NONE', #11043, 0.1000000000000016431 ) ;
#12098=VECTOR ( 'NONE', #12932, 1000.000000000000000 ) ;
#12110=ORIENTED_EDGE ( 'NONE', *, *, #10040, .F. ) ;
#12120=CARTESIAN_POINT ( 'NONE',  ( 44.77625694075214824, 27.41454579807170688, 48.23360063142255427 ) ) ;
#12144=DIRECTION ( 'NONE',  ( 0.4544104193609911913, 0.000000000000000000, 0.8907924397839085406 ) ) ;
#12145=DIRECTION ( 'NONE',  ( 0.7549115352271290602, 0.6546536707079775308, 0.03920644602090527647 ) ) ;
#12156=CARTESIAN_POINT ( 'NONE',  ( 48.18662509608405742, 27.19624452788248803, 49.18364984542562013 ) ) ;
#12164=CARTESIAN_POINT ( 'NONE',  ( 45.79384627280941089, 27.16618040159427139, 49.05938063676250493 ) ) ;
#12180=CARTESIAN_POINT ( 'NONE',  ( 48.83862994770794330, 25.24118040159426712, 48.17861352429476796 ) ) ;
#12185=DIRECTION ( 'NONE',  ( -0.03667427209081837447, 0.7071067811865474617, 0.7061550805358612903 ) ) ;
#12191=B_SPLINE_SURFACE_WITH_KNOTS ( 'NONE', 3, 3, ( 
 ( #21138, #13941, #13015, #10386, #20384, #30415 ),
 ( #30579, #23010, #7932, #526, #8526, #10560 ),
 ( #3756, #3593, #18519, #28554, #16064, #26073 ),
 ( #13779, #31815, #24422, #19164, #2103, #26562 ),
 ( #4562, #9172, #4404, #11636, #29525, #14427 ),
 ( #29189, #26726, #1937, #11955, #31979, #6549 ) ),
 .UNSPECIFIED., .F., .F., .F.,
 ( 4, 2, 4 ),
 ( 4, 2, 4 ),
 ( 0.000000000000000000, 0.5000000000000000000, 1.000000000000000000 ),
 ( 0.000000000000000000, 0.5000000000000000000, 1.000000000000000000 ),
 .UNSPECIFIED. ) ;
#12199=CARTESIAN_POINT ( 'NONE',  ( 49.77860763202481564, 24.96454579807170404, 45.68180464904889959 ) ) ;
#12241=EDGE_CURVE ( 'NONE', #29156, #5398, #25147, .T. ) ;
#12250=LINE ( 'NONE', #12415, #176 ) ;
#12252=ORIENTED_EDGE ( 'NONE', *, *, #31675, .T. ) ;
#12268=DIRECTION ( 'NONE',  ( 1.234978253042719660E-16, -1.000000000000000000, -1.109335647967047851E-31 ) ) ;
#12274=PLANE ( 'NONE',  #32114 ) ;
#12282=CARTESIAN_POINT ( 'NONE',  ( 47.20547626766766314, 28.18791119454915162, 44.97710074790751378 ) ) ;
#12286=CARTESIAN_POINT ( 'NONE',  ( 47.13718051761725292, 29.59454644216853936, 44.97967791668052229 ) ) ;
#12306=CARTESIAN_POINT ( 'NONE',  ( 48.83862994770794330, 25.85457786121582302, 48.17861352429476796 ) ) ;
#12307=VERTEX_POINT ( 'NONE', #30403 ) ;
#12312=ADVANCED_FACE ( 'NONE', ( #25313 ), #24118, .T. ) ;
#12320=CARTESIAN_POINT ( 'NONE',  ( 46.99023568444673060, 29.23791119454914877, 49.12151524109405898 ) ) ;
#12326=B_SPLINE_CURVE_WITH_KNOTS ( 'NONE', 3,
 ( #19181, #11821, #29209, #6722, #1798, #20491 ),
 .UNSPECIFIED., .F., .F.,
 ( 4, 2, 4 ),
 ( 0.000000000000000000, 0.5000000000000000000, 1.000000000000000000 ),
 .UNSPECIFIED. ) ;
#12329=CARTESIAN_POINT ( 'NONE',  ( 48.18662509608405031, 29.38284706826092574, 49.18364984542562013 ) ) ;
#12333=CARTESIAN_POINT ( 'NONE',  ( 45.73035263060504718, 26.53954579807170688, 44.36855633853329550 ) ) ;
#12355=DIRECTION ( 'NONE',  ( 0.05186525298100497228, 2.168404344971009115E-16, -0.9986540920324796788 ) ) ;
#12356=EDGE_CURVE ( 'NONE', #18631, #15214, #19951, .T. ) ;
#12361=EDGE_CURVE ( 'NONE', #25372, #21089, #3058, .T. ) ;
#12363=ORIENTED_EDGE ( 'NONE', *, *, #22531, .T. ) ;
#12378=CARTESIAN_POINT ( 'NONE',  ( 48.83862994770794330, 29.44118040159425931, 48.17861352429476796 ) ) ;
#12382=CARTESIAN_POINT ( 'NONE',  ( 45.73517587035135534, 29.24587785034128373, 45.04535568177062288 ) ) ;
#12400=EDGE_CURVE ( 'NONE', #26705, #26305, #12093, .T. ) ;
#12415=CARTESIAN_POINT ( 'NONE',  ( 46.27249149607015966, 23.24793988701932079, 46.54352925064344504 ) ) ;
#12424=AXIS2_PLACEMENT_3D ( 'NONE', #16942, #19732, #14665 ) ;
#12431=CARTESIAN_POINT ( 'NONE',  ( 44.79156314060809763, 22.86454579224779948, 46.92953032342012420 ) ) ;
#12445=CARTESIAN_POINT ( 'NONE',  ( 44.70507715278255745, 26.96291119454915730, 46.92503878583765697 ) ) ;
#12467=CARTESIAN_POINT ( 'NONE',  ( 46.81682104422132085, 23.12036939723557083, 47.03471240234085116 ) ) ;
#12473=CARTESIAN_POINT ( 'NONE',  ( 45.24946171279598417, 24.92124452788249300, 47.99220971130007030 ) ) ;
#12488=ORIENTED_EDGE ( 'NONE', *, *, #32399, .T. ) ;
#12490=B_SPLINE_CURVE_WITH_KNOTS ( 'NONE', 3,
 ( #10381, #205, #12528, #25477, #4972, #7927, #17758, #17599, #5615, #27611, #15144, #10223, #20546, #3136, #24992, #20221 ),
 .UNSPECIFIED., .F., .F.,
 ( 4, 2, 2, 2, 2, 2, 2, 4 ),
 ( 0.000000000000000000, 0.0002419933622418494166, 0.0004839867244836988333, 0.0009679734489673894266, 0.001451960173451080074, 0.001935946897934770830, 0.002903920346902169689, 0.003871893795869568982 ),
 .UNSPECIFIED. ) ;
#12495=CARTESIAN_POINT ( 'NONE',  ( 45.24946171279598417, 28.50784706826092929, 47.99220971130007030 ) ) ;
#12499=CARTESIAN_POINT ( 'NONE',  ( 48.35473289974373756, 19.96454579224779380, 45.11188864597615833 ) ) ;
#12512=CARTESIAN_POINT ( 'NONE',  ( 49.32483701613094240, 27.82587066347689486, 45.91328182968236860 ) ) ;
#12516=CARTESIAN_POINT ( 'NONE',  ( 44.21498992391907024, 27.29488759933318676, 46.89958605635244027 ) ) ;
#12518=CARTESIAN_POINT ( 'NONE',  ( 47.63716429968715005, 27.61960992152947725, 49.58068632438585155 ) ) ;
#12528=CARTESIAN_POINT ( 'NONE',  ( 49.59575279743435772, 24.95410501111153323, 46.37542181765395100 ) ) ;
#12539=CARTESIAN_POINT ( 'NONE',  ( 45.24946171279598417, 27.80784706826093000, 47.99220971130007030 ) ) ;
#12544=VERTEX_POINT ( 'NONE', #22070 ) ;
#12609=CARTESIAN_POINT ( 'NONE',  ( 48.79601671567883159, 22.86454579224779948, 48.10649398831456125 ) ) ;
#12610=CARTESIAN_POINT ( 'NONE',  ( 47.73724253767792192, 22.99884124225578219, 48.30271392650413276 ) ) ;
#12612=CARTESIAN_POINT ( 'NONE',  ( 48.94625023931840957, 27.37124452788248874, 46.10640627770150246 ) ) ;
#12617=CARTESIAN_POINT ( 'NONE',  ( 47.17209261226641104, 29.58954579224849368, 44.97563639035409011 ) ) ;
#12637=( BOUNDED_CURVE ( )  B_SPLINE_CURVE ( 2, ( #4099, #3949, #23959, #1476, #14125 ),
 .UNSPECIFIED., .F., .F. ) 
 B_SPLINE_CURVE_WITH_KNOTS ( ( 3, 2, 3 ),
 ( 0.08390304798631194327, 0.09523809523809523281, 0.1071428583041297289 ),
 .UNSPECIFIED. ) 
 CURVE ( )  GEOMETRIC_REPRESENTATION_ITEM ( )  RATIONAL_B_SPLINE_CURVE ( ( 0.9331661161814950312, 0.9362184480970371370, 1.000000000000000000, 0.9330126953578162796, 0.9330127018922200755 ) ) 
 REPRESENTATION_ITEM ( '' )  );
#12641=CARTESIAN_POINT ( 'NONE',  ( 48.37829923888483563, 28.85122849631042286, 45.07556196625585443 ) ) ;
#12663=CARTESIAN_POINT ( 'NONE',  ( 46.99023568444673060, 29.32451373492759217, 49.12151524109405898 ) ) ;
#12667=AXIS2_PLACEMENT_3D ( 'NONE', #17791, #723, #27816 ) ;
#12676=CARTESIAN_POINT ( 'NONE',  ( 48.94625023931840957, 27.45784706826093213, 46.10640627770150246 ) ) ;
#12686=EDGE_CURVE ( 'NONE', #28026, #20793, #31891, .T. ) ;
#12690=CARTESIAN_POINT ( 'NONE',  ( 45.37383841111020644, 22.88065857334295217, 47.92876263475718446 ) ) ;
#12711=CARTESIAN_POINT ( 'NONE',  ( 46.00908685603034343, 27.63284706826092929, 44.91496614357595263 ) ) ;
#12739=ADVANCED_FACE ( 'NONE', ( #29262 ), #8750, .T. ) ;
#12777=CARTESIAN_POINT ( 'NONE',  ( 45.35708200440645044, 29.70457786121581378, 45.92000246470679770 ) ) ;
#12797=CARTESIAN_POINT ( 'NONE',  ( 45.63968093275011029, 22.91413368675619111, 48.10984057092807831 ) ) ;
#12802=CARTESIAN_POINT ( 'NONE',  ( 48.18662509608405031, 26.49624452788248874, 49.18364984542562013 ) ) ;
#12806=EDGE_LOOP ( 'NONE', ( #4283, #20838, #10030, #15795 ) ) ;
#12815=PRODUCT_CONTEXT ( 'NONE', #22499, 'mechanical' ) ;
#12821=CARTESIAN_POINT ( 'NONE',  ( 45.24946171279598417, 27.80784706826093000, 47.99220971130007740 ) ) ;
#12835=CARTESIAN_POINT ( 'NONE',  ( 46.00908685603034343, 26.93284706826093000, 44.91496614357595263 ) ) ;
#12836=EDGE_CURVE ( 'NONE', #30606, #25372, #454, .T. ) ;
#12841=CARTESIAN_POINT ( 'NONE',  ( 44.21498992391908445, 26.01753733014356129, 46.89958605635242606 ) ) ;
#12843=CARTESIAN_POINT ( 'NONE',  ( 49.70056603649367588, 24.90621246473837047, 47.18448000306445067 ) ) ;
#12848=CARTESIAN_POINT ( 'NONE',  ( 49.28428300279882990, 29.04787913140503974, 48.46772541801551171 ) ) ;
#12850=ORIENTED_EDGE ( 'NONE', *, *, #23977, .F. ) ;
#12865=CARTESIAN_POINT ( 'NONE',  ( 45.79384627280941089, 25.76618040159426570, 49.05938063676249072 ) ) ;
#12868=CARTESIAN_POINT ( 'NONE',  ( 48.40186567930498285, 28.82957786121581378, 45.03923535223908203 ) ) ;
#12879=ADVANCED_FACE ( 'NONE', ( #29757 ), #29819, .T. ) ;
#12895=CARTESIAN_POINT ( 'NONE',  ( 44.79156314060809763, 22.86454579224779948, 46.92953032342012420 ) ) ;
#12908=CARTESIAN_POINT ( 'NONE',  ( 48.85960306834331135, 19.86454579224779948, 48.19221970711091529 ) ) ;
#12931=CARTESIAN_POINT ( 'NONE',  ( 47.58479084802739578, 23.04411657098542676, 46.02349645909773557 ) ) ;
#12932=DIRECTION ( 'NONE',  ( -4.793929595204190462E-17, -1.000000000000000000, -3.360725575046568817E-16 ) ) ;
#12933=CARTESIAN_POINT ( 'NONE',  ( 45.90820269358763994, 22.93328494799376571, 48.28896993515231628 ) ) ;
#12936=CARTESIAN_POINT ( 'NONE',  ( 45.79384627280941089, 27.77957786121582018, 49.05938063676249072 ) ) ;
#12961=CARTESIAN_POINT ( 'NONE',  ( 48.16694854572211426, 27.21789516297709355, 49.14507740233662503 ) ) ;
#12992=CARTESIAN_POINT ( 'NONE',  ( 48.79980305660560447, 22.93328494799376571, 46.81390877062097644 ) ) ;
#13001=AXIS2_PLACEMENT_3D ( 'NONE', #4173, #14201, #6803 ) ;
#13015=CARTESIAN_POINT ( 'NONE',  ( 47.65993751833249092, 23.10527845304106620, 47.07849978535075053 ) ) ;
#13017=ORIENTED_EDGE ( 'NONE', *, *, #22571, .F. ) ;
#13019=CARTESIAN_POINT ( 'NONE',  ( 48.18662509608405031, 26.58284706826093213, 49.18364984542562013 ) ) ;
#13023=CARTESIAN_POINT ( 'NONE',  ( 48.94625023931840246, 28.07124452788248803, 46.10640627770150246 ) ) ;
#13027=( BOUNDED_CURVE ( )  B_SPLINE_CURVE ( 2, ( #31442, #29421, #12843, #35, #194 ),
 .UNSPECIFIED., .F., .F. ) 
 B_SPLINE_CURVE_WITH_KNOTS ( ( 3, 2, 3 ),
 ( 0.7921717258529592520, 0.8333333333333329263, 1.000000000000000000 ),
 .UNSPECIFIED. ) 
 CURVE ( )  GEOMETRIC_REPRESENTATION_ITEM ( )  RATIONAL_B_SPLINE_CURVE ( ( 0.9501679776138609590, 0.9669123415494011997, 1.000000000000000000, 0.8660254037844387076, 1.000000000000000000 ) ) 
 REPRESENTATION_ITEM ( '' )  );
#13047=DIRECTION ( 'NONE',  ( 0.4544104193609903586, 0.000000000000000000, 0.8907924397839088737 ) ) ;
#13058=FACE_OUTER_BOUND ( 'NONE', #23230, .T. ) ;
#13067=VERTEX_POINT ( 'NONE', #21332 ) ;
#13074=ADVANCED_FACE ( 'NONE', ( #19198 ), #26438, .F. ) ;
#13118=CARTESIAN_POINT ( 'NONE',  ( 48.72149481846882679, 22.88065857334295217, 48.10262368218729279 ) ) ;
#13121=DIRECTION ( 'NONE',  ( 0.4544104193609915243, 0.000000000000000000, 0.8907924397839082076 ) ) ;
#13122=CARTESIAN_POINT ( 'NONE',  ( 46.02876340639226527, 27.56789516297709497, 44.95353858666495483 ) ) ;
#13166=CARTESIAN_POINT ( 'NONE',  ( 48.99461295342375422, 29.56774068890345930, 46.14022547996226820 ) ) ;
#13171=CARTESIAN_POINT ( 'NONE',  ( 44.09250526802607340, 29.45621246473837118, 46.89322480343881949 ) ) ;
#13173=( LENGTH_UNIT ( ) NAMED_UNIT ( * ) SI_UNIT ( .MILLI., .METRE. ) );
#13188=ORIENTED_EDGE ( 'NONE', *, *, #21958, .T. ) ;
#13191=CARTESIAN_POINT ( 'NONE',  ( 46.99023568444673060, 27.22451373492759785, 49.12151524109405898 ) ) ;
#13193=CARTESIAN_POINT ( 'NONE',  ( 44.70507715278255745, 27.66291119454915304, 46.92503878583764987 ) ) ;
#13201=ORIENTED_EDGE ( 'NONE', *, *, #6901, .F. ) ;
#13224=CARTESIAN_POINT ( 'NONE',  ( 47.16621377848951369, 29.60751587792711348, 44.99339554510944339 ) ) ;
#13227=ORIENTED_EDGE ( 'NONE', *, *, #13494, .F. ) ;
#13234=CARTESIAN_POINT ( 'NONE',  ( 48.72149481846882679, 22.88065857334295217, 48.10262368218729279 ) ) ;
#13280=AXIS2_PLACEMENT_3D ( 'NONE', #10676, #23610, #20661 ) ;
#13287=CARTESIAN_POINT ( 'NONE',  ( 48.39051051835283346, 22.95310733321322516, 48.05892087412300384 ) ) ;
#13292=CARTESIAN_POINT ( 'NONE',  ( 49.44739180854976013, 28.03456182964376708, 47.17133137409169308 ) ) ;
#13314=AXIS2_PLACEMENT_3D ( 'NONE', #10472, #17844, #27375 ) ;
#13345=CARTESIAN_POINT ( 'NONE',  ( 46.96268396749378127, 29.63121246473836834, 49.65201805493727960 ) ) ;
#13346=CARTESIAN_POINT ( 'NONE',  ( 46.99023568444673060, 27.83791119454915375, 49.12151524109405898 ) ) ;
#13371=CARTESIAN_POINT ( 'NONE',  ( 46.69388217747229675, 23.10527865767145173, 46.62354503484363022 ) ) ;
#13392=VERTEX_POINT ( 'NONE', #3272 ) ;
#13413=CARTESIAN_POINT ( 'NONE',  ( 45.84510715990803220, 22.84434098701873594, 45.30553951807763013 ) ) ;
#13419=CARTESIAN_POINT ( 'NONE',  ( 46.99023568444673060, 25.03791119454916014, 49.12151524109405898 ) ) ;
#13442=CARTESIAN_POINT ( 'NONE',  ( 47.50182977464208989, 23.10527865767145173, 47.47507095415797096 ) ) ;
#13445=CARTESIAN_POINT ( 'NONE',  ( 48.91284552371730143, 25.99289516297709923, 46.12344667017377020 ) ) ;
#13447=ORIENTED_EDGE ( 'NONE', *, *, #24187, .T. ) ;
#13453=DIRECTION ( 'NONE',  ( 1.234978253042719660E-16, -1.000000000000000000, -1.109335647967047851E-31 ) ) ;
#13462=CARTESIAN_POINT ( 'NONE',  ( 48.83059991212272166, 25.45948167178348953, 48.97189174113093912 ) ) ;
#13486=CARTESIAN_POINT ( 'NONE',  ( 47.41252533345003428, 29.19474943853624183, 44.59074167925342635 ) ) ;
#13494=EDGE_CURVE ( 'NONE', #11279, #24034, #17208, .T. ) ;
#13502=CARTESIAN_POINT ( 'NONE',  ( 45.73035263060504718, 27.23954579807170262, 44.36855633853329550 ) ) ;
#13521=CARTESIAN_POINT ( 'NONE',  ( 44.21498992391908445, 25.31753733014356555, 46.89958605635242606 ) ) ;
#13523=CARTESIAN_POINT ( 'NONE',  ( 47.16432553341419975, 22.86454579224779948, 45.05006465737218235 ) ) ;
#13525=CARTESIAN_POINT ( 'NONE',  ( 48.94625023931840246, 29.47124452788248306, 46.10640627770150246 ) ) ;
#13542=VERTEX_POINT ( 'NONE', #14428 ) ;
#13559=ADVANCED_FACE ( 'NONE', ( #1782 ), #26727, .F. ) ;
#13593=CARTESIAN_POINT ( 'NONE',  ( 47.22573328838134188, 23.12036939723557083, 47.29998918090146987 ) ) ;
#13594=CARTESIAN_POINT ( 'NONE',  ( 46.99747725352182925, 22.88065857334294861, 48.98207832244369087 ) ) ;
#13596=CARTESIAN_POINT ( 'NONE',  ( 48.80717017713595141, 25.17622849631044346, 48.15820438821415195 ) ) ;
#13641=VECTOR ( 'NONE', #26624, 999.9999999999998863 ) ;
#13647=CARTESIAN_POINT ( 'NONE',  ( 46.78253665710180087, 29.21161237798985866, 44.60769444413243434 ) ) ;
#13663=CARTESIAN_POINT ( 'NONE',  ( 44.77625694075214824, 27.41454579807170688, 48.23360063142255427 ) ) ;
#13669=EDGE_CURVE ( 'NONE', #7056, #16020, #23741, .T. ) ;
#13686=( BOUNDED_CURVE ( )  B_SPLINE_CURVE ( 2, ( #9701, #7236, #2793, #4937, #22811, #12329, #12663, #27583, #15271, #22324, #24791, #17231, #17401, #15109, #2634, #27743, #15427, #10346, #27246, #32350, #12495, #25119, #22650, #27908, #9861, #10190, #17721, #19860, #20187, #29890, #5261, #25286, #12821, #27421, #325, #20341, #30370, #7889, #32189, #5426, #14953, #25440, #24959, #12164, #22160, #2473, #28704, #6224, #10995, #30856, #18198, #30538, #972, #22964, #815, #3273, #28070, #1131, #5582, #15580, #28230, #31018, #15912, #16066, #8363, #484, #25918, #3099, #28391, #8209, #28556, #23461, #10840, #20673, #11158, #30700, #18681, #654, #20990 ),
 .UNSPECIFIED., .F., .F. ) 
 B_SPLINE_CURVE_WITH_KNOTS ( ( 3, 2, 2, 2, 2, 2, 2, 2, 2, 2, 2, 2, 2, 2, 2, 2, 2, 2, 2, 2, 2, 2, 2, 2, 2, 2, 2, 2, 2, 2, 2, 2, 2, 2, 2, 2, 2, 2, 2, 3 ),
 ( 0.06466318693218657543, 0.07142857142857142461, 0.09523809523809523281, 0.1190476190476190410, 0.1428571428571428492, 0.1666666666666666574, 0.1904761904761904656, 0.2142857142857143016, 0.2380952380952380820, 0.2619047619047619180, 0.2857142857142856984, 0.3095238095238095344, 0.3333333333333333148, 0.3571428571428571508, 0.3809523809523809312, 0.4047619047619047672, 0.4285714285714285476, 0.4523809523809523836, 0.4761904761904761640, 0.5000000000000000000, 0.5238095238095238360, 0.5476190476190476719, 0.5714285714285713969, 0.5952380952380952328, 0.6190476190476190688, 0.6428571428571429047, 0.6666666666666666297, 0.6904761904761904656, 0.7142857142857143016, 0.7380952380952381375, 0.7619047619047618625, 0.7857142857142856984, 0.8095238095238095344, 0.8333333333333333703, 0.8571428571428570953, 0.8809523809523809312, 0.9047619047619047672, 0.9285714285714287142, 0.9523809523809523281, 0.9642857142857166330 ),
 .UNSPECIFIED. ) 
 CURVE ( )  GEOMETRIC_REPRESENTATION_ITEM ( )  RATIONAL_B_SPLINE_CURVE ( ( 0.9454972278162998567, 0.9619316344418604725, 1.000000000000000000, 0.8660254037844387076, 1.000000000000000000, 0.8660254037844387076, 1.000000000000000000, 0.8660254037844387076, 1.000000000000000000, 0.8660254037844387076, 1.000000000000000000, 0.8660254037844387076, 1.000000000000000000, 0.8660254037844387076, 1.000000000000000000, 0.8660254037844387076, 1.000000000000000000, 0.8660254037844387076, 1.000000000000000000, 0.8660254037844387076, 1.000000000000000000, 0.8660254037844387076, 1.000000000000000000, 0.8660254037844387076, 1.000000000000000000, 0.8660254037844387076, 1.000000000000000000, 0.8660254037844387076, 1.000000000000000000, 0.8660254037844387076, 1.000000000000000000, 0.8660254037844387076, 1.000000000000000000, 0.8660254037844387076, 1.000000000000000000, 0.8660254037844387076, 1.000000000000000000, 0.8660254037844387076, 1.000000000000000000, 0.8660254037844387076, 1.000000000000000000, 0.8660254037844387076, 1.000000000000000000, 0.8660254037844387076, 1.000000000000000000, 0.8660254037844387076, 1.000000000000000000, 0.8660254037844387076, 1.000000000000000000, 0.8660254037844387076, 1.000000000000000000, 0.8660254037844387076, 1.000000000000000000, 0.8660254037844387076, 1.000000000000000000, 0.8660254037844387076, 1.000000000000000000, 0.8660254037844387076, 1.000000000000000000, 0.8660254037844387076, 1.000000000000000000, 0.8660254037844387076, 1.000000000000000000, 0.8660254037844387076, 1.000000000000000000, 0.8660254037844387076, 1.000000000000000000, 0.8660254037844387076, 1.000000000000000000, 0.8660254037844387076, 1.000000000000000000, 0.8660254037844387076, 1.000000000000000000, 0.8660254037844387076, 1.000000000000000000, 0.8660254037844387076, 1.000000000000000000, 0.9330127018922058646, 0.9330127018922192983 ) ) 
 REPRESENTATION_ITEM ( '' )  );
#13690=CARTESIAN_POINT ( 'NONE',  ( 48.18662509608405742, 27.89624452788248377, 49.18364984542562013 ) ) ;
#13697=CARTESIAN_POINT ( 'NONE',  ( 46.45846941443645761, 22.99884124225578930, 45.79590206249746132 ) ) ;
#13719=VERTEX_POINT ( 'NONE', #738 ) ;
#13730=CARTESIAN_POINT ( 'NONE',  ( 45.44030796846719511, 22.86454579224779948, 45.92951929762858043 ) ) ;
#13736=CARTESIAN_POINT ( 'NONE',  ( 44.70507715278255745, 25.56291119454915517, 46.92503878583764987 ) ) ;
#13738=CARTESIAN_POINT ( 'NONE',  ( 45.00053793792376666, 28.63655426599985176, 45.68869892245983522 ) ) ;
#13741=DIRECTION ( 'NONE',  ( -0.4441739386571981751, 0.2110602665713104675, -0.8707256032141232893 ) ) ;
#13746=UNCERTAINTY_MEASURE_WITH_UNIT (LENGTH_MEASURE( 1.000000000000000082E-05 ), #18023, 'distance_accuracy_value', 'NONE');
#13762=CARTESIAN_POINT ( 'NONE',  ( 48.91284552371730143, 29.53619643316630672, 46.12344667017377020 ) ) ;
#13767=CARTESIAN_POINT ( 'NONE',  ( 48.38152489017220148, 29.46964073901252590, 48.83753094390939253 ) ) ;
#13777=PLANE ( 'NONE',  #27151 ) ;
#13779=CARTESIAN_POINT ( 'NONE',  ( 47.71045395478045492, 23.04411619146718238, 46.10501571378621577 ) ) ;
#13803=CARTESIAN_POINT ( 'NONE',  ( 48.35473289974373756, 22.86454579224779948, 45.11188864597615833 ) ) ;
#13822=CARTESIAN_POINT ( 'NONE',  ( 46.99023568444673060, 25.12451373492760354, 49.12151524109405898 ) ) ;
#13832=CARTESIAN_POINT ( 'NONE',  ( 45.81741271322955100, 25.04452976649966089, 49.02305402274571122 ) ) ;
#13845=CARTESIAN_POINT ( 'NONE',  ( 48.83862994770794330, 27.25457786121581805, 48.17861352429476796 ) ) ;
#13869=( BOUNDED_CURVE ( )  B_SPLINE_CURVE ( 2, ( #7250, #2482, #5108 ),
 .UNSPECIFIED., .F., .T. ) 
 B_SPLINE_CURVE_WITH_KNOTS ( ( 3, 3 ),
 ( 0.7892923757256058437, 0.7921717258529592520 ),
 .UNSPECIFIED. ) 
 CURVE ( )  GEOMETRIC_REPRESENTATION_ITEM ( )  RATIONAL_B_SPLINE_CURVE ( ( 0.9479053363475489213, 0.9489966704326912028, 0.9501679776138607370 ) ) 
 REPRESENTATION_ITEM ( '' )  );
#13872=LINE ( 'NONE', #30955, #17161 ) ;
#13885=CYLINDRICAL_SURFACE ( 'NONE', #17574, 7.999999999999996447 ) ;
#13888=CARTESIAN_POINT ( 'NONE',  ( 45.42945060211348363, 22.93328494799376216, 46.63886900051237916 ) ) ;
#13890=CARTESIAN_POINT ( 'NONE',  ( 47.33512057650604277, 22.89977464660286444, 45.20042056806582309 ) ) ;
#13900=CARTESIAN_POINT ( 'NONE',  ( 47.09785597605719687, 15.77906836436399374, 47.04930799450078638 ) ) ;
#13902=DIRECTION ( 'NONE',  ( -0.3935310072385434510, 0.5000000000000004441, -0.7714488617801033010 ) ) ;
#13904=VECTOR ( 'NONE', #30191, 1000.000000000000000 ) ;
#13909=EDGE_CURVE ( 'NONE', #21141, #5136, #6629, .T. ) ;
#13915=ORIENTED_EDGE ( 'NONE', *, *, #6962, .T. ) ;
#13921=CARTESIAN_POINT ( 'NONE',  ( 44.74832014356462651, 29.12786309983297883, 46.92728461490987257 ) ) ;
#13928=CARTESIAN_POINT ( 'NONE',  ( 49.13594796351935656, 29.51161737861004397, 47.76250447815154843 ) ) ;
#13933=CARTESIAN_POINT ( 'NONE',  ( 45.46000861347822308, 27.47287913140504045, 49.57397645940629616 ) ) ;
#13941=CARTESIAN_POINT ( 'NONE',  ( 47.37889090789306579, 23.12036939723557083, 47.06390358666074292 ) ) ;
#13943=EDGE_LOOP ( 'NONE', ( #8685, #16111, #28149, #13949 ) ) ;
#13949=ORIENTED_EDGE ( 'NONE', *, *, #30504, .F. ) ;
#13973=ORIENTED_EDGE ( 'NONE', *, *, #14063, .T. ) ;
#13983=CARTESIAN_POINT ( 'NONE',  ( 46.96268396749378127, 27.53121246473837402, 49.65201805493727960 ) ) ;
#13995=CARTESIAN_POINT ( 'NONE',  ( 45.24946171279598417, 28.50784706826092929, 47.99220971130007030 ) ) ;
#14007=CARTESIAN_POINT ( 'NONE',  ( 44.70507715278255034, 27.66291119454915304, 46.92503878583765697 ) ) ;
#14037=ORIENTED_EDGE ( 'NONE', *, *, #396, .F. ) ;
#14048=CARTESIAN_POINT ( 'NONE',  ( 46.33059210211230550, 22.93807716476589675, 45.54522087609679204 ) ) ;
#14063=EDGE_CURVE ( 'NONE', #5136, #17834, #60, .T. ) ;
#14067=ORIENTED_EDGE ( 'NONE', *, *, #13909, .T. ) ;
#14068=( BOUNDED_CURVE ( )  B_SPLINE_CURVE ( 2, ( #29251, #28940, #16451, #24165, #16771, #8745, #11065, #11705, #11372 ),
 .UNSPECIFIED., .F., .F. ) 
 B_SPLINE_CURVE_WITH_KNOTS ( ( 3, 2, 2, 2, 3 ),
 ( 0.5357142845530131758, 0.5476190476190476719, 0.5714285714285713969, 0.5952380952380952328, 0.6071428559815844617 ),
 .UNSPECIFIED. ) 
 CURVE ( )  GEOMETRIC_REPRESENTATION_ITEM ( )  RATIONAL_B_SPLINE_CURVE ( ( 0.9330127018922200755, 0.9330126953578163906, 1.000000000000000000, 0.8660254037844387076, 1.000000000000000000, 0.8660254037844387076, 1.000000000000000000, 0.9330127084266230941, 0.9330127018922200755 ) ) 
 REPRESENTATION_ITEM ( '' )  );
#14073=ADVANCED_FACE ( 'NONE', ( #27953 ), #24595, .T. ) ;
#14079=CARTESIAN_POINT ( 'NONE',  ( 46.99218062947583974, 26.50286309983298949, 49.08406571254116102 ) ) ;
#14082=DIRECTION ( 'NONE',  ( -0.01254734031692028573, 0.9702957262759968060, 0.2415962909928611735 ) ) ;
#14092=CARTESIAN_POINT ( 'NONE',  ( 44.09250526802607340, 25.95621246473837829, 46.89322480343881949 ) ) ;
#14094=CARTESIAN_POINT ( 'NONE',  ( 47.09785597605719687, 23.12036939723557083, 47.04930799450080059 ) ) ;
#14102=CARTESIAN_POINT ( 'NONE',  ( 46.55854765242722237, 25.74696019071911124, 44.51792966461573542 ) ) ;
#14122=EDGE_CURVE ( 'NONE', #13542, #17767, #27095, .T. ) ;
#14125=CARTESIAN_POINT ( 'NONE',  ( 48.23388202445966044, 29.05087065737811969, 49.27628909396056400 ) ) ;
#14136=CARTESIAN_POINT ( 'NONE',  ( 47.09785597605719687, 29.86454579224779948, 47.04930799450078638 ) ) ;
#14152=CARTESIAN_POINT ( 'NONE',  ( 49.49063479933183629, 28.79951373492759359, 47.17357720316391578 ) ) ;
#14161=DIRECTION ( 'NONE',  ( -0.9986540920324801229, -6.158269594508763597E-17, -0.05186525298099629866 ) ) ;
#14169=CARTESIAN_POINT ( 'NONE',  ( 46.96819297411687444, 25.49253733014356271, 49.54594323136014822 ) ) ;
#14174=CARTESIAN_POINT ( 'NONE',  ( 46.48089935138444417, 23.09557481883486929, 46.64906498822688974 ) ) ;
#14175=CARTESIAN_POINT ( 'NONE',  ( 45.84822719475717889, 25.05653309617948210, 44.59962885041953484 ) ) ;
#14177=CARTESIAN_POINT ( 'NONE',  ( 47.09785597605719687, 15.77906836436399374, 47.04930799450078638 ) ) ;
#14180=CARTESIAN_POINT ( 'NONE',  ( 46.84209603737756566, 23.10527845304106620, 46.54793520446708044 ) ) ;
#14183=CARTESIAN_POINT ( 'NONE',  ( 47.91579473090698116, 29.86454579224779948, 48.65273438611181689 ) ) ;
#14201=DIRECTION ( 'NONE',  ( 0.8907924160295465077, 1.100109261771873178E-16, -0.4544104659272754643 ) ) ;
#14222=CARTESIAN_POINT ( 'NONE',  ( 48.14727188781975542, 19.96454579224779380, 49.10650501410607660 ) ) ;
#14224=CARTESIAN_POINT ( 'NONE',  ( 45.41164638504195494, 22.93807716476589675, 46.96173444154113241 ) ) ;
#14228=EDGE_CURVE ( 'NONE', #5398, #12307, #5624, .T. ) ;
#14229=ORIENTED_EDGE ( 'NONE', *, *, #31061, .F. ) ;
#14238=EDGE_LOOP ( 'NONE', ( #19993, #11960, #26546, #6270, #9300, #14259 ) ) ;
#14243=CARTESIAN_POINT ( 'NONE',  ( 45.81741271322955100, 26.44452976649965237, 49.02305402274571122 ) ) ;
#14251=CARTESIAN_POINT ( 'NONE',  ( 48.59475124299144966, 29.58954579224780090, 45.61232171765963272 ) ) ;
#14256=CARTESIAN_POINT ( 'NONE',  ( 45.73035263060504718, 27.93954579807170546, 44.36855633853329550 ) ) ;
#14257=CARTESIAN_POINT ( 'NONE',  ( 47.15639191806693020, 22.95310733321322161, 48.68846859551268835 ) ) ;
#14258=CARTESIAN_POINT ( 'NONE',  ( 47.09785597605719687, 15.77906836436399374, 47.04930799450078638 ) ) ;
#14259=ORIENTED_EDGE ( 'NONE', *, *, #23303, .T. ) ;
#14275=ORIENTED_EDGE ( 'NONE', *, *, #6228, .F. ) ;
#14279=CARTESIAN_POINT ( 'NONE',  ( 47.98162936688354563, 22.84434098701873239, 45.09251145694314289 ) ) ;
#14307=CARTESIAN_POINT ( 'NONE',  ( 48.73570333863616355, 25.72287913140504756, 44.52463952959527660 ) ) ;
#14311=ORIENTED_EDGE ( 'NONE', *, *, #1026, .F. ) ;
#14313=LINE ( 'NONE', #11689, #30275 ) ;
#14316=CARTESIAN_POINT ( 'NONE',  ( 49.44739180854976013, 25.97786309983299091, 47.17133137409169308 ) ) ;
#14317=ORIENTED_EDGE ( 'NONE', *, *, #6405, .T. ) ;
#14333=CARTESIAN_POINT ( 'NONE',  ( 45.80520143376154607, 22.95310733321322161, 46.03969511487858313 ) ) ;
#14398=VERTEX_POINT ( 'NONE', #11655 ) ;
#14400=CARTESIAN_POINT ( 'NONE',  ( 47.40417757965286683, 23.10527845304106620, 46.57712699531703038 ) ) ;
#14401=DIRECTION ( 'NONE',  ( -0.4544104193609807552, 0.000000000000000000, -0.8907924397839137587 ) ) ;
#14402=CARTESIAN_POINT ( 'NONE',  ( 45.38854177497844944, 27.66952976649964668, 45.94041160078741370 ) ) ;
#14406=CARTESIAN_POINT ( 'NONE',  ( 48.14727188781972700, 22.86454579224779948, 49.10650501410609081 ) ) ;
#14413=CARTESIAN_POINT ( 'NONE',  ( 47.23302798462060537, 26.48121246473837687, 44.44659793406428605 ) ) ;
#14427=CARTESIAN_POINT ( 'NONE',  ( 48.81767175631193112, 22.89977464660286444, 46.33034145269077442 ) ) ;
#14428=CARTESIAN_POINT ( 'NONE',  ( 45.96182992765472619, 28.00087065737811898, 44.82232689504102296 ) ) ;
#14433=B_SPLINE_CURVE_WITH_KNOTS ( 'NONE', 3,
 ( #6329, #16331, #13888, #23887, #1398, #11412 ),
 .UNSPECIFIED., .F., .F.,
 ( 4, 2, 4 ),
 ( 0.000000000000000000, 0.5000000000000000000, 1.000000000000000000 ),
 .UNSPECIFIED. ) ;
#14436=VECTOR ( 'NONE', #12145, 999.9999999999998863 ) ;
#14481=CARTESIAN_POINT ( 'NONE',  ( 48.91284552371730143, 26.03619643316632448, 46.12344667017377020 ) ) ;
#14489=EDGE_CURVE ( 'NONE', #306, #9336, #30474, .T. ) ;
#14490=CARTESIAN_POINT ( 'NONE',  ( 48.14727188781975542, 22.86454579224779948, 49.10650501410607660 ) ) ;
#14496=CARTESIAN_POINT ( 'NONE',  ( 45.95383497628772318, 23.03451764446790051, 46.65777585308548225 ) ) ;
#14497=CARTESIAN_POINT ( 'NONE',  ( 48.51627339957213536, 25.02287913140503761, 44.86288096775929546 ) ) ;
#14570=DIRECTION ( 'NONE',  ( -0.5932111027100930301, 0.7071067811865471286, -0.3848383915638822761 ) ) ;
#14574=CARTESIAN_POINT ( 'NONE',  ( 50.10320668408830613, 26.30621246473837616, 47.20539118556276037 ) ) ;
#14575=EDGE_CURVE ( 'NONE', #14642, #24034, #13872, .T. ) ;
#14576=CARTESIAN_POINT ( 'NONE',  ( 47.35361591473682097, 23.10527845304106265, 47.55068078453451363 ) ) ;
#14579=EDGE_LOOP ( 'NONE', ( #14067, #13973, #28082 ) ) ;
#14580=CARTESIAN_POINT ( 'NONE',  ( 47.13083292863866802, 29.59604743734263010, 44.98107144923852019 ) ) ;
#14582=CARTESIAN_POINT ( 'NONE',  ( 47.09785597605719687, 15.77906836436399374, 47.04930799450078638 ) ) ;
#14616=CARTESIAN_POINT ( 'NONE',  ( 44.70507715278255034, 28.36291119454914877, 46.92503878583765697 ) ) ;
#14640=CARTESIAN_POINT ( 'NONE',  ( 44.70507715278255745, 25.64951373492759856, 46.92503878583764987 ) ) ;
#14642=VERTEX_POINT ( 'NONE', #18771 ) ;
#14649=DIRECTION ( 'NONE',  ( 1.234978253042719660E-16, -1.000000000000000000, -1.109335647967047851E-31 ) ) ;
#14659=CARTESIAN_POINT ( 'NONE',  ( 47.26255010802070444, 24.99819976284614853, 43.87815533714887550 ) ) ;
#14665=DIRECTION ( 'NONE',  ( -0.8389271868029088974, 0.000000000000000000, -0.5442436726714948714 ) ) ;
#14675=CARTESIAN_POINT ( 'NONE',  ( 44.81325834503692107, 29.29399940044038786, 46.39891453572019486 ) ) ;
#14699=DIRECTION ( 'NONE',  ( 0.4544104193609903586, 0.000000000000000000, 0.8907924397839087627 ) ) ;
#14700=CARTESIAN_POINT ( 'NONE',  ( 46.04844006429464542, 19.96454579224779380, 44.99211097489548905 ) ) ;
#14719=EDGE_CURVE ( 'NONE', #26434, #22710, #9301, .T. ) ;
#14735=FACE_OUTER_BOUND ( 'NONE', #6045, .T. ) ;
#14740=FACE_OUTER_BOUND ( 'NONE', #20078, .T. ) ;
#14742=CARTESIAN_POINT ( 'NONE',  ( 45.35708200440645044, 26.20457786121582444, 45.92000246470679770 ) ) ;
#14772=CARTESIAN_POINT ( 'NONE',  ( 48.83862994770794330, 25.15457786121582373, 48.17861352429476796 ) ) ;
#14783=CARTESIAN_POINT ( 'NONE',  ( 45.79384627280941089, 28.47957786121581591, 49.05938063676249072 ) ) ;
#14801=ORIENTED_EDGE ( 'NONE', *, *, #10774, .F. ) ;
#14813=DIRECTION ( 'NONE',  ( -0.8907924397839087627, -1.100109291107994187E-16, 0.4544104193609907472 ) ) ;
#14822=ORIENTED_EDGE ( 'NONE', *, *, #19135, .F. ) ;
#14825=CARTESIAN_POINT ( 'NONE',  ( 45.84097905237065618, 22.86454579224779948, 48.98672734302541443 ) ) ;
#14829=CARTESIAN_POINT ( 'NONE',  ( 49.32483701613094240, 27.12587066347689557, 45.91328182968236860 ) ) ;
#14843=CARTESIAN_POINT ( 'NONE',  ( 45.99457799031791438, 29.23661293962803143, 44.88652376508412090 ) ) ;
#14846=VECTOR ( 'NONE', #20294, 1000.000000000000114 ) ;
#14859=EDGE_LOOP ( 'NONE', ( #5880, #3238, #32383, #32333, #14229, #25412 ) ) ;
#14883=CARTESIAN_POINT ( 'NONE',  ( 48.28214861297873028, 24.78954579807170333, 49.37090702980594870 ) ) ;
#14884=VERTEX_POINT ( 'NONE', #18420 ) ;
#14890=FACE_OUTER_BOUND ( 'NONE', #1137, .T. ) ;
#14891=EDGE_CURVE ( 'NONE', #17834, #4178, #30265, .T. ) ;
#14905=CARTESIAN_POINT ( 'NONE',  ( 45.35708200440645044, 27.60457786121581947, 45.92000246470679770 ) ) ;
#14909=CARTESIAN_POINT ( 'NONE',  ( 47.13159012232203082, 29.60361862379404840, 44.98865247363699638 ) ) ;
#14919=AXIS2_PLACEMENT_3D ( 'NONE', #15294, #14649, #14973 ) ;
#14929=CARTESIAN_POINT ( 'NONE',  ( 48.94625023931840957, 26.67124452788248945, 46.10640627770150246 ) ) ;
#14943=EDGE_LOOP ( 'NONE', ( #14317, #21754, #7901, #29595 ) ) ;
#14953=CARTESIAN_POINT ( 'NONE',  ( 48.83862994770794330, 27.34118040159426499, 48.17861352429476796 ) ) ;
#14956=FACE_OUTER_BOUND ( 'NONE', #15567, .T. ) ;
#14961=CIRCLE ( 'NONE', #6565, 3.699999999999994849 ) ;
#14967=CARTESIAN_POINT ( 'NONE',  ( 49.49063479933183629, 25.99951373492759643, 47.17357720316391578 ) ) ;
#14973=DIRECTION ( 'NONE',  ( 0.4544104193609900810, 5.611869858668441979E-17, 0.8907924397839090958 ) ) ;
#14979=DIRECTION ( 'NONE',  ( 0.4441739386571981751, -0.2110602665713104398, 0.8707256032141232893 ) ) ;
#14987=EDGE_CURVE ( 'NONE', #2302, #10357, #31066, .T. ) ;
#15003=CARTESIAN_POINT ( 'NONE',  ( 44.74186670439651436, 29.31291848938220568, 47.00181081234863001 ) ) ;
#15017=ORIENTED_EDGE ( 'NONE', *, *, #25090, .F. ) ;
#15038=ORIENTED_EDGE ( 'NONE', *, *, #26856, .F. ) ;
#15065=CARTESIAN_POINT ( 'NONE',  ( 48.94625023931840246, 28.77124452788248732, 46.10640627770150246 ) ) ;
#15083=CARTESIAN_POINT ( 'NONE',  ( 45.90820269358763994, 22.93328494799376571, 48.28896993515231628 ) ) ;
#15089=CARTESIAN_POINT ( 'NONE',  ( 48.40186567930498285, 27.42957786121582231, 45.03923535223908203 ) ) ;
#15109=CARTESIAN_POINT ( 'NONE',  ( 48.40186567930497574, 28.91618040159426073, 45.03923535223908203 ) ) ;
#15124=CARTESIAN_POINT ( 'NONE',  ( 48.94625023931840957, 26.05784706826093355, 46.10640627770150246 ) ) ;
#15132=LINE ( 'NONE', #20046, #7731 ) ;
#15144=CARTESIAN_POINT ( 'NONE',  ( 48.67890918804130251, 25.06197292877712002, 45.08320410557258384 ) ) ;
#15148=ORIENTED_EDGE ( 'NONE', *, *, #9852, .T. ) ;
#15155=CARTESIAN_POINT ( 'NONE',  ( 48.83862994770794330, 25.94118040159426641, 48.17861352429476796 ) ) ;
#15160=ORIENTED_EDGE ( 'NONE', *, *, #14489, .T. ) ;
#15161=DIRECTION ( 'NONE',  ( 1.234978253042719660E-16, -1.000000000000000000, -1.109335647967047851E-31 ) ) ;
#15166=DIRECTION ( 'NONE',  ( 0.4544104193609807552, 0.000000000000000000, 0.8907924397839137587 ) ) ;
#15171=CARTESIAN_POINT ( 'NONE',  ( 44.79156314060809763, 22.86454579224779948, 46.92953032342011710 ) ) ;
#15207=ORIENTED_EDGE ( 'NONE', *, *, #17116, .F. ) ;
#15212=EDGE_LOOP ( 'NONE', ( #28305, #5358, #23321, #9400 ) ) ;
#15214=VERTEX_POINT ( 'NONE', #22498 ) ;
#15223=CARTESIAN_POINT ( 'NONE',  ( 46.99023568444673060, 27.83791119454915375, 49.12151524109405898 ) ) ;
#15232=ORIENTED_EDGE ( 'NONE', *, *, #30507, .T. ) ;
#15234=EDGE_CURVE ( 'NONE', #15887, #26305, #25088, .T. ) ;
#15244=ORIENTED_EDGE ( 'NONE', *, *, #20256, .F. ) ;
#15246=CARTESIAN_POINT ( 'NONE',  ( 46.04064016343871657, 22.98879437201065912, 48.06859758049203180 ) ) ;
#15250=CARTESIAN_POINT ( 'NONE',  ( 49.25382518103883456, 29.29907168554532149, 46.06391241801129866 ) ) ;
#15252=CARTESIAN_POINT ( 'NONE',  ( 49.49063479933183629, 27.31291119454915517, 47.17357720316391578 ) ) ;
#15262=CARTESIAN_POINT ( 'NONE',  ( 49.49063479933183629, 25.21291119454915730, 47.17357720316391578 ) ) ;
#15271=CARTESIAN_POINT ( 'NONE',  ( 45.24946171279598417, 29.20784706826092503, 47.99220971130007030 ) ) ;
#15277=CLOSED_SHELL ( 'NONE', ( #16789, #5447, #9821, #2926, #18650, #27720, #15753, #8538, #1356, #16591, #5629, #21206, #26853, #1593, #12739, #12879, #25120, #25306, #3339, #15760, #13074, #32097, #16922, #5955, #18244, #3710, #2523, #3438, #6193, #31506, #16014, #16631, #18160, #2036, #6485, #10652, #18984, #24344, #18291, #1515, #5233, #2445, #1656, #17975, #13559, #22082, #19182, #25450, #30392, #23201, #24341, #20439, #2638, #18768, #16808, #29310, #30098, #9630, #26044, #23495, #12312, #14073, #6250 ) ) ;
#15281=EDGE_CURVE ( 'NONE', #8039, #25543, #22693, .T. ) ;
#15293=CARTESIAN_POINT ( 'NONE',  ( 44.87087493598345134, 26.07587066347689486, 48.18533415931919706 ) ) ;
#15294=CARTESIAN_POINT ( 'NONE',  ( 47.09785597605719687, 24.76454579224779806, 47.04930799450078638 ) ) ;
#15297=CARTESIAN_POINT ( 'NONE',  ( 45.40326095744675428, 22.93807716476589675, 47.12319401418537268 ) ) ;
#15316=CARTESIAN_POINT ( 'NONE',  ( 48.94625023931840957, 26.05784706826093355, 46.10640627770150246 ) ) ;
#15325=ORIENTED_EDGE ( 'NONE', *, *, #1174, .T. ) ;
#15338=CARTESIAN_POINT ( 'NONE',  ( 45.29931651390019454, 22.86454579224779948, 47.92489232862990889 ) ) ;
#15340=CARTESIAN_POINT ( 'NONE',  ( 45.96182992765471909, 27.87822092656774586, 44.82232689504102296 ) ) ;
#15354=EDGE_CURVE ( 'NONE', #9336, #18648, #26749, .T. ) ;
#15356=ORIENTED_EDGE ( 'NONE', *, *, #9260, .T. ) ;
#15370=FACE_OUTER_BOUND ( 'NONE', #8210, .T. ) ;
#15382=CARTESIAN_POINT ( 'NONE',  ( 47.13599827484107863, 23.09557481883486929, 46.31488638136413272 ) ) ;
#15386=CARTESIAN_POINT ( 'NONE',  ( 44.70507715278255745, 29.06291119454914806, 46.92503878583764987 ) ) ;
#15410=CARTESIAN_POINT ( 'NONE',  ( 47.20547626766766314, 26.78791119454915659, 44.97710074790751378 ) ) ;
#15414=DIRECTION ( 'NONE',  ( 1.234978253042719660E-16, -1.000000000000000000, -1.109335647967047851E-31 ) ) ;
#15422=CARTESIAN_POINT ( 'NONE',  ( 48.53603344299159517, 25.12750526699945297, 48.64505250420380378 ) ) ;
#15423=SHAPE_DEFINITION_REPRESENTATION ( #27115, #5723 ) ;
#15427=CARTESIAN_POINT ( 'NONE',  ( 48.83862994770794330, 28.74118040159426002, 48.17861352429476796 ) ) ;
#15458=CARTESIAN_POINT ( 'NONE',  ( 44.91142894931555674, 28.69787913140503832, 45.63089057098605394 ) ) ;
#15473=CARTESIAN_POINT ( 'NONE',  ( 46.99023568444673060, 27.92451373492759714, 49.12151524109405898 ) ) ;
#15477=CARTESIAN_POINT ( 'NONE',  ( 48.18662509608405031, 28.59624452788247950, 49.18364984542562013 ) ) ;
#15492=ORIENTED_EDGE ( 'NONE', *, *, #22968, .T. ) ;
#15510=VERTEX_POINT ( 'NONE', #16719 ) ;
#15511=DIRECTION ( 'NONE',  ( 1.234978253042719660E-16, -1.000000000000000000, -1.109335647967047851E-31 ) ) ;
#15513=CARTESIAN_POINT ( 'NONE',  ( 48.40423897560355471, 29.16454579224780019, 44.91779129072006072 ) ) ;
#15516=CARTESIAN_POINT ( 'NONE',  ( 48.74539165043771760, 22.91413368675619111, 47.78185833695556539 ) ) ;
#15527=CARTESIAN_POINT ( 'NONE',  ( 46.81682104422132085, 23.12036939723557083, 47.03471240234085116 ) ) ;
#15543=CARTESIAN_POINT ( 'NONE',  ( 45.36511207810799107, 28.60948166895303402, 45.12672418911606087 ) ) ;
#15561=EDGE_CURVE ( 'NONE', #29641, #29156, #15972, .T. ) ;
#15563=CARTESIAN_POINT ( 'NONE',  ( 47.09785597605719687, 15.77906836436399374, 47.04930799450078638 ) ) ;
#15565=CARTESIAN_POINT ( 'NONE',  ( 45.38854177497844944, 26.92622849631043991, 45.94041160078741370 ) ) ;
#15567=EDGE_LOOP ( 'NONE', ( #10257, #3698, #3222, #24351 ) ) ;
#15568=FACE_OUTER_BOUND ( 'NONE', #27087, .T. ) ;
#15574=CARTESIAN_POINT ( 'NONE',  ( 48.83862994770795041, 25.15457786121582373, 48.17861352429476085 ) ) ;
#15580=CARTESIAN_POINT ( 'NONE',  ( 46.00908685603032922, 26.23284706826093071, 44.91496614357595263 ) ) ;
#15586=( BOUNDED_CURVE ( )  B_SPLINE_CURVE ( 2, ( #18637, #15543, #13738, #28024, #30812, #23418, #28186, #1091, #25554 ),
 .UNSPECIFIED., .F., .F. ) 
 B_SPLINE_CURVE_WITH_KNOTS ( ( 3, 2, 2, 2, 3 ),
 ( 0.6785714274101559695, 0.6904761904761904656, 0.7142857142857143016, 0.7380952380952381375, 0.7499999988387272554 ),
 .UNSPECIFIED. ) 
 CURVE ( )  GEOMETRIC_REPRESENTATION_ITEM ( )  RATIONAL_B_SPLINE_CURVE ( ( 0.9330127018922199644, 0.9330126953578159466, 1.000000000000000000, 0.8660254037844387076, 1.000000000000000000, 0.8660254037844387076, 1.000000000000000000, 0.9330127084266233162, 0.9330127018922199644 ) ) 
 REPRESENTATION_ITEM ( '' )  );
#15588=EDGE_CURVE ( 'NONE', #19042, #12544, #23546, .T. ) ;
#15605=DIRECTION ( 'NONE',  ( 0.5442436726714898754, 1.289618226626749973E-16, -0.8389271868029121171 ) ) ;
#15606=DIRECTION ( 'NONE',  ( 1.234978253042719660E-16, -1.000000000000000000, -1.109335647967047851E-31 ) ) ;
#15607=CARTESIAN_POINT ( 'NONE',  ( 48.24519908733286400, 29.46405251693653682, 48.93429100061246118 ) ) ;
#15610=CARTESIAN_POINT ( 'NONE',  ( 47.27395380374088774, 22.74928388133296764, 49.52406241924104791 ) ) ;
#15624=CARTESIAN_POINT ( 'NONE',  ( 45.79384627280941089, 26.46618040159426144, 49.05938063676249072 ) ) ;
#15626=CARTESIAN_POINT ( 'NONE',  ( 49.49063479933183629, 28.01291119454915091, 47.17357720316391578 ) ) ;
#15627=VECTOR ( 'NONE', #6001, 1000.000000000000000 ) ;
#15636=CYLINDRICAL_SURFACE ( 'NONE', #10407, 2.499999999999997335 ) ;
#15661=CARTESIAN_POINT ( 'NONE',  ( 49.64105649875294546, 24.93604219378083187, 46.47965702198763438 ) ) ;
#15697=CARTESIAN_POINT ( 'NONE',  ( 49.65101332465108186, 24.93501648625822398, 46.52608845888364186 ) ) ;
#15698=VECTOR ( 'NONE', #19579, 1000.000000000000227 ) ;
#15702=CARTESIAN_POINT ( 'NONE',  ( 48.94625023931840957, 25.27124452788249442, 46.10640627770150246 ) ) ;
#15727=CARTESIAN_POINT ( 'NONE',  ( 48.74539165043771760, 22.91413368675619111, 47.78185833695556539 ) ) ;
#15731=CARTESIAN_POINT ( 'NONE',  ( 47.20353132263855400, 25.40956182964377419, 45.01455027646040463 ) ) ;
#15734=ORIENTED_EDGE ( 'NONE', *, *, #4298, .F. ) ;
#15740=B_SPLINE_CURVE_WITH_KNOTS ( 'NONE', 3,
 ( #23056, #3190, #8454, #15516, #25526, #13234 ),
 .UNSPECIFIED., .F., .F.,
 ( 4, 2, 4 ),
 ( 0.000000000000000000, 0.5000000000000000000, 1.000000000000000000 ),
 .UNSPECIFIED. ) ;
#15753=ADVANCED_FACE ( 'NONE', ( #17872 ), #3413, .T. ) ;
#15760=ADVANCED_FACE ( 'NONE', ( #22944 ), #2794, .T. ) ;
#15795=ORIENTED_EDGE ( 'NONE', *, *, #21881, .F. ) ;
#15797=CARTESIAN_POINT ( 'NONE',  ( 45.79384627280941089, 27.86618040159426357, 49.05938063676249072 ) ) ;
#15799=CARTESIAN_POINT ( 'NONE',  ( 45.79384627280941089, 27.77957786121582018, 49.05938063676249072 ) ) ;
#15809=CARTESIAN_POINT ( 'NONE',  ( 47.77416835495956349, 22.84434098701873950, 49.08712782507307537 ) ) ;
#15812=TOROIDAL_SURFACE ( 'NONE', #20519, 2.799999999999998490, 0.2999999999999999334 ) ;
#15822=CARTESIAN_POINT ( 'NONE',  ( 46.33059210211230550, 22.93807716476589675, 45.54522087609679204 ) ) ;
#15864=CARTESIAN_POINT ( 'NONE',  ( 47.09785597605719687, 19.86454579224779948, 47.04930799450078638 ) ) ;
#15887=VERTEX_POINT ( 'NONE', #31316 ) ;
#15899=CARTESIAN_POINT ( 'NONE',  ( 48.16694854572211426, 26.51789516297709781, 49.14507740233662503 ) ) ;
#15904=VERTEX_POINT ( 'NONE', #18813 ) ;
#15912=CARTESIAN_POINT ( 'NONE',  ( 48.94625023931840246, 26.05784706826093355, 46.10640627770148825 ) ) ;
#15920=CIRCLE ( 'NONE', #13314, 4.200000000000000178 ) ;
#15935=LINE ( 'NONE', #13803, #31073 ) ;
#15950=CARTESIAN_POINT ( 'NONE',  ( 44.91142894931555674, 28.69787913140503832, 45.63089057098605394 ) ) ;
#15956=ORIENTED_EDGE ( 'NONE', *, *, #16441, .F. ) ;
#15958=EDGE_CURVE ( 'NONE', #30715, #23081, #31957, .T. ) ;
#15959=CARTESIAN_POINT ( 'NONE',  ( 47.03138641870017977, 22.86454579224779948, 49.04855133162938330 ) ) ;
#15964=ORIENTED_EDGE ( 'NONE', *, *, #17213, .F. ) ;
#15968=CARTESIAN_POINT ( 'NONE',  ( 45.18933221474103590, 15.77906836436399374, 43.30797974740836764 ) ) ;
#15972=( BOUNDED_CURVE ( )  B_SPLINE_CURVE ( 3, ( #22306, #4754, #2611, #2775 ),
 .UNSPECIFIED., .F., .F. ) 
 B_SPLINE_CURVE_WITH_KNOTS ( ( 4, 4 ),
 ( 5.062864179022698252, 5.184122060454619429 ),
 .UNSPECIFIED. ) 
 CURVE ( )  GEOMETRIC_REPRESENTATION_ITEM ( )  RATIONAL_B_SPLINE_CURVE ( ( 1.000000000000000000, 0.9987750858034806223, 0.9987750858034806223, 1.000000000000000000 ) ) 
 REPRESENTATION_ITEM ( '' )  );
#15978=CARTESIAN_POINT ( 'NONE',  ( 47.18879033565401215, 29.58872476413164776, 44.97623416235143168 ) ) ;
#16014=ADVANCED_FACE ( 'NONE', ( #14890 ), #9801, .F. ) ;
#16020=VERTEX_POINT ( 'NONE', #9962 ) ;
#16026=CARTESIAN_POINT ( 'NONE',  ( 48.22193606911519481, 23.04411619146717882, 47.10768726602483980 ) ) ;
#16047=CARTESIAN_POINT ( 'NONE',  ( 48.22193606911519481, 23.04411619146717882, 47.10768726602483980 ) ) ;
#16049=CARTESIAN_POINT ( 'NONE',  ( 49.44739180854976013, 28.73456182964376282, 47.17133137409169308 ) ) ;
#16064=CARTESIAN_POINT ( 'NONE',  ( 48.54365229441402363, 22.98879437201065912, 46.79176277441978016 ) ) ;
#16066=CARTESIAN_POINT ( 'NONE',  ( 49.49063479933183629, 25.99951373492759998, 47.17357720316391578 ) ) ;
#16104=CARTESIAN_POINT ( 'NONE',  ( 45.73035263060504718, 29.33954579807170404, 44.36855633853329550 ) ) ;
#16111=ORIENTED_EDGE ( 'NONE', *, *, #7905, .F. ) ;
#16122=ORIENTED_EDGE ( 'NONE', *, *, #25570, .F. ) ;
#16145=CARTESIAN_POINT ( 'NONE',  ( 48.55356409855115629, 22.86454579224779593, 48.48022381235000466 ) ) ;
#16156=( BOUNDED_CURVE ( )  B_SPLINE_CURVE ( 2, ( #20868, #17929, #25639, #3635, #31057, #18086, #25953, #18557, #852 ),
 .UNSPECIFIED., .F., .F. ) 
 B_SPLINE_CURVE_WITH_KNOTS ( ( 3, 2, 2, 2, 3 ),
 ( 0.6071428559815844617, 0.6190476190476190688, 0.6428571428571427937, 0.6666666666666667407, 0.6785714274101559695 ),
 .UNSPECIFIED. ) 
 CURVE ( )  GEOMETRIC_REPRESENTATION_ITEM ( )  RATIONAL_B_SPLINE_CURVE ( ( 0.9330127018922200755, 0.9330126953578157245, 1.000000000000000000, 0.8660254037844387076, 1.000000000000000000, 0.8660254037844387076, 1.000000000000000000, 0.9330127084266226500, 0.9330127018922199644 ) ) 
 REPRESENTATION_ITEM ( '' )  );
#16175=CARTESIAN_POINT ( 'NONE',  ( 47.19823469859255738, 22.88065857334294861, 45.11653766655789610 ) ) ;
#16178=CARTESIAN_POINT ( 'NONE',  ( 48.40186567930498285, 26.02957786121582373, 45.03923535223908203 ) ) ;
#16189=VERTEX_POINT ( 'NONE', #16601 ) ;
#16203=CARTESIAN_POINT ( 'NONE',  ( 46.02876340639226527, 28.26789516297709071, 44.95353858666495483 ) ) ;
#16208=CARTESIAN_POINT ( 'NONE',  ( 49.17081279531085158, 29.55164023231963455, 46.60812646017934213 ) ) ;
#16223=CARTESIAN_POINT ( 'NONE',  ( 46.34827318194108159, 20.53597436367636675, 45.57988155192556690 ) ) ;
#16262=VERTEX_POINT ( 'NONE', #31562 ) ;
#16264=VECTOR ( 'NONE', #16412, 1000.000000000000000 ) ;
#16269=CARTESIAN_POINT ( 'NONE',  ( 50.10320668408830613, 29.80621246473836905, 47.20539118556276037 ) ) ;
#16277=CARTESIAN_POINT ( 'NONE',  ( 46.99023568444673060, 29.32451373492759217, 49.12151524109405898 ) ) ;
#16295=CARTESIAN_POINT ( 'NONE',  ( 45.79384627280941800, 26.37957786121582160, 49.05938063676250493 ) ) ;
#16331=CARTESIAN_POINT ( 'NONE',  ( 45.42003181263716272, 22.93807716476589675, 46.80027486889689214 ) ) ;
#16364=CARTESIAN_POINT ( 'NONE',  ( 48.91284552371730143, 26.73619643316632377, 46.12344667017377020 ) ) ;
#16375=CARTESIAN_POINT ( 'NONE',  ( 44.91142894931555674, 27.99787913140503903, 45.63089057098605394 ) ) ;
#16385=DIRECTION ( 'NONE',  ( 0.3435019893673583735, 0.6546536707079779749, 0.6733757901270565061 ) ) ;
#16412=DIRECTION ( 'NONE',  ( 1.234978253042719660E-16, -1.000000000000000000, -1.109335647967047851E-31 ) ) ;
#16430=CARTESIAN_POINT ( 'NONE',  ( 48.46535932150934656, 29.68954579807170191, 49.73005965046827015 ) ) ;
#16439=CARTESIAN_POINT ( 'NONE',  ( 49.19517401419062708, 28.40920399681022701, 48.40991706654173754 ) ) ;
#16440=CARTESIAN_POINT ( 'NONE',  ( 46.02876340639226527, 25.51119643316632235, 44.95353858666495483 ) ) ;
#16441=EDGE_CURVE ( 'NONE', #3511, #4649, #15935, .T. ) ;
#16451=CARTESIAN_POINT ( 'NONE',  ( 45.00053793792376666, 27.93655426599985248, 45.68869892245983522 ) ) ;
#16455=CARTESIAN_POINT ( 'NONE',  ( 48.40186567930497574, 28.12957786121581805, 45.03923535223908203 ) ) ;
#16461=CARTESIAN_POINT ( 'NONE',  ( 45.96182992765472619, 28.70087065737811827, 44.82232689504103007 ) ) ;
#16468=AXIS2_PLACEMENT_3D ( 'NONE', #32369, #12185, #4959 ) ;
#16472=ORIENTED_EDGE ( 'NONE', *, *, #2221, .F. ) ;
#16473=CARTESIAN_POINT ( 'NONE',  ( 47.38797297166576072, 29.43365986774335497, 49.26645484953866116 ) ) ;
#16499=CARTESIAN_POINT ( 'NONE',  ( 47.47194490827082092, 22.91413368675619111, 45.28548791484912783 ) ) ;
#16510=VECTOR ( 'NONE', #3253, 1000.000000000000000 ) ;
#16511=ORIENTED_EDGE ( 'NONE', *, *, #8213, .T. ) ;
#16524=CARTESIAN_POINT ( 'NONE',  ( 48.80717017713595141, 28.01952976649964810, 48.15820438821415195 ) ) ;
#16534=AXIS2_PLACEMENT_3D ( 'NONE', #14490, #19392, #14161 ) ;
#16536=CARTESIAN_POINT ( 'NONE',  ( 44.09250526802607340, 25.25621246473838255, 46.89322480343881949 ) ) ;
#16548=CARTESIAN_POINT ( 'NONE',  ( 48.23388214087538017, 25.16454579224780019, 49.27628903457465270 ) ) ;
#16552=EDGE_CURVE ( 'NONE', #25764, #16020, #28200, .T. ) ;
#16555=EDGE_CURVE ( 'NONE', #12544, #28026, #27076, .T. ) ;
#16560=AXIS2_PLACEMENT_3D ( 'NONE', #5326, #5154, #15166 ) ;
#16565=ORIENTED_EDGE ( 'NONE', *, *, #14719, .T. ) ;
#16584=CARTESIAN_POINT ( 'NONE',  ( 48.46535932150934656, 26.18954579807170902, 49.73005965046827015 ) ) ;
#16591=ADVANCED_FACE ( 'NONE', ( #19355 ), #6577, .T. ) ;
#16595=CARTESIAN_POINT ( 'NONE',  ( 48.83862994770794330, 28.04118040159426428, 48.17861352429476796 ) ) ;
#16600=CARTESIAN_POINT ( 'NONE',  ( 45.96182992765472619, 26.47822092656774728, 44.82232689504103007 ) ) ;
#16601=CARTESIAN_POINT ( 'NONE',  ( 45.33322567907855927, 22.86454579224779948, 47.99136533781562974 ) ) ;
#16609=CARTESIAN_POINT ( 'NONE',  ( 48.94625023931840246, 28.77124452788248377, 46.10640627770150246 ) ) ;
#16615=CARTESIAN_POINT ( 'NONE',  ( 46.96997866373305186, 23.12036939723557083, 46.79862680810013131 ) ) ;
#16616=PLANE ( 'NONE',  #9428 ) ;
#16627=CARTESIAN_POINT ( 'NONE',  ( 47.08544753267502614, 29.42444312243182836, 49.29451668004490728 ) ) ;
#16631=ADVANCED_FACE ( 'NONE', ( #31689 ), #32008, .F. ) ;
#16639=ORIENTED_EDGE ( 'NONE', *, *, #6521, .F. ) ;
#16642=EDGE_CURVE ( 'NONE', #5063, #22685, #12637, .T. ) ;
#16678=CARTESIAN_POINT ( 'NONE',  ( 48.37829923888483563, 28.89452976649964810, 45.07556196625585443 ) ) ;
#16685=DIRECTION ( 'NONE',  ( 0.4544104193609915243, 0.000000000000000000, 0.8907924397839082076 ) ) ;
#16692=CARTESIAN_POINT ( 'NONE',  ( 44.77625694075215534, 24.61454579807171328, 48.23360063142255427 ) ) ;
#16693=CARTESIAN_POINT ( 'NONE',  ( 47.86511985000206693, 22.93807716476589320, 48.55339511290479493 ) ) ;
#16695=ORIENTED_EDGE ( 'NONE', *, *, #19049, .F. ) ;
#16719=CARTESIAN_POINT ( 'NONE',  ( 44.67624849883564053, 19.86454579224779948, 46.92354143986608506 ) ) ;
#16745=CARTESIAN_POINT ( 'NONE',  ( 49.28428300279882990, 25.54787913140504685, 48.46772541801551171 ) ) ;
#16750=AXIS2_PLACEMENT_3D ( 'NONE', #11463, #1778, #29188 ) ;
#16756=CARTESIAN_POINT ( 'NONE',  ( 48.80717017713595141, 25.91952976649965734, 48.15820438821415195 ) ) ;
#16771=CARTESIAN_POINT ( 'NONE',  ( 44.87087493598345134, 28.05322093266651962, 48.18533415931919706 ) ) ;
#16789=ADVANCED_FACE ( 'NONE', ( #7395 ), #10845, .F. ) ;
#16808=ADVANCED_FACE ( 'NONE', ( #6209 ), #23291, .F. ) ;
#16825=DIRECTION ( 'NONE',  ( 1.234978253042719660E-16, -1.000000000000000000, -1.109335647967047851E-31 ) ) ;
#16851=CARTESIAN_POINT ( 'NONE',  ( 45.38854177497844944, 29.06952976649964882, 45.94041160078741370 ) ) ;
#16858=FACE_OUTER_BOUND ( 'NONE', #639, .T. ) ;
#16863=CARTESIAN_POINT ( 'NONE',  ( 46.96268396749378127, 27.53121246473837402, 49.65201805493727960 ) ) ;
#16879=EDGE_CURVE ( 'NONE', #4161, #29641, #20194, .T. ) ;
#16901=DIRECTION ( 'NONE',  ( 1.234978253042719660E-16, -1.000000000000000000, -1.109335647967047851E-31 ) ) ;
#16903=ORIENTED_EDGE ( 'NONE', *, *, #22531, .F. ) ;
#16918=CARTESIAN_POINT ( 'NONE',  ( 46.95686452149019630, 22.86454579224779948, 49.04468102550210773 ) ) ;
#16921=CARTESIAN_POINT ( 'NONE',  ( 48.40186567930498285, 28.21618040159426499, 45.03923535223908203 ) ) ;
#16922=ADVANCED_FACE ( 'NONE', ( #5901 ), #5397, .T. ) ;
#16926=CARTESIAN_POINT ( 'NONE',  ( 47.99562520726186676, 20.53597436367637386, 45.66543703126890819 ) ) ;
#16937=CARTESIAN_POINT ( 'NONE',  ( 45.46177120706448704, 22.89977464660286444, 46.15605224449101485 ) ) ;
#16938=CARTESIAN_POINT ( 'NONE',  ( 44.57318751115185052, 25.19787913140503477, 45.41146063192157101 ) ) ;
#16942=CARTESIAN_POINT ( 'NONE',  ( 47.42898969722134694, 14.98691807112498964, 46.53888023006170727 ) ) ;
#16943=CARTESIAN_POINT ( 'NONE',  ( 45.41653742442153430, 19.86454579224779948, 43.75337596730032175 ) ) ;
#16945=ORIENTED_EDGE ( 'NONE', *, *, #6228, .T. ) ;
#16973=FACE_OUTER_BOUND ( 'NONE', #10798, .T. ) ;
#16991=AXIS2_PLACEMENT_3D ( 'NONE', #26783, #4131, #28760 ) ;
#17005=CARTESIAN_POINT ( 'NONE',  ( 48.80717017713595141, 29.41952976649965024, 48.15820438821415195 ) ) ;
#17006=EDGE_LOOP ( 'NONE', ( #15232, #28212, #28409, #4693 ) ) ;
#17008=ORIENTED_EDGE ( 'NONE', *, *, #27990, .T. ) ;
#17010=ORIENTED_EDGE ( 'NONE', *, *, #27901, .F. ) ;
#17016=CARTESIAN_POINT ( 'NONE',  ( 44.91142894931555674, 26.59787913140504401, 45.63089057098605394 ) ) ;
#17024=CARTESIAN_POINT ( 'NONE',  ( 47.15451600283464728, 29.59167404947196900, 44.97719271889386050 ) ) ;
#17033=EDGE_LOOP ( 'NONE', ( #26212, #27474, #20476 ) ) ;
#17065=ORIENTED_EDGE ( 'NONE', *, *, #9539, .T. ) ;
#17086=CARTESIAN_POINT ( 'NONE',  ( 47.20547626766766314, 25.47451373492760140, 44.97710074790751378 ) ) ;
#17100=CARTESIAN_POINT ( 'NONE',  ( 45.98154733146137119, 23.04411657098542676, 46.84134192585683820 ) ) ;
#17101=DIRECTION ( 'NONE',  ( -0.4544104193609908027, 6.737912671758736131E-17, -0.8907924397839086517 ) ) ;
#17116=EDGE_CURVE ( 'NONE', #3003, #6052, #17351, .T. ) ;
#17118=CARTESIAN_POINT ( 'NONE',  ( 44.74510487398335812, 29.30808892249564934, 46.84805612806227515 ) ) ;
#17127=EDGE_LOOP ( 'NONE', ( #24523, #30681, #22887, #4898 ) ) ;
#17133=ORIENTED_EDGE ( 'NONE', *, *, #24722, .F. ) ;
#17137=DIRECTION ( 'NONE',  ( 0.9986540920324801229, 1.233316085972235327E-16, 0.05186525298099653458 ) ) ;
#17161=VECTOR ( 'NONE', #30785, 1000.000000000000000 ) ;
#17173=DIRECTION ( 'NONE',  ( 0.4544104193609900810, 5.611869858668441979E-17, 0.8907924397839090958 ) ) ;
#17180=CARTESIAN_POINT ( 'NONE',  ( 46.99023568444673060, 26.43791119454915517, 49.12151524109405898 ) ) ;
#17181=CARTESIAN_POINT ( 'NONE',  ( 47.72109904461037644, 22.93807716476589320, 48.62686290590787053 ) ) ;
#17185=CARTESIAN_POINT ( 'NONE',  ( 48.82187354100420151, 22.88065857334294861, 46.16985335424439540 ) ) ;
#17190=VECTOR ( 'NONE', #17101, 1000.000000000000114 ) ;
#17199=CARTESIAN_POINT ( 'NONE',  ( 46.18676869530867179, 23.03451764446790051, 47.84429317205637489 ) ) ;
#17202=VECTOR ( 'NONE', #6891, 1000.000000000000227 ) ;
#17208=( BOUNDED_CURVE ( )  B_SPLINE_CURVE ( 2, ( #1130, #13462, #8690, #26563, #23460, #10994, #3920, #14102, #971 ),
 .UNSPECIFIED., .F., .F. ) 
 B_SPLINE_CURVE_WITH_KNOTS ( ( 3, 2, 2, 2, 3 ),
 ( 0.03571428571428342941, 0.04761904761904767192, 0.07142857142857139685, 0.09523809523809523281, 0.1071428559815845449 ),
 .UNSPECIFIED. ) 
 CURVE ( )  GEOMETRIC_REPRESENTATION_ITEM ( )  RATIONAL_B_SPLINE_CURVE ( ( 0.9330127018922194093, 0.9330127018922063087, 1.000000000000000000, 0.8660254037844387076, 1.000000000000000000, 0.8660254037844387076, 1.000000000000000000, 0.9330127084266226500, 0.9330127018922200755 ) ) 
 REPRESENTATION_ITEM ( '' )  );
#17212=CARTESIAN_POINT ( 'NONE',  ( 47.20547626766766314, 25.38791119454915801, 44.97710074790751378 ) ) ;
#17213=EDGE_CURVE ( 'NONE', #9336, #2302, #25883, .T. ) ;
#17223=CARTESIAN_POINT ( 'NONE',  ( 48.14727188781975542, 22.86454579224779948, 49.10650501410607660 ) ) ;
#17224=CARTESIAN_POINT ( 'NONE',  ( 48.18662509608405742, 26.49624452788248519, 49.18364984542562013 ) ) ;
#17228=LINE ( 'NONE', #24296, #21390 ) ;
#17231=CARTESIAN_POINT ( 'NONE',  ( 46.00908685603033632, 29.03284706826092076, 44.91496614357595263 ) ) ;
#17266=CARTESIAN_POINT ( 'NONE',  ( 48.28214861297873739, 24.78954579807170333, 49.37090702980594159 ) ) ;
#17278=CARTESIAN_POINT ( 'NONE',  ( 48.18662509608405031, 29.38284706826092574, 49.18364984542562013 ) ) ;
#17349=DIRECTION ( 'NONE',  ( -0.5442436726714897643, -6.721291001053910056E-17, 0.8389271868029121171 ) ) ;
#17350=CARTESIAN_POINT ( 'NONE',  ( 48.52450352821730917, 22.84434098701873594, 45.44469437819130775 ) ) ;
#17351=LINE ( 'NONE', #4723, #14846 ) ;
#17352=CARTESIAN_POINT ( 'NONE',  ( 44.70507715278255745, 29.76291119454914380, 46.92503878583764987 ) ) ;
#17356=DIRECTION ( 'NONE',  ( 1.234978253042719660E-16, -1.000000000000000000, -1.109335647967047851E-31 ) ) ;
#17369=CARTESIAN_POINT ( 'NONE',  ( 46.65195039438923885, 23.10527865767145173, 47.43093233858343893 ) ) ;
#17381=CARTESIAN_POINT ( 'NONE',  ( 45.24946171279598417, 27.02124452788248732, 47.99220971130007030 ) ) ;
#17393=CARTESIAN_POINT ( 'NONE',  ( 45.35708200440645044, 26.90457786121582018, 45.92000246470680480 ) ) ;
#17396=ORIENTED_EDGE ( 'NONE', *, *, #3931, .T. ) ;
#17401=CARTESIAN_POINT ( 'NONE',  ( 47.20547626766765603, 28.97451373492759430, 44.97710074790751378 ) ) ;
#17412=( BOUNDED_CURVE ( )  B_SPLINE_CURVE ( 3, ( #3539, #13413, #10632, #13730 ),
 .UNSPECIFIED., .F., .F. ) 
 B_SPLINE_CURVE_WITH_KNOTS ( ( 4, 4 ),
 ( 5.062864179022701805, 5.184122060454622982 ),
 .UNSPECIFIED. ) 
 CURVE ( )  GEOMETRIC_REPRESENTATION_ITEM ( )  RATIONAL_B_SPLINE_CURVE ( ( 1.000000000000000000, 0.9987750858034806223, 0.9987750858034806223, 1.000000000000000000 ) ) 
 REPRESENTATION_ITEM ( '' )  );
#17416=CARTESIAN_POINT ( 'NONE',  ( 45.79384627280941089, 26.46618040159426144, 49.05938063676249072 ) ) ;
#17426=CARTESIAN_POINT ( 'NONE',  ( 45.84097905237065618, 19.96454579224779380, 48.98672734302541443 ) ) ;
#17439=VECTOR ( 'NONE', #13902, 1000.000000000000114 ) ;
#17451=CARTESIAN_POINT ( 'NONE',  ( 46.48213017528662760, 29.40643497231507553, 49.22721246743694223 ) ) ;
#17508=CARTESIAN_POINT ( 'NONE',  ( 48.23388214087538017, 25.42822093266651606, 49.27628903457465270 ) ) ;
#17510=FACE_OUTER_BOUND ( 'NONE', #20316, .T. ) ;
#17520=CARTESIAN_POINT ( 'NONE',  ( 46.00908685603034343, 27.54624452788248590, 44.91496614357595263 ) ) ;
#17527=CARTESIAN_POINT ( 'NONE',  ( 47.63716429968715005, 28.31960992152947298, 49.58068632438585155 ) ) ;
#17529=VECTOR ( 'NONE', #31557, 1000.000000000000114 ) ;
#17538=CARTESIAN_POINT ( 'NONE',  ( 46.17891025898683921, 22.93807716476589675, 48.46582155994513386 ) ) ;
#17546=CARTESIAN_POINT ( 'NONE',  ( 46.99023568444673060, 25.73791119454915588, 49.12151524109405898 ) ) ;
#17560=CARTESIAN_POINT ( 'NONE',  ( 45.00053793792376666, 28.75920399681022488, 45.68869892245983522 ) ) ;
#17574=AXIS2_PLACEMENT_3D ( 'NONE', #10939, #26346, #5862 ) ;
#17579=CARTESIAN_POINT ( 'NONE',  ( 46.99023568444673060, 27.22451373492759785, 49.12151524109405898 ) ) ;
#17585=CARTESIAN_POINT ( 'NONE',  ( 44.87087493598345134, 27.47587066347689344, 48.18533415931919706 ) ) ;
#17599=CARTESIAN_POINT ( 'NONE',  ( 49.13615439483240976, 25.02317097547241076, 45.53350292621570361 ) ) ;
#17609=CARTESIAN_POINT ( 'NONE',  ( 46.00908685603034343, 26.23284706826093071, 44.91496614357595263 ) ) ;
#17634=EDGE_CURVE ( 'NONE', #13719, #24589, #30470, .T. ) ;
#17644=AXIS2_PLACEMENT_3D ( 'NONE', #5256, #165, #10186 ) ;
#17654=CARTESIAN_POINT ( 'NONE',  ( 44.21498992391908445, 25.89488759933319173, 46.89958605635244027 ) ) ;
#17676=CARTESIAN_POINT ( 'NONE',  ( 49.49063479933183629, 27.31291119454915517, 47.17357720316391578 ) ) ;
#17683=CARTESIAN_POINT ( 'NONE',  ( 44.21498992391908445, 28.11753733014355916, 46.89958605635242606 ) ) ;
#17694=CARTESIAN_POINT ( 'NONE',  ( 45.39590889550878927, 22.93328494799376571, 47.28470721838063184 ) ) ;
#17699=CARTESIAN_POINT ( 'NONE',  ( 47.20547626766766314, 26.08791119454915730, 44.97710074790751378 ) ) ;
#17721=CARTESIAN_POINT ( 'NONE',  ( 48.94625023931840246, 28.15784706826092787, 46.10640627770149536 ) ) ;
#17735=CARTESIAN_POINT ( 'NONE',  ( 45.79384627280941089, 25.06618040159426641, 49.05938063676249072 ) ) ;
#17740=DIRECTION ( 'NONE',  ( 0.4544104193609900810, 0.000000000000000000, 0.8907924397839089847 ) ) ;
#17741=CARTESIAN_POINT ( 'NONE',  ( 46.96819297411687444, 26.19253733014356200, 49.54594323136014822 ) ) ;
#17747=CARTESIAN_POINT ( 'NONE',  ( 45.38329851326696485, 22.91413368675619111, 47.60724751575505564 ) ) ;
#17753=CARTESIAN_POINT ( 'NONE',  ( 45.73035263060504718, 29.33954579807170404, 44.36855633853329550 ) ) ;
#17757=CIRCLE ( 'NONE', #24056, 4.100000000000001421 ) ;
#17758=CARTESIAN_POINT ( 'NONE',  ( 49.31977745283734293, 25.00299017030662441, 45.79416704315556075 ) ) ;
#17767=VERTEX_POINT ( 'NONE', #31920 ) ;
#17770=CARTESIAN_POINT ( 'NONE',  ( 48.94625023931840246, 28.15784706826092787, 46.10640627770150246 ) ) ;
#17779=EDGE_LOOP ( 'NONE', ( #11218, #14037, #14801, #15964, #21685, #1167 ) ) ;
#17791=CARTESIAN_POINT ( 'NONE',  ( 47.09785597605719687, 25.16454579224780019, 47.04930799450078638 ) ) ;
#17820=CARTESIAN_POINT ( 'NONE',  ( 48.83059987400640978, 26.85948166895303402, 48.97189179988552610 ) ) ;
#17830=CYLINDRICAL_SURFACE ( 'NONE', #2861, 2.499999999999997335 ) ;
#17834=VERTEX_POINT ( 'NONE', #22874 ) ;
#17841=CARTESIAN_POINT ( 'NONE',  ( 48.40186567930498285, 29.52957786121581307, 45.03923535223908203 ) ) ;
#17844=DIRECTION ( 'NONE',  ( 1.234978253042719660E-16, -1.000000000000000000, -1.109335647967047851E-31 ) ) ;
#17871=CARTESIAN_POINT ( 'NONE',  ( 48.97837830602554021, 29.34785002538245990, 45.68769290308407705 ) ) ;
#17872=FACE_OUTER_BOUND ( 'NONE', #23497, .T. ) ;
#17873=CARTESIAN_POINT ( 'NONE',  ( 48.80717017713595141, 29.37622849631043209, 48.15820438821415195 ) ) ;
#17878=VECTOR ( 'NONE', #17349, 1000.000000000000227 ) ;
#17896=EDGE_CURVE ( 'NONE', #19042, #20793, #4670, .T. ) ;
#17910=CARTESIAN_POINT ( 'NONE',  ( 47.09785597605719687, 24.76454579224779806, 47.04930799450078638 ) ) ;
#17911=CARTESIAN_POINT ( 'NONE',  ( 45.96182992765471909, 25.90087065737812466, 44.82232689504102296 ) ) ;
#17929=CARTESIAN_POINT ( 'NONE',  ( 48.83059987400640267, 28.25948166895303260, 48.97189179988551899 ) ) ;
#17933=CARTESIAN_POINT ( 'NONE',  ( 46.99023568444673060, 26.52451373492759856, 49.12151524109405898 ) ) ;
#17934=CARTESIAN_POINT ( 'NONE',  ( 46.99023568444673060, 29.23791119454914877, 49.12151524109405898 ) ) ;
#17958=DIRECTION ( 'NONE',  ( 0.4544104193609990738, 0.000000000000000000, 0.8907924397839043218 ) ) ;
#17967=CARTESIAN_POINT ( 'NONE',  ( 49.00477282619483788, 29.13168691486794515, 45.28585184200404967 ) ) ;
#17975=ADVANCED_FACE ( 'NONE', ( #32412 ), #27482, .F. ) ;
#17994=ORIENTED_EDGE ( 'NONE', *, *, #29204, .F. ) ;
#18000=CARTESIAN_POINT ( 'NONE',  ( 46.04327488119035650, 22.93807716476589675, 48.37782978030396208 ) ) ;
#18002=B_SPLINE_CURVE_WITH_KNOTS ( 'NONE', 3,
 ( #23706, #3841, #31422, #6472, #16473, #16627, #21719, #19248, #17451, #26816, #32395, #24846, #21877, #20076, #4332, #2516, #2365, #2198, #19909, #15003, #17118, #4496, #14675, #25006, #29448, #11881, #27137, #24680, #27473, #12382, #4655, #14843 ),
 .UNSPECIFIED., .F., .F.,
 ( 4, 2, 2, 2, 2, 2, 2, 2, 2, 2, 2, 2, 2, 2, 2, 4 ),
 ( 0.003975046523139969153, 0.004428463406335606325, 0.004881880289531242631, 0.005335297172726879804, 0.005788714055922516109, 0.006242130939118153282, 0.006695547822313789588, 0.007148964705509426761, 0.007602381588705063933, 0.008509215355096317462, 0.008962632238291936421, 0.009416049121487553644, 0.009869466004683170868, 0.01032288288787878809, 0.01077629977107440531, 0.01122971665427002254 ),
 .UNSPECIFIED. ) ;
#18009=DIRECTION ( 'NONE',  ( 0.4544104193609903586, 0.000000000000000000, 0.8907924397839087627 ) ) ;
#18023=( LENGTH_UNIT ( ) NAMED_UNIT ( * ) SI_UNIT ( .MILLI., .METRE. ) );
#18024=CARTESIAN_POINT ( 'NONE',  ( 47.32773967697124817, 29.57151323798673914, 44.96316438875158639 ) ) ;
#18026=CARTESIAN_POINT ( 'NONE',  ( 47.20353132263855400, 27.50956182964376140, 45.01455027646040463 ) ) ;
#18074=DIRECTION ( 'NONE',  ( -0.9761574614375593262, 0.2110602665713100234, -0.05069688703093822718 ) ) ;
#18086=CARTESIAN_POINT ( 'NONE',  ( 48.66895200406656841, 28.46155426599985105, 44.62753372671560470 ) ) ;
#18090=VECTOR ( 'NONE', #15605, 1000.000000000000227 ) ;
#18091=CARTESIAN_POINT ( 'NONE',  ( 48.83862994770794330, 25.24118040159427068, 48.17861352429476796 ) ) ;
#18097=FACE_OUTER_BOUND ( 'NONE', #15212, .T. ) ;
#18114=FACE_OUTER_BOUND ( 'NONE', #27800, .T. ) ;
#18118=VECTOR ( 'NONE', #31114, 1000.000000000000000 ) ;
#18121=CARTESIAN_POINT ( 'NONE',  ( 49.19517401419062708, 26.18655426599985958, 48.40991706654173754 ) ) ;
#18124=CARTESIAN_POINT ( 'NONE',  ( 49.70752207505586284, 24.90576773639369179, 46.59986279770737383 ) ) ;
#18126=ORIENTED_EDGE ( 'NONE', *, *, #16552, .T. ) ;
#18129=CARTESIAN_POINT ( 'NONE',  ( 49.98072202819531640, 29.04488759933318676, 47.19902993264913960 ) ) ;
#18145=LINE ( 'NONE', #8309, #24140 ) ;
#18159=CARTESIAN_POINT ( 'NONE',  ( 45.35708200440645044, 25.50457786121582515, 45.92000246470679770 ) ) ;
#18160=ADVANCED_FACE ( 'NONE', ( #19221 ), #9233, .F. ) ;
#18170=VERTEX_POINT ( 'NONE', #8901 ) ;
#18178=CARTESIAN_POINT ( 'NONE',  ( 47.86511985000206693, 22.93807716476589320, 48.55339511290479493 ) ) ;
#18179=LINE ( 'NONE', #5724, #16510 ) ;
#18181=CARTESIAN_POINT ( 'NONE',  ( 45.81741271322955100, 28.50122849631042499, 49.02305402274571122 ) ) ;
#18192=EDGE_CURVE ( 'NONE', #20793, #21089, #2176, .T. ) ;
#18198=CARTESIAN_POINT ( 'NONE',  ( 48.94625023931840246, 26.75784706826093284, 46.10640627770148825 ) ) ;
#18225=CARTESIAN_POINT ( 'NONE',  ( 46.31735793284625657, 25.18224532316113340, 44.64096519649219630 ) ) ;
#18238=CARTESIAN_POINT ( 'NONE',  ( 48.18662509608405031, 28.68284706826092290, 49.18364984542562013 ) ) ;
#18239=CARTESIAN_POINT ( 'NONE',  ( 47.20547626766766314, 28.88791119454915091, 44.97710074790751378 ) ) ;
#18244=ADVANCED_FACE ( 'NONE', ( #25141 ), #30636, .T. ) ;
#18245=EDGE_CURVE ( 'NONE', #11490, #30019, #10806, .T. ) ;
#18251=ORIENTED_EDGE ( 'NONE', *, *, #9164, .T. ) ;
#18263=( BOUNDED_CURVE ( )  B_SPLINE_CURVE ( 2, ( #18722, #28928, #6757, #11204, #26131, #8895, #16439, #23827, #9057 ),
 .UNSPECIFIED., .F., .F. ) 
 B_SPLINE_CURVE_WITH_KNOTS ( ( 3, 2, 2, 2, 3 ),
 ( 0.1785714297327012090, 0.1904761904761904656, 0.2142857142857142738, 0.2380952380952380820, 0.2500000011612727446 ),
 .UNSPECIFIED. ) 
 CURVE ( )  GEOMETRIC_REPRESENTATION_ITEM ( )  RATIONAL_B_SPLINE_CURVE ( ( 0.9330127018922200755, 0.9330127084266228721, 1.000000000000000000, 0.8660254037844388186, 1.000000000000000000, 0.8660254037844388186, 1.000000000000000000, 0.9330126953578155025, 0.9330127018922200755 ) ) 
 REPRESENTATION_ITEM ( '' )  );
#18275=CARTESIAN_POINT ( 'NONE',  ( 47.34970371437788828, 29.61382036679943752, 45.01289284012537451 ) ) ;
#18291=ADVANCED_FACE ( 'NONE', ( #2171 ), #30234, .F. ) ;
#18297=CARTESIAN_POINT ( 'NONE',  ( 46.55854765242722948, 27.14696019071910982, 44.51792966461572831 ) ) ;
#18302=CARTESIAN_POINT ( 'NONE',  ( 47.09785597605719687, 29.86454579224779948, 47.04930799450078638 ) ) ;
#18335=EDGE_CURVE ( 'NONE', #17767, #30606, #6769, .T. ) ;
#18342=CARTESIAN_POINT ( 'NONE',  ( 47.09785597605719687, 23.12036939723557083, 47.04930799450080059 ) ) ;
#18344=CARTESIAN_POINT ( 'NONE',  ( 49.58529161108529593, 29.18166210836908547, 47.08701687824213167 ) ) ;
#18346=CARTESIAN_POINT ( 'NONE',  ( 45.81741271322955100, 26.40122849631043422, 49.02305402274571122 ) ) ;
#18390=CARTESIAN_POINT ( 'NONE',  ( 45.99457799031791438, 29.23661293962803143, 44.88652376508412090 ) ) ;
#18402=ORIENTED_EDGE ( 'NONE', *, *, #1927, .T. ) ;
#18406=CARTESIAN_POINT ( 'NONE',  ( 49.28428300279882990, 29.04787913140503974, 48.46772541801551171 ) ) ;
#18420=CARTESIAN_POINT ( 'NONE',  ( 48.34748475735720774, 24.70653309617948423, 49.49898713858203791 ) ) ;
#18424=DIRECTION ( 'NONE',  ( -0.4441739386572048365, -0.2110602665713104675, -0.8707256032141199587 ) ) ;
#18430=CARTESIAN_POINT ( 'NONE',  ( 46.54440680854508372, 23.10527865767145173, 46.85395460512839350 ) ) ;
#18460=CARTESIAN_POINT ( 'NONE',  ( 45.96182992765471909, 27.87822092656774231, 44.82232689504102296 ) ) ;
#18471=EDGE_LOOP ( 'NONE', ( #29924, #22900, #21869, #23743 ) ) ;
#18476=CARTESIAN_POINT ( 'NONE',  ( 46.74373320708509283, 22.98879437201065912, 45.62408745049495451 ) ) ;
#18501=CARTESIAN_POINT ( 'NONE',  ( 47.74276738922625896, 23.04411657098542321, 47.98391173131702914 ) ) ;
#18506=CARTESIAN_POINT ( 'NONE',  ( 45.28286642839709231, 25.64289516297710847, 47.97516931882780966 ) ) ;
#18519=CARTESIAN_POINT ( 'NONE',  ( 47.75295489951383132, 23.09557481883486929, 46.71512938763805067 ) ) ;
#18557=CARTESIAN_POINT ( 'NONE',  ( 46.55854765242723659, 28.54696019071910840, 44.51792966461573542 ) ) ;
#18562=CARTESIAN_POINT ( 'NONE',  ( 44.91142894931555674, 30.09787913140503335, 45.63089057098605394 ) ) ;
#18563=FACE_OUTER_BOUND ( 'NONE', #23453, .T. ) ;
#18595=CARTESIAN_POINT ( 'NONE',  ( 49.68037673357003570, 24.91954977745023214, 46.56884725464978203 ) ) ;
#18598=DIRECTION ( 'NONE',  ( 0.3213166889719795694, -0.7071067811865470176, 0.6298853748009115572 ) ) ;
#18631=VERTEX_POINT ( 'NONE', #22914 ) ;
#18636=EDGE_LOOP ( 'NONE', ( #19202, #17396, #15734 ) ) ;
#18637=CARTESIAN_POINT ( 'NONE',  ( 45.96182992765472619, 28.57822092656774160, 44.82232689504103007 ) ) ;
#18648=VERTEX_POINT ( 'NONE', #30160 ) ;
#18650=ADVANCED_FACE ( 'NONE', ( #17510 ), #17830, .T. ) ;
#18659=CARTESIAN_POINT ( 'NONE',  ( 48.00914065539375741, 22.93807716476589320, 48.47992731990171933 ) ) ;
#18662=CARTESIAN_POINT ( 'NONE',  ( 49.44739180854976013, 27.33456182964376779, 47.17133137409169308 ) ) ;
#18675=CARTESIAN_POINT ( 'NONE',  ( 48.34748475735720064, 24.70653309617948423, 49.49898713858203791 ) ) ;
#18681=CARTESIAN_POINT ( 'NONE',  ( 48.83862994770795041, 25.24118040159427068, 48.17861352429476085 ) ) ;
#18684=DIRECTION ( 'NONE',  ( 0.4441739386572013393, 0.2110602665713099402, 0.8707256032141217350 ) ) ;
#18689=CARTESIAN_POINT ( 'NONE',  ( 48.66895200406656130, 25.78420399681023056, 44.62753372671561181 ) ) ;
#18711=PRODUCT_DEFINITION ( 'UNKNOWN', '', #26528, #23589 ) ;
#18714=CARTESIAN_POINT ( 'NONE',  ( 44.91142894931555674, 27.29787913140503974, 45.63089057098605394 ) ) ;
#18722=CARTESIAN_POINT ( 'NONE',  ( 45.96182992765472619, 28.70087065737811827, 44.82232689504103007 ) ) ;
#18723=CARTESIAN_POINT ( 'NONE',  ( 47.20353132263855400, 25.45286309983299233, 45.01455027646041174 ) ) ;
#18732=CARTESIAN_POINT ( 'NONE',  ( 46.17891025898683921, 22.93807716476589675, 48.46582155994513386 ) ) ;
#18741=CARTESIAN_POINT ( 'NONE',  ( 46.79396160029377683, 22.86454579224780659, 45.03082974987060538 ) ) ;
#18743=CARTESIAN_POINT ( 'NONE',  ( 46.00908685603032922, 26.14624452788249087, 44.91496614357595263 ) ) ;
#18768=ADVANCED_FACE ( 'NONE', ( #23560 ), #13885, .F. ) ;
#18771=CARTESIAN_POINT ( 'NONE',  ( 45.96182992765471909, 25.90087065737812466, 44.82232689504102296 ) ) ;
#18786=CARTESIAN_POINT ( 'NONE',  ( 46.61910388458303345, 22.93328494799376216, 45.39920705986084215 ) ) ;
#18813=CARTESIAN_POINT ( 'NONE',  ( 46.71168188241476571, 25.16454579224780019, 44.57931415454905988 ) ) ;
#18814=CARTESIAN_POINT ( 'NONE',  ( 48.80717017713595141, 27.31952976649965592, 48.15820438821415195 ) ) ;
#18819=CARTESIAN_POINT ( 'NONE',  ( 48.74040444119073356, 29.48593875711943113, 48.49014004655320065 ) ) ;
#18825=CARTESIAN_POINT ( 'NONE',  ( 45.46000861347822308, 28.17287913140503619, 49.57397645940629616 ) ) ;
#18833=FACE_OUTER_BOUND ( 'NONE', #5038, .T. ) ;
#18852=CARTESIAN_POINT ( 'NONE',  ( 47.60921136374460616, 22.86454579224779948, 45.07316987100104200 ) ) ;
#18857=ORIENTED_EDGE ( 'NONE', *, *, #6962, .F. ) ;
#18878=VECTOR ( 'NONE', #16901, 1000.000000000000000 ) ;
#18882=CARTESIAN_POINT ( 'NONE',  ( 48.46535932150934656, 27.58954579807170759, 49.73005965046827015 ) ) ;
#18893=CARTESIAN_POINT ( 'NONE',  ( 46.02876340639226527, 26.21119643316632164, 44.95353858666495483 ) ) ;
#18903=CARTESIAN_POINT ( 'NONE',  ( 45.52675994804781112, 26.71155426599985461, 49.47108226228597516 ) ) ;
#18909=CARTESIAN_POINT ( 'NONE',  ( 48.83862994770794330, 28.65457786121581663, 48.17861352429476796 ) ) ;
#18979=CARTESIAN_POINT ( 'NONE',  ( 45.28286642839709231, 24.94289516297709852, 47.97516931882780966 ) ) ;
#18984=ADVANCED_FACE ( 'NONE', ( #16973 ), #19442, .F. ) ;
#18986=CARTESIAN_POINT ( 'NONE',  ( 49.20498434852767389, 29.54590370372963903, 46.77290885782220187 ) ) ;
#18992=CARTESIAN_POINT ( 'NONE',  ( 47.23302798462060537, 25.08121246473838184, 44.44659793406428605 ) ) ;
#19007=VERTEX_POINT ( 'NONE', #15340 ) ;
#19014=CARTESIAN_POINT ( 'NONE',  ( 48.35473289974373756, 22.80400562401889530, 45.11188864597615833 ) ) ;
#19035=AXIS2_PLACEMENT_3D ( 'NONE', #884, #5656, #8754 ) ;
#19042=VERTEX_POINT ( 'NONE', #5337 ) ;
#19044=CARTESIAN_POINT ( 'NONE',  ( 47.23302798462060537, 27.88121246473837544, 44.44659793406428605 ) ) ;
#19049=EDGE_CURVE ( 'NONE', #4178, #19268, #20415, .T. ) ;
#19052=CARTESIAN_POINT ( 'NONE',  ( 49.49063479933183629, 28.09951373492759430, 47.17357720316391578 ) ) ;
#19069=CARTESIAN_POINT ( 'NONE',  ( 48.83862994770794330, 26.55457786121582231, 48.17861352429476796 ) ) ;
#19073=ORIENTED_EDGE ( 'NONE', *, *, #12361, .F. ) ;
#19082=CARTESIAN_POINT ( 'NONE',  ( 46.24715649518903149, 23.24793988701932435, 47.51120522962222736 ) ) ;
#19110=CARTESIAN_POINT ( 'NONE',  ( 47.05339576314583638, 22.89977464660286444, 45.18578914680342251 ) ) ;
#19133=DIRECTION ( 'NONE',  ( -0.4544104193609917464, 0.000000000000000000, -0.8907924397839080966 ) ) ;
#19135=EDGE_CURVE ( 'NONE', #18170, #26418, #67, .T. ) ;
#19143=CARTESIAN_POINT ( 'NONE',  ( 49.44739180854976013, 26.67786309983298665, 47.17133137409169308 ) ) ;
#19150=CARTESIAN_POINT ( 'NONE',  ( 47.09785597605719687, 29.86454579224779948, 47.04930799450078638 ) ) ;
#19156=CARTESIAN_POINT ( 'NONE',  ( 45.73035263060504718, 26.53954579807170688, 44.36855633853329550 ) ) ;
#19164=CARTESIAN_POINT ( 'NONE',  ( 48.41187465712202709, 22.98765316579147111, 46.37900169951733886 ) ) ;
#19181=CARTESIAN_POINT ( 'NONE',  ( 45.47421713364555274, 22.88065857334294861, 45.99599230681428708 ) ) ;
#19182=ADVANCED_FACE ( 'NONE', ( #18114 ), #30567, .T. ) ;
#19186=ORIENTED_EDGE ( 'NONE', *, *, #8416, .F. ) ;
#19198=FACE_OUTER_BOUND ( 'NONE', #6422, .T. ) ;
#19202=ORIENTED_EDGE ( 'NONE', *, *, #522, .T. ) ;
#19215=CARTESIAN_POINT ( 'NONE',  ( 44.70507715278255745, 27.74951373492759643, 46.92503878583764987 ) ) ;
#19221=FACE_OUTER_BOUND ( 'NONE', #14238, .T. ) ;
#19247=EDGE_LOOP ( 'NONE', ( #21892, #9898, #25898, #9913, #13017 ) ) ;
#19248=CARTESIAN_POINT ( 'NONE',  ( 46.63102355535853150, 29.41114986400162934, 49.25898951255931735 ) ) ;
#19268=VERTEX_POINT ( 'NONE', #2501 ) ;
#19293=ORIENTED_EDGE ( 'NONE', *, *, #25730, .F. ) ;
#19304=CARTESIAN_POINT ( 'NONE',  ( 45.38854177497844944, 26.96952976649965450, 45.94041160078741370 ) ) ;
#19311=CARTESIAN_POINT ( 'NONE',  ( 48.93186884373860579, 29.49610055912359741, 48.21814732446082985 ) ) ;
#19318=CARTESIAN_POINT ( 'NONE',  ( 44.91142894931555674, 25.19787913140504543, 45.63089057098605394 ) ) ;
#19319=( BOUNDED_CURVE ( )  B_SPLINE_CURVE ( 2, ( #28580, #18225, #20860 ),
 .UNSPECIFIED., .F., .T. ) 
 B_SPLINE_CURVE_WITH_KNOTS ( ( 3, 3 ),
 ( 0.8928571440184154273, 0.8999500719669653037 ),
 .UNSPECIFIED. ) 
 CURVE ( )  GEOMETRIC_REPRESENTATION_ITEM ( )  RATIONAL_B_SPLINE_CURVE ( ( 0.9330127018922200755, 0.9330127057854562533, 0.9567921774292901249 ) ) 
 REPRESENTATION_ITEM ( '' )  );
#19327=LINE ( 'NONE', #29352, #7985 ) ;
#19328=DIRECTION ( 'NONE',  ( 0.8643320973212949010, 0.2419218955996663700, -0.4409124878812526460 ) ) ;
#19340=ORIENTED_EDGE ( 'NONE', *, *, #24432, .F. ) ;
#19350=VERTEX_POINT ( 'NONE', #22687 ) ;
#19355=FACE_OUTER_BOUND ( 'NONE', #20489, .T. ) ;
#19357=SURFACE_STYLE_USAGE ( .BOTH. , #9201 ) ;
#19370=CARTESIAN_POINT ( 'NONE',  ( 46.96268396749378127, 26.13121246473837544, 49.65201805493727960 ) ) ;
#19372=VECTOR ( 'NONE', #4329, 1000.000000000000114 ) ;
#19384=CARTESIAN_POINT ( 'NONE',  ( 45.38854177497844944, 25.56952976649965947, 45.94041160078741370 ) ) ;
#19392=DIRECTION ( 'NONE',  ( -0.05186525298099629866, -6.405245952009066254E-18, 0.9986540920324801229 ) ) ;
#19396=DIRECTION ( 'NONE',  ( 0.9761574614375593262, -0.2110602665713099957, 0.05069688703093822718 ) ) ;
#19404=CARTESIAN_POINT ( 'NONE',  ( 45.67943855254225127, 25.37287913140503548, 49.23573502124227730 ) ) ;
#19407=ORIENTED_EDGE ( 'NONE', *, *, #23285, .T. ) ;
#19411=VERTEX_POINT ( 'NONE', #19890 ) ;
#19422=ORIENTED_EDGE ( 'NONE', *, *, #19814, .T. ) ;
#19442=PLANE ( 'NONE',  #1303 ) ;
#19472=DIRECTION ( 'NONE',  ( 0.9986540920324801229, 1.233316085972235327E-16, 0.05186525298099630560 ) ) ;
#19475=CARTESIAN_POINT ( 'NONE',  ( 46.02876340639226527, 28.31119643316631240, 44.95353858666495483 ) ) ;
#19486=DIRECTION ( 'NONE',  ( 0.5442436726714897643, 6.721291001053910056E-17, -0.8389271868029121171 ) ) ;
#19489=CARTESIAN_POINT ( 'NONE',  ( 48.46535932150934656, 26.88954579807171186, 49.73005965046827015 ) ) ;
#19490=CARTESIAN_POINT ( 'NONE',  ( 46.31454563678332903, 22.93807716476589675, 48.55381333958629142 ) ) ;
#19491=DIRECTION ( 'NONE',  ( -0.09590798424311161585, 0.9774730502038649904, -0.1880108898004995421 ) ) ;
#19498=ORIENTED_EDGE ( 'NONE', *, *, #22968, .F. ) ;
#19545=CARTESIAN_POINT ( 'NONE',  ( 45.79384627280941089, 27.16618040159427139, 49.05938063676249072 ) ) ;
#19554=DIRECTION ( 'NONE',  ( 1.234978253042719660E-16, -1.000000000000000000, -1.109335647967047851E-31 ) ) ;
#19579=DIRECTION ( 'NONE',  ( -0.5442436726714893203, -1.289618226626749726E-16, 0.8389271868029124501 ) ) ;
#19644=CARTESIAN_POINT ( 'NONE',  ( 48.83862994770794330, 26.55457786121582231, 48.17861352429476796 ) ) ;
#19667=CARTESIAN_POINT ( 'NONE',  ( 46.76015065834239692, 23.11533908250407165, 47.22157799611917994 ) ) ;
#19676=CARTESIAN_POINT ( 'NONE',  ( 45.35708200440645044, 25.50457786121582515, 45.92000246470679770 ) ) ;
#19686=CARTESIAN_POINT ( 'NONE',  ( 48.94625023931840246, 27.37124452788248874, 46.10640627770149536 ) ) ;
#19687=( LENGTH_UNIT ( ) NAMED_UNIT ( * ) SI_UNIT ( .MILLI., .METRE. ) );
#19707=( BOUNDED_CURVE ( )  B_SPLINE_CURVE ( 2, ( #7743, #2654, #17741, #27763, #15293, #12841, #30389, #7912, #17911 ),
 .UNSPECIFIED., .F., .F. ) 
 B_SPLINE_CURVE_WITH_KNOTS ( ( 3, 2, 2, 2, 3 ),
 ( 0.6785714297327011257, 0.6904761904761904656, 0.7142857142857143016, 0.7380952380952381375, 0.7500000011612726336 ),
 .UNSPECIFIED. ) 
 CURVE ( )  GEOMETRIC_REPRESENTATION_ITEM ( )  RATIONAL_B_SPLINE_CURVE ( ( 0.9330127018922200755, 0.9330127084266224280, 1.000000000000000000, 0.8660254037844388186, 1.000000000000000000, 0.8660254037844388186, 1.000000000000000000, 0.9330126953578160576, 0.9330127018922200755 ) ) 
 REPRESENTATION_ITEM ( '' )  );
#19712=ORIENTED_EDGE ( 'NONE', *, *, #13494, .T. ) ;
#19727=CARTESIAN_POINT ( 'NONE',  ( 48.34748475735720774, 24.70653309617948423, 49.49898713858203791 ) ) ;
#19732=DIRECTION ( 'NONE',  ( -0.5319835227803602073, 0.2110602665713099124, 0.8200287161831869565 ) ) ;
#19801=DIRECTION ( 'NONE',  ( 0.01254734031692010705, 0.9702957262759969170, -0.2415962909928610070 ) ) ;
#19807=CARTESIAN_POINT ( 'NONE',  ( 46.45074414369405957, 22.93328494799376571, 48.64093701409239401 ) ) ;
#19808=CARTESIAN_POINT ( 'NONE',  ( 45.24946171279598417, 27.02124452788248732, 47.99220971130007030 ) ) ;
#19814=EDGE_CURVE ( 'NONE', #28677, #2146, #24973, .T. ) ;
#19837=CARTESIAN_POINT ( 'NONE',  ( 48.66895200406656130, 26.48420399681022630, 44.62753372671561181 ) ) ;
#19839=CARTESIAN_POINT ( 'NONE',  ( 45.35708200440645044, 26.90457786121582018, 45.92000246470679770 ) ) ;
#19850=CARTESIAN_POINT ( 'NONE',  ( 44.70507715278255034, 29.06291119454914806, 46.92503878583765697 ) ) ;
#19860=CARTESIAN_POINT ( 'NONE',  ( 49.49063479933183629, 28.09951373492759430, 47.17357720316391578 ) ) ;
#19864=STYLED_ITEM('',(#32543),#23129);
#19873=CARTESIAN_POINT ( 'NONE',  ( 45.96182992765472619, 28.00087065737811898, 44.82232689504102296 ) ) ;
#19890=CARTESIAN_POINT ( 'NONE',  ( 47.19823469859255738, 22.88065857334294861, 45.11653766655789610 ) ) ;
#19903=ORIENTED_EDGE ( 'NONE', *, *, #15354, .F. ) ;
#19909=CARTESIAN_POINT ( 'NONE',  ( 44.77595935755559253, 29.32712625747106827, 47.45364450062632500 ) ) ;
#19933=DIRECTION ( 'NONE',  ( 1.234978253042719660E-16, -1.000000000000000000, -1.109335647967047851E-31 ) ) ;
#19951=CIRCLE ( 'NONE', #2123, 1.799999999999998490 ) ;
#19967=DIRECTION ( 'NONE',  ( -0.3213166889719794583, -0.7071067811865470176, -0.6298853748009115572 ) ) ;
#19968=DIRECTION ( 'NONE',  ( 1.234978253042719660E-16, -1.000000000000000000, -1.109335647967047851E-31 ) ) ;
#19978=CARTESIAN_POINT ( 'NONE',  ( 46.99023568444673060, 29.23791119454914877, 49.12151524109405898 ) ) ;
#19993=ORIENTED_EDGE ( 'NONE', *, *, #4667, .F. ) ;
#19997=CARTESIAN_POINT ( 'NONE',  ( 45.65205965770037011, 22.98879437201065912, 47.30685321458182813 ) ) ;
#20000=EDGE_CURVE ( 'NONE', #22418, #26434, #29028, .T. ) ;
#20005=CARTESIAN_POINT ( 'NONE',  ( 48.18662509608405031, 27.19624452788248803, 49.18364984542562013 ) ) ;
#20017=CARTESIAN_POINT ( 'NONE',  ( 48.04075769285628894, 25.09624452788247950, 48.89770225776209855 ) ) ;
#20024=ORIENTED_EDGE ( 'NONE', *, *, #1711, .T. ) ;
#20045=CARTESIAN_POINT ( 'NONE',  ( 45.00053793792376666, 27.23655426599985674, 45.68869892245983522 ) ) ;
#20046=CARTESIAN_POINT ( 'NONE',  ( 45.96182992765471909, 15.77906836436399374, 44.82232689504101586 ) ) ;
#20058=ORIENTED_EDGE ( 'NONE', *, *, #21260, .F. ) ;
#20062=AXIS2_PLACEMENT_3D ( 'NONE', #14406, #14082, #26706 ) ;
#20073=CARTESIAN_POINT ( 'NONE',  ( 49.49063479933183629, 27.39951373492759856, 47.17357720316391578 ) ) ;
#20076=CARTESIAN_POINT ( 'NONE',  ( 45.43273841042186234, 29.36740968959510312, 48.63901743999641525 ) ) ;
#20078=EDGE_LOOP ( 'NONE', ( #26564, #17010, #320, #17133 ) ) ;
#20110=ORIENTED_EDGE ( 'NONE', *, *, #21792, .F. ) ;
#20139=CARTESIAN_POINT ( 'NONE',  ( 48.83862994770794330, 28.65457786121581663, 48.17861352429476796 ) ) ;
#20165=LINE ( 'NONE', #20811, #13904 ) ;
#20168=CARTESIAN_POINT ( 'NONE',  ( 48.91284552371730143, 28.79289516297709284, 46.12344667017377020 ) ) ;
#20187=CARTESIAN_POINT ( 'NONE',  ( 48.83862994770794330, 28.04118040159426428, 48.17861352429476796 ) ) ;
#20194=( BOUNDED_CURVE ( )  B_SPLINE_CURVE ( 3, ( #30845, #961, #28542, #26062 ),
 .UNSPECIFIED., .F., .F. ) 
 B_SPLINE_CURVE_WITH_KNOTS ( ( 4, 4 ),
 ( 1.099063246724954146, 1.220321128156879320 ),
 .UNSPECIFIED. ) 
 CURVE ( )  GEOMETRIC_REPRESENTATION_ITEM ( )  RATIONAL_B_SPLINE_CURVE ( ( 1.000000000000000000, 0.9987750858034805113, 0.9987750858034805113, 1.000000000000000000 ) ) 
 REPRESENTATION_ITEM ( '' )  );
#20205=CARTESIAN_POINT ( 'NONE',  ( 48.83862994770794330, 27.34118040159426499, 48.17861352429476796 ) ) ;
#20209=CARTESIAN_POINT ( 'NONE',  ( 47.63716429968717136, 27.49696019071910769, 49.58068632438585155 ) ) ;
#20215=CARTESIAN_POINT ( 'NONE',  ( 49.00637973737335074, 20.36454579224780304, 50.79063624159320511 ) ) ;
#20219=VECTOR ( 'NONE', #391, 1000.000000000000000 ) ;
#20221=CARTESIAN_POINT ( 'NONE',  ( 46.71168188241476571, 25.16454579224780019, 44.57931415454905988 ) ) ;
#20232=CARTESIAN_POINT ( 'NONE',  ( 45.35708200440645044, 28.39118040159425860, 45.92000246470679770 ) ) ;
#20244=EDGE_LOOP ( 'NONE', ( #10813, #7924, #14311, #24878 ) ) ;
#20256=EDGE_CURVE ( 'NONE', #19350, #11589, #1788, .T. ) ;
#20290=CARTESIAN_POINT ( 'NONE',  ( 47.26459061581830667, 23.10527865767145173, 46.48657494263439816 ) ) ;
#20294=DIRECTION ( 'NONE',  ( 0.3435019893673572078, -0.6546536707079771977, 0.6733757901270577273 ) ) ;
#20295=CARTESIAN_POINT ( 'NONE',  ( 49.49063479933183629, 29.41291119454914593, 47.17357720316391578 ) ) ;
#20302=CARTESIAN_POINT ( 'NONE',  ( 46.96819297411687444, 28.29253733014355632, 49.54594323136014822 ) ) ;
#20314=ORIENTED_EDGE ( 'NONE', *, *, #13669, .F. ) ;
#20316=EDGE_LOOP ( 'NONE', ( #8219, #9575, #25000, #22334 ) ) ;
#20320=CARTESIAN_POINT ( 'NONE',  ( 45.79384627280941089, 27.07957786121581734, 49.05938063676249072 ) ) ;
#20327=CARTESIAN_POINT ( 'NONE',  ( 48.34748475735720774, 24.70653309617948423, 49.49898713858203791 ) ) ;
#20341=CARTESIAN_POINT ( 'NONE',  ( 46.00908685603033632, 27.63284706826092929, 44.91496614357595263 ) ) ;
#20348=AXIS2_PLACEMENT_3D ( 'NONE', #12499, #27746, #7568 ) ;
#20355=CARTESIAN_POINT ( 'NONE',  ( 48.82187354100420151, 22.88065857334294861, 46.16985335424439540 ) ) ;
#20360=CARTESIAN_POINT ( 'NONE',  ( 44.87087493598345134, 27.35322093266652033, 48.18533415931919706 ) ) ;
#20367=LINE ( 'NONE', #15610, #525 ) ;
#20374=CARTESIAN_POINT ( 'NONE',  ( 49.59034552300744281, 29.16454579224780019, 47.24294646780535345 ) ) ;
#20384=CARTESIAN_POINT ( 'NONE',  ( 48.50303063523655567, 22.99884124225578574, 47.12228595530052644 ) ) ;
#20386=ORIENTED_EDGE ( 'NONE', *, *, #18192, .T. ) ;
#20390=CARTESIAN_POINT ( 'NONE',  ( 48.18662509608405031, 27.28284706826093142, 49.18364984542562013 ) ) ;
#20391=CARTESIAN_POINT ( 'NONE',  ( 45.79384627280941089, 28.47957786121581591, 49.05938063676249072 ) ) ;
#20393=DIRECTION ( 'NONE',  ( 0.9986540920324801229, 6.158269594508761132E-17, 0.05186525298099653458 ) ) ;
#20395=EDGE_LOOP ( 'NONE', ( #2237, #23250, #13201, #22083, #11427, #31301 ) ) ;
#20396=DIRECTION ( 'NONE',  ( 1.234978253042719660E-16, -1.000000000000000000, -1.109335647967047851E-31 ) ) ;
#20415=LINE ( 'NONE', #12895, #20219 ) ;
#20416=CARTESIAN_POINT ( 'NONE',  ( 48.37020515026796375, 24.86454579224779593, 49.54352682589573220 ) ) ;
#20419=CARTESIAN_POINT ( 'NONE',  ( 47.22751897799751220, 26.41988759933319031, 44.55267275764142454 ) ) ;
#20429=DIRECTION ( 'NONE',  ( 0.5442436726714893203, 6.721291001053903893E-17, -0.8389271868029124501 ) ) ;
#20432=ORIENTED_EDGE ( 'NONE', *, *, #21260, .T. ) ;
#20439=ADVANCED_FACE ( 'NONE', ( #26961 ), #2016, .F. ) ;
#20447=VERTEX_POINT ( 'NONE', #16461 ) ;
#20452=ORIENTED_EDGE ( 'NONE', *, *, #23084, .F. ) ;
#20453=DIRECTION ( 'NONE',  ( 0.4544104193609903586, 0.000000000000000000, 0.8907924397839087627 ) ) ;
#20461=CARTESIAN_POINT ( 'NONE',  ( 48.34748475735720064, 25.57255849996392172, 49.49898713858203791 ) ) ;
#20464=CARTESIAN_POINT ( 'NONE',  ( 46.00908685603034343, 25.44624452788248448, 44.91496614357595263 ) ) ;
#20474=CARTESIAN_POINT ( 'NONE',  ( 45.96182992765472619, 27.30087065737811969, 44.82232689504102296 ) ) ;
#20475=ORIENTED_EDGE ( 'NONE', *, *, #32056, .T. ) ;
#20476=ORIENTED_EDGE ( 'NONE', *, *, #224, .F. ) ;
#20489=EDGE_LOOP ( 'NONE', ( #8374, #5866, #5336, #30405 ) ) ;
#20491=CARTESIAN_POINT ( 'NONE',  ( 46.33059210211230550, 22.93807716476589675, 45.54522087609679204 ) ) ;
#20493=CARTESIAN_POINT ( 'NONE',  ( 47.09785597605719687, 29.86454579224779948, 47.04930799450078638 ) ) ;
#20494=CARTESIAN_POINT ( 'NONE',  ( 46.99218062947583974, 28.55956182964376211, 49.08406571254116102 ) ) ;
#20519=AXIS2_PLACEMENT_3D ( 'NONE', #7017, #27192, #7344 ) ;
#20527=CIRCLE ( 'NONE', #23153, 3.699999999999994849 ) ;
#20546=CARTESIAN_POINT ( 'NONE',  ( 47.98183884068953375, 25.10658484134872381, 44.68358619858262415 ) ) ;
#20554=CARTESIAN_POINT ( 'NONE',  ( 46.99023568444673060, 25.82451373492760283, 49.12151524109405898 ) ) ;
#20555=CARTESIAN_POINT ( 'NONE',  ( 45.35708200440645044, 29.70457786121581378, 45.92000246470679770 ) ) ;
#20558=VECTOR ( 'NONE', #16385, 1000.000000000000000 ) ;
#20569=CARTESIAN_POINT ( 'NONE',  ( 48.23388202445966044, 26.95087065737812182, 49.27628909396054979 ) ) ;
#20571=CARTESIAN_POINT ( 'NONE',  ( 44.99489604499470374, 22.84434098701873594, 46.61610178023796891 ) ) ;
#20578=( BOUNDED_CURVE ( )  B_SPLINE_CURVE ( 2, ( #7964, #15978, #25985, #3497, #13525, #4593, #9076, #11375, #12320, #26474, #24782, #19850, #11220, #22147, #22317, #32180, #16609, #24003, #18909, #24618, #23842, #14783, #1358, #14616, #2300, #32341, #6456, #16455, #3664, #7224, #2138, #13690, #9851, #6290, #9692, #14007, #21365, #21208, #31248, #29101, #19686, #29881, #13845, #12156, #28773, #8911, #7397, #26313, #17393, #8749, #23691, #1193, #1519, #31406, #19069, #17224, #29714, #16295, #11540, #27238, #26630, #18743, #3826, #31570, #28943, #3986, #4766, #21532, #6616, #4928, #10678, #30533, #10182, #28064, #27735, #5253, #5576, #15262, #15574, #15422, #20017 ),
 .UNSPECIFIED., .F., .F. ) 
 B_SPLINE_CURVE_WITH_KNOTS ( ( 3, 2, 2, 2, 2, 2, 2, 2, 2, 2, 2, 2, 2, 2, 2, 2, 2, 2, 2, 2, 2, 2, 2, 2, 2, 2, 2, 2, 2, 2, 2, 2, 2, 2, 2, 2, 2, 2, 2, 2, 3 ),
 ( 0.04723643264279250159, 0.04761904761904761640, 0.07142857142857142461, 0.09523809523809523281, 0.1190476190476190410, 0.1428571428571428492, 0.1666666666666666574, 0.1904761904761904656, 0.2142857142857142738, 0.2380952380952381098, 0.2619047619047619180, 0.2857142857142856984, 0.3095238095238095344, 0.3333333333333333148, 0.3571428571428571508, 0.3809523809523809312, 0.4047619047619047672, 0.4285714285714285476, 0.4523809523809523836, 0.4761904761904762196, 0.5000000000000000000, 0.5238095238095238360, 0.5476190476190476719, 0.5714285714285713969, 0.5952380952380951218, 0.6190476190476190688, 0.6428571428571429047, 0.6666666666666666297, 0.6904761904761904656, 0.7142857142857143016, 0.7380952380952381375, 0.7619047619047618625, 0.7857142857142856984, 0.8095238095238095344, 0.8333333333333333703, 0.8571428571428570953, 0.8809523809523809312, 0.9047619047619047672, 0.9285714285714286031, 0.9523809523809523281, 0.9642857142857166330 ),
 .UNSPECIFIED. ) 
 CURVE ( )  GEOMETRIC_REPRESENTATION_ITEM ( )  RATIONAL_B_SPLINE_CURVE ( ( 0.9957632973360193152, 0.9978470511481081218, 1.000000000000000000, 0.8660254037844387076, 1.000000000000000000, 0.8660254037844387076, 1.000000000000000000, 0.8660254037844387076, 1.000000000000000000, 0.8660254037844387076, 1.000000000000000000, 0.8660254037844387076, 1.000000000000000000, 0.8660254037844387076, 1.000000000000000000, 0.8660254037844387076, 1.000000000000000000, 0.8660254037844387076, 1.000000000000000000, 0.8660254037844387076, 1.000000000000000000, 0.8660254037844387076, 1.000000000000000000, 0.8660254037844387076, 1.000000000000000000, 0.8660254037844387076, 1.000000000000000000, 0.8660254037844387076, 1.000000000000000000, 0.8660254037844387076, 1.000000000000000000, 0.8660254037844387076, 1.000000000000000000, 0.8660254037844387076, 1.000000000000000000, 0.8660254037844387076, 1.000000000000000000, 0.8660254037844387076, 1.000000000000000000, 0.8660254037844387076, 1.000000000000000000, 0.8660254037844387076, 1.000000000000000000, 0.8660254037844387076, 1.000000000000000000, 0.8660254037844387076, 1.000000000000000000, 0.8660254037844387076, 1.000000000000000000, 0.8660254037844387076, 1.000000000000000000, 0.8660254037844387076, 1.000000000000000000, 0.8660254037844387076, 1.000000000000000000, 0.8660254037844387076, 1.000000000000000000, 0.8660254037844387076, 1.000000000000000000, 0.8660254037844387076, 1.000000000000000000, 0.8660254037844387076, 1.000000000000000000, 0.8660254037844387076, 1.000000000000000000, 0.8660254037844387076, 1.000000000000000000, 0.8660254037844387076, 1.000000000000000000, 0.8660254037844387076, 1.000000000000000000, 0.8660254037844387076, 1.000000000000000000, 0.8660254037844387076, 1.000000000000000000, 0.8660254037844387076, 1.000000000000000000, 0.8660254037844387076, 1.000000000000000000, 0.9330127018922058646, 0.9330127018922192983 ) ) 
 REPRESENTATION_ITEM ( '' )  );
#20606=CARTESIAN_POINT ( 'NONE',  ( 47.22751897799751220, 27.81988759933318889, 44.55267275764142454 ) ) ;
#20614=CARTESIAN_POINT ( 'NONE',  ( 45.97377588299919893, 23.04411619146718238, 46.99092872297675427 ) ) ;
#20625=CARTESIAN_POINT ( 'NONE',  ( 47.25101359556892078, 23.12036939723557083, 46.81322240026007364 ) ) ;
#20640=ORIENTED_EDGE ( 'NONE', *, *, #31304, .T. ) ;
#20652=CARTESIAN_POINT ( 'NONE',  ( 48.73394074504988538, 22.89977464660286444, 47.94256374451057212 ) ) ;
#20655=CARTESIAN_POINT ( 'NONE',  ( 46.02876340639226527, 26.86789516297709568, 44.95353858666495483 ) ) ;
#20661=DIRECTION ( 'NONE',  ( 0.8389271868029106738, 0.000000000000000000, 0.5442436726714922068 ) ) ;
#20673=CARTESIAN_POINT ( 'NONE',  ( 48.40186567930497574, 25.41618040159426783, 45.03923535223908203 ) ) ;
#20676=CARTESIAN_POINT ( 'NONE',  ( 47.09785597605719687, 29.86454579224779948, 47.04930799450078638 ) ) ;
#20716=CARTESIAN_POINT ( 'NONE',  ( 48.83862994770794330, 26.64118040159426570, 48.17861352429476796 ) ) ;
#20719=CARTESIAN_POINT ( 'NONE',  ( 46.00908685603034343, 27.54624452788248590, 44.91496614357595263 ) ) ;
#20729=CARTESIAN_POINT ( 'NONE',  ( 47.09785597605719687, 23.12036939723557083, 47.04930799450080059 ) ) ;
#20741=CARTESIAN_POINT ( 'NONE',  ( 46.42154359715483736, 22.84434098701873950, 45.01148816392849739 ) ) ;
#20748=CARTESIAN_POINT ( 'NONE',  ( 47.14446097802335345, 29.60550614078797693, 44.99079124510692651 ) ) ;
#20789=CARTESIAN_POINT ( 'NONE',  ( 48.40186567930498285, 25.32957786121582089, 45.03923535223908203 ) ) ;
#20793=VERTEX_POINT ( 'NONE', #29227 ) ;
#20796=LINE ( 'NONE', #30984, #17439 ) ;
#20811=CARTESIAN_POINT ( 'NONE',  ( 48.14727188781975542, 19.96454579224779380, 49.10650501410607660 ) ) ;
#20813=CARTESIAN_POINT ( 'NONE',  ( 45.38854177497844944, 27.62622849631042499, 45.94041160078741370 ) ) ;
#20818=EDGE_CURVE ( 'NONE', #26923, #3283, #4602, .T. ) ;
#20838=ORIENTED_EDGE ( 'NONE', *, *, #936, .T. ) ;
#20853=EDGE_CURVE ( 'NONE', #11589, #22710, #13686, .T. ) ;
#20855=CARTESIAN_POINT ( 'NONE',  ( 45.96182992765472619, 27.30087065737811969, 44.82232689504102296 ) ) ;
#20860=CARTESIAN_POINT ( 'NONE',  ( 46.71168188241476571, 25.16454579224780019, 44.57931415454905988 ) ) ;
#20868=CARTESIAN_POINT ( 'NONE',  ( 48.23388202445966044, 28.22822092656774373, 49.27628909396054979 ) ) ;
#20870=CARTESIAN_POINT ( 'NONE',  ( 45.73035263060504718, 27.93954579807170546, 44.36855633853329550 ) ) ;
#20872=CARTESIAN_POINT ( 'NONE',  ( 48.83862994770794330, 27.95457786121581734, 48.17861352429476796 ) ) ;
#20898=CARTESIAN_POINT ( 'NONE',  ( 46.84209603737756566, 23.10527845304106620, 46.54793520446708044 ) ) ;
#20915=ORIENTED_EDGE ( 'NONE', *, *, #11930, .T. ) ;
#20921=CARTESIAN_POINT ( 'NONE',  ( 48.83059987400640978, 27.55948166895303686, 48.97189179988552610 ) ) ;
#20923=CARTESIAN_POINT ( 'NONE',  ( 48.23388202445966044, 26.12822092656774586, 49.27628909396054979 ) ) ;
#20947=CARTESIAN_POINT ( 'NONE',  ( 48.50303063523655567, 22.99884124225578574, 47.12228595530052644 ) ) ;
#20972=CARTESIAN_POINT ( 'NONE',  ( 46.99218062947583974, 25.75956182964376495, 49.08406571254116102 ) ) ;
#20990=CARTESIAN_POINT ( 'NONE',  ( 48.04075769285628894, 25.18284706826092290, 48.89770225776209145 ) ) ;
#21002=ORIENTED_EDGE ( 'NONE', *, *, #12836, .T. ) ;
#21012=CARTESIAN_POINT ( 'NONE',  ( 48.14727188781975542, 22.80400562401890241, 49.10650501410607660 ) ) ;
#21027=CARTESIAN_POINT ( 'NONE',  ( 50.10320668408830613, 29.10621246473837331, 47.20539118556276037 ) ) ;
#21061=CARTESIAN_POINT ( 'NONE',  ( 49.70065004996131819, 24.90951171049934842, 46.59606017514272480 ) ) ;
#21073=AXIS2_PLACEMENT_3D ( 'NONE', #5821, #2863, #17958 ) ;
#21082=CARTESIAN_POINT ( 'NONE',  ( 45.96182992765471909, 27.17822092656774302, 44.82232689504102296 ) ) ;
#21089=VERTEX_POINT ( 'NONE', #1072 ) ;
#21095=CARTESIAN_POINT ( 'NONE',  ( 47.18886224597662249, 22.92747281079970278, 45.29700218990083016 ) ) ;
#21119=CARTESIAN_POINT ( 'NONE',  ( 48.78406556707242459, 22.93807716476589675, 47.13688154746047587 ) ) ;
#21124=CARTESIAN_POINT ( 'NONE',  ( 46.99218062947583974, 27.15956182964376708, 49.08406571254116102 ) ) ;
#21138=CARTESIAN_POINT ( 'NONE',  ( 47.09785597605719687, 23.12036939723557083, 47.04930799450080059 ) ) ;
#21141=VERTEX_POINT ( 'NONE', #3206 ) ;
#21166=CARTESIAN_POINT ( 'NONE',  ( 48.02750443086935661, 29.17693647873863583, 44.73249073240486240 ) ) ;
#21179=CARTESIAN_POINT ( 'NONE',  ( 48.73570333863616355, 28.52287913140503761, 44.52463952959527660 ) ) ;
#21206=ADVANCED_FACE ( 'NONE', ( #18097 ), #15636, .T. ) ;
#21208=CARTESIAN_POINT ( 'NONE',  ( 46.00908685603033632, 27.54624452788248590, 44.91496614357595263 ) ) ;
#21217=CARTESIAN_POINT ( 'NONE',  ( 48.39288112930642427, 29.59930898745696126, 45.41613349220816076 ) ) ;
#21260=EDGE_CURVE ( 'NONE', #7293, #26705, #26629, .T. ) ;
#21281=CARTESIAN_POINT ( 'NONE',  ( 47.37889090789306579, 23.12036939723557083, 47.06390358666074292 ) ) ;
#21284=CARTESIAN_POINT ( 'NONE',  ( 48.16694854572211426, 29.36119643316632022, 49.14507740233662503 ) ) ;
#21332=CARTESIAN_POINT ( 'NONE',  ( 48.10030433005226769, 29.45850404830353142, 49.01443330185325920 ) ) ;
#21338=CARTESIAN_POINT ( 'NONE',  ( 45.46000861347822308, 26.77287913140504116, 49.57397645940629616 ) ) ;
#21347=CARTESIAN_POINT ( 'NONE',  ( 48.83862994770794330, 28.74118040159426002, 48.17861352429476796 ) ) ;
#21353=CARTESIAN_POINT ( 'NONE',  ( 47.63716429968717136, 26.79696019071911195, 49.58068632438585155 ) ) ;
#21365=CARTESIAN_POINT ( 'NONE',  ( 45.35708200440645044, 27.60457786121581947, 45.92000246470680480 ) ) ;
#21390=VECTOR ( 'NONE', #29224, 1000.000000000000114 ) ;
#21408=CARTESIAN_POINT ( 'NONE',  ( 47.32587910665017006, 22.95310733321322516, 45.42502988274431175 ) ) ;
#21429=VECTOR ( 'NONE', #23942, 1000.000000000000227 ) ;
#21436=VECTOR ( 'NONE', #4983, 1000.000000000000000 ) ;
#21442=CARTESIAN_POINT ( 'NONE',  ( 45.28286642839709231, 28.48619643316631311, 47.97516931882780966 ) ) ;
#21448=CARTESIAN_POINT ( 'NONE',  ( 48.81899109467476450, 29.57820558303529168, 45.85849491930559196 ) ) ;
#21453=CARTESIAN_POINT ( 'NONE',  ( 46.96268396749378127, 28.23121246473837331, 49.65201805493727960 ) ) ;
#21455=CARTESIAN_POINT ( 'NONE',  ( 46.46324171377475665, 22.99884124225578574, 48.31483337462398708 ) ) ;
#21482=CARTESIAN_POINT ( 'NONE',  ( 49.40414881150629611, 19.96454579224779380, 47.16908566558144855 ) ) ;
#21493=ORIENTED_EDGE ( 'NONE', *, *, #29944, .T. ) ;
#21505=CIRCLE ( 'NONE', #5790, 2.800000000000002043 ) ;
#21506=CARTESIAN_POINT ( 'NONE',  ( 49.28428300279882990, 29.74787913140503903, 48.46772541801551171 ) ) ;
#21517=CARTESIAN_POINT ( 'NONE',  ( 47.20547626766766314, 28.97451373492759075, 44.97710074790751378 ) ) ;
#21531=CARTESIAN_POINT ( 'NONE',  ( 45.42003181263716272, 22.93807716476589675, 46.80027486889689214 ) ) ;
#21532=CARTESIAN_POINT ( 'NONE',  ( 48.18662509608405742, 25.79624452788248945, 49.18364984542562013 ) ) ;
#21540=DIRECTION ( 'NONE',  ( 0.8389271868029124501, 1.036056831587903609E-16, 0.5442436726714893203 ) ) ;
#21548=CARTESIAN_POINT ( 'NONE',  ( 48.75540398364718442, 22.86454579224779948, 48.16909669137300654 ) ) ;
#21609=CARTESIAN_POINT ( 'NONE',  ( 45.38854177497844944, 29.76952976649964100, 45.94041160078741370 ) ) ;
#21622=CARTESIAN_POINT ( 'NONE',  ( 45.46000861347822308, 25.37287913140504614, 49.57397645940629616 ) ) ;
#21624=CARTESIAN_POINT ( 'NONE',  ( 46.48525799733394592, 23.04411619146717882, 47.99360027521537830 ) ) ;
#21650=CARTESIAN_POINT ( 'NONE',  ( 45.96182992765471198, 25.16454579224780019, 44.82232689504101586 ) ) ;
#21684=CARTESIAN_POINT ( 'NONE',  ( 48.18662509608405031, 28.68284706826092290, 49.18364984542562013 ) ) ;
#21685=ORIENTED_EDGE ( 'NONE', *, *, #14489, .F. ) ;
#21686=AXIS2_PLACEMENT_3D ( 'NONE', #23897, #16825, #24221 ) ;
#21696=CARTESIAN_POINT ( 'NONE',  ( 45.00053793792376666, 25.25920399681023198, 45.68869892245983522 ) ) ;
#21699=CARTESIAN_POINT ( 'NONE',  ( 48.59452595530246555, 24.93986642951281496, 44.74225815255415739 ) ) ;
#21719=CARTESIAN_POINT ( 'NONE',  ( 46.93148653487033073, 29.42016659326356987, 49.29260710712500781 ) ) ;
#21746=DIRECTION ( 'NONE',  ( 0.8907924397839086517, 1.100109291107994064E-16, -0.4544104193609905251 ) ) ;
#21754=ORIENTED_EDGE ( 'NONE', *, *, #18245, .T. ) ;
#21769=CARTESIAN_POINT ( 'NONE',  ( 48.37829923888483563, 27.49452976649965308, 45.07556196625585443 ) ) ;
#21784=CARTESIAN_POINT ( 'NONE',  ( 49.41945501136223839, 24.96454579807171470, 45.86501535757901848 ) ) ;
#21787=CARTESIAN_POINT ( 'NONE',  ( 46.82137942583813128, 14.98691807112498964, 46.50732389770341513 ) ) ;
#21792=EDGE_CURVE ( 'NONE', #14642, #1960, #5542, .T. ) ;
#21802=EDGE_LOOP ( 'NONE', ( #15160, #24970, #6665 ) ) ;
#21804=( GEOMETRIC_REPRESENTATION_CONTEXT ( 3 ) GLOBAL_UNCERTAINTY_ASSIGNED_CONTEXT ( ( #8498 ) ) GLOBAL_UNIT_ASSIGNED_CONTEXT ( ( #19687, #21979, #32010 ) ) REPRESENTATION_CONTEXT ( 'NONE', 'WORKASPACE' ) );
#21820=DIRECTION ( 'NONE',  ( 1.234978253042719660E-16, -1.000000000000000000, -1.109335647967047851E-31 ) ) ;
#21822=EDGE_CURVE ( 'NONE', #13392, #5398, #24880, .T. ) ;
#21835=CARTESIAN_POINT ( 'NONE',  ( 44.09250526802607340, 25.95621246473837829, 46.89322480343881949 ) ) ;
#21846=CARTESIAN_POINT ( 'NONE',  ( 44.70507715278255745, 29.84951373492758719, 46.92503878583764987 ) ) ;
#21861=CARTESIAN_POINT ( 'NONE',  ( 46.94177278499491734, 25.43121246473836550, 50.05465870253188854 ) ) ;
#21869=ORIENTED_EDGE ( 'NONE', *, *, #14228, .T. ) ;
#21877=CARTESIAN_POINT ( 'NONE',  ( 45.66249254611258124, 29.37705119628220274, 48.83685427499938214 ) ) ;
#21881=EDGE_CURVE ( 'NONE', #22685, #7056, #4084, .T. ) ;
#21892=ORIENTED_EDGE ( 'NONE', *, *, #12015, .T. ) ;
#21894=VECTOR ( 'NONE', #17356, 1000.000000000000000 ) ;
#21930=CARTESIAN_POINT ( 'NONE',  ( 48.37829923888483563, 26.79452976649965379, 45.07556196625585443 ) ) ;
#21931=ORIENTED_EDGE ( 'NONE', *, *, #5359, .T. ) ;
#21939=CARTESIAN_POINT ( 'NONE',  ( 47.60933809039193676, 23.04411619146718238, 48.05197954673941751 ) ) ;
#21942=CARTESIAN_POINT ( 'NONE',  ( 48.46535932150934656, 26.18954579807170902, 49.73005965046827015 ) ) ;
#21958=EDGE_CURVE ( 'NONE', #3511, #1048, #25848, .T. ) ;
#21979=( NAMED_UNIT ( * ) PLANE_ANGLE_UNIT ( ) SI_UNIT ( $, .RADIAN. ) );
#21992=CARTESIAN_POINT ( 'NONE',  ( 46.96268396749378127, 25.43121246473837971, 49.65201805493727960 ) ) ;
#22005=CARTESIAN_POINT ( 'NONE',  ( 48.16694854572211426, 25.16119643316632093, 49.14507740233662503 ) ) ;
#22010=VECTOR ( 'NONE', #8043, 1000.000000000000114 ) ;
#22023=CARTESIAN_POINT ( 'NONE',  ( 45.97377588299919893, 23.04411619146718238, 46.99092872297675427 ) ) ;
#22058=ORIENTED_EDGE ( 'NONE', *, *, #28830, .F. ) ;
#22070=CARTESIAN_POINT ( 'NONE',  ( 48.23388202445966755, 26.25087065737812253, 49.27628909396054979 ) ) ;
#22082=ADVANCED_FACE ( 'NONE', ( #22622 ), #22681, .T. ) ;
#22083=ORIENTED_EDGE ( 'NONE', *, *, #14228, .F. ) ;
#22093=CARTESIAN_POINT ( 'NONE',  ( 45.84097905237065618, 22.80400562401890241, 48.98672734302541443 ) ) ;
#22110=CARTESIAN_POINT ( 'NONE',  ( 48.73570333863616355, 25.02287913140504827, 44.52463952959527660 ) ) ;
#22111=CARTESIAN_POINT ( 'NONE',  ( 46.79153437246152691, 23.10527845304106265, 47.52148899368456370 ) ) ;
#22132=AXIS2_PLACEMENT_3D ( 'NONE', #24739, #19968, #17173 ) ;
#22138=CARTESIAN_POINT ( 'NONE',  ( 48.18662509608405031, 25.79624452788248945, 49.18364984542562013 ) ) ;
#22142=ORIENTED_EDGE ( 'NONE', *, *, #28673, .F. ) ;
#22147=CARTESIAN_POINT ( 'NONE',  ( 46.00908685603033632, 28.94624452788248092, 44.91496614357595263 ) ) ;
#22160=CARTESIAN_POINT ( 'NONE',  ( 45.24946171279598417, 27.10784706826093071, 47.99220971130007740 ) ) ;
#22161=CARTESIAN_POINT ( 'NONE',  ( 48.86248627303584158, 22.86454579224779948, 46.10725065118596433 ) ) ;
#22173=CARTESIAN_POINT ( 'NONE',  ( 45.35708200440645044, 26.99118040159426357, 45.92000246470679770 ) ) ;
#22177=CARTESIAN_POINT ( 'NONE',  ( 45.52675994804781112, 27.41155426599985034, 49.47108226228597516 ) ) ;
#22184=DIRECTION ( 'NONE',  ( -0.9761574614375592152, 0.2110602665713099957, -0.05069688703093822024 ) ) ;
#22188=LINE ( 'NONE', #10060, #22620 ) ;
#22195=CARTESIAN_POINT ( 'NONE',  ( 46.55854765242722948, 27.26960992152947938, 44.51792966461572121 ) ) ;
#22210=ORIENTED_EDGE ( 'NONE', *, *, #3712, .F. ) ;
#22251=CARTESIAN_POINT ( 'NONE',  ( 45.00053793792376666, 25.83655426599985816, 45.68869892245983522 ) ) ;
#22273=CARTESIAN_POINT ( 'NONE',  ( 46.00908685603034343, 26.84624452788248661, 44.91496614357595263 ) ) ;
#22280=CARTESIAN_POINT ( 'NONE',  ( 47.12873084020358760, 29.59659471728345181, 44.98158648324610454 ) ) ;
#22295=( BOUNDED_SURFACE ( )  B_SPLINE_SURFACE ( 1, 2, ( 
 ( #11708, #7103, #26633, #4145, #29257, #4638, #14175, #14659, #21699, #24665, #27289, #1850, #19727 ),
 ( #2343, #21861, #19404, #6940, #24832, #16938, #4479, #31731, #14497, #12199, #24491, #7271, #17266 ) ),
 .UNSPECIFIED., .F., .F., .F. ) 
 B_SPLINE_SURFACE_WITH_KNOTS ( ( 2, 2 ),
 ( 3, 2, 2, 2, 2, 2, 3 ),
 ( 0.000000000000000000, 1.000000000000000000 ),
 ( 0.000000000000000000, 0.1666666666666666574, 0.3333333333333333148, 0.5000000000000000000, 0.6666666666666666297, 0.8333333333333333703, 1.000000000000000000 ),
 .UNSPECIFIED. ) 
 GEOMETRIC_REPRESENTATION_ITEM ( )  RATIONAL_B_SPLINE_SURFACE ( (
 ( 1.000000000000000000, 0.8660254037844387076, 1.000000000000000000, 0.8660254037844387076, 1.000000000000000000, 0.8660254037844387076, 1.000000000000000000, 0.8660254037844387076, 1.000000000000000000, 0.8660254037844387076, 1.000000000000000000, 0.8660254037844387076, 1.000000000000000000),
 ( 1.000000000000000000, 0.8660254037844387076, 1.000000000000000000, 0.8660254037844387076, 1.000000000000000000, 0.8660254037844387076, 1.000000000000000000, 0.8660254037844387076, 1.000000000000000000, 0.8660254037844387076, 1.000000000000000000, 0.8660254037844387076, 1.000000000000000000) ) ) 
 REPRESENTATION_ITEM ( '' )  SURFACE ( )  );
#22306=CARTESIAN_POINT ( 'NONE',  ( 49.40414881150629611, 22.80400562401889530, 47.16908566558144855 ) ) ;
#22307=CARTESIAN_POINT ( 'NONE',  ( 47.20547626766766314, 27.48791119454915233, 44.97710074790751378 ) ) ;
#22311=ORIENTED_EDGE ( 'NONE', *, *, #18192, .F. ) ;
#22317=CARTESIAN_POINT ( 'NONE',  ( 47.20547626766765603, 28.88791119454915091, 44.97710074790751378 ) ) ;
#22324=CARTESIAN_POINT ( 'NONE',  ( 44.70507715278255034, 29.14951373492759146, 46.92503878583765697 ) ) ;
#22330=( GEOMETRIC_REPRESENTATION_CONTEXT ( 3 ) GLOBAL_UNCERTAINTY_ASSIGNED_CONTEXT ( ( #23270 ) ) GLOBAL_UNIT_ASSIGNED_CONTEXT ( ( #13173, #11026, #1156 ) ) REPRESENTATION_CONTEXT ( 'NONE', 'WORKASPACE' ) );
#22334=ORIENTED_EDGE ( 'NONE', *, *, #6185, .F. ) ;
#22365=CARTESIAN_POINT ( 'NONE',  ( 48.40186567930498285, 28.91618040159426073, 45.03923535223908203 ) ) ;
#22418=VERTEX_POINT ( 'NONE', #14883 ) ;
#22428=CARTESIAN_POINT ( 'NONE',  ( 46.00908685603034343, 26.14624452788249087, 44.91496614357595263 ) ) ;
#22436=ORIENTED_EDGE ( 'NONE', *, *, #1711, .F. ) ;
#22439=CARTESIAN_POINT ( 'NONE',  ( 45.00053793792376666, 28.05920399681022559, 45.68869892245983522 ) ) ;
#22447=ORIENTED_EDGE ( 'NONE', *, *, #7036, .F. ) ;
#22449=CARTESIAN_POINT ( 'NONE',  ( 45.41164638504195494, 22.93807716476589675, 46.96173444154113241 ) ) ;
#22453=ORIENTED_EDGE ( 'NONE', *, *, #31028, .T. ) ;
#22455=( NAMED_UNIT ( * ) PLANE_ANGLE_UNIT ( ) SI_UNIT ( $, .RADIAN. ) );
#22459=CARTESIAN_POINT ( 'NONE',  ( 45.81741271322955100, 29.20122849631042072, 49.02305402274571122 ) ) ;
#22486=EDGE_CURVE ( 'NONE', #24034, #28026, #31514, .T. ) ;
#22494=CARTESIAN_POINT ( 'NONE',  ( 48.94625023931840957, 25.35784706826093426, 46.10640627770150246 ) ) ;
#22498=CARTESIAN_POINT ( 'NONE',  ( 46.27991722120741258, 29.86454579224779948, 45.44588160288975587 ) ) ;
#22499=APPLICATION_CONTEXT ( 'automotive_design' ) ;
#22507=DIRECTION ( 'NONE',  ( -0.6298853748009114462, 0.7071067811865472397, 0.3213166889719795694 ) ) ;
#22524=ORIENTED_EDGE ( 'NONE', *, *, #14891, .F. ) ;
#22527=CARTESIAN_POINT ( 'NONE',  ( 46.00908685603034343, 28.33284706826092503, 44.91496614357594552 ) ) ;
#22531=EDGE_CURVE ( 'NONE', #21089, #8039, #29201, .T. ) ;
#22550=ORIENTED_EDGE ( 'NONE', *, *, #31113, .T. ) ;
#22571=EDGE_CURVE ( 'NONE', #1960, #11279, #751, .T. ) ;
#22600=CARTESIAN_POINT ( 'NONE',  ( 48.69396222501143967, 22.86454579224779948, 45.77688862270734660 ) ) ;
#22601=CARTESIAN_POINT ( 'NONE',  ( 47.09785597605719687, 23.12036939723557083, 47.04930799450080059 ) ) ;
#22603=CARTESIAN_POINT ( 'NONE',  ( 45.79384627280941089, 27.07957786121582444, 49.05938063676249072 ) ) ;
#22608=CARTESIAN_POINT ( 'NONE',  ( 48.37020528065356473, 25.16454579224780019, 49.54352675938351069 ) ) ;
#22620=VECTOR ( 'NONE', #4472, 1000.000000000000000 ) ;
#22622=FACE_OUTER_BOUND ( 'NONE', #17127, .T. ) ;
#22629=CARTESIAN_POINT ( 'NONE',  ( 48.18662509608405031, 25.09624452788248661, 49.18364984542562013 ) ) ;
#22650=CARTESIAN_POINT ( 'NONE',  ( 45.35708200440645044, 28.39118040159425860, 45.92000246470680480 ) ) ;
#22666=CARTESIAN_POINT ( 'NONE',  ( 45.35708200440645044, 25.59118040159426855, 45.92000246470679770 ) ) ;
#22678=CARTESIAN_POINT ( 'NONE',  ( 45.37804019580246973, 22.89977464660286444, 47.76827453631080544 ) ) ;
#22681=B_SPLINE_SURFACE_WITH_KNOTS ( 'NONE', 3, 3, ( 
 ( #7698, #12467, #5235, #5072, #9834, #22449 ),
 ( #29862, #19667, #2769, #29697, #7377, #32484 ),
 ( #30187, #17369, #145, #10001, #19997, #17694 ),
 ( #7204, #7861, #17199, #7544, #5400, #27218 ),
 ( #10163, #4745, #15246, #30025, #27556, #304 ),
 ( #17538, #25257, #15083, #12797, #22781, #10324 ) ),
 .UNSPECIFIED., .F., .F., .F.,
 ( 4, 2, 4 ),
 ( 4, 2, 4 ),
 ( 0.000000000000000000, 0.5000000000000000000, 1.000000000000000000 ),
 ( 0.000000000000000000, 0.5000000000000000000, 1.000000000000000000 ),
 .UNSPECIFIED. ) ;
#22685=VERTEX_POINT ( 'NONE', #4174 ) ;
#22687=CARTESIAN_POINT ( 'NONE',  ( 47.17209261226641104, 29.58954579224849368, 44.97563639035409011 ) ) ;
#22693=( BOUNDED_CURVE ( )  B_SPLINE_CURVE ( 2, ( #27598, #2489, #20045, #12516, #20360, #22177, #5114, #20209, #4791 ),
 .UNSPECIFIED., .F., .F. ) 
 B_SPLINE_CURVE_WITH_KNOTS ( ( 3, 2, 2, 2, 3 ),
 ( 0.3928571416958702711, 0.4047619047619047672, 0.4285714285714286031, 0.4523809523809523281, 0.4642857131244416125 ),
 .UNSPECIFIED. ) 
 CURVE ( )  GEOMETRIC_REPRESENTATION_ITEM ( )  RATIONAL_B_SPLINE_CURVE ( ( 0.9330127018922200755, 0.9330126953578163906, 1.000000000000000000, 0.8660254037844387076, 1.000000000000000000, 0.8660254037844387076, 1.000000000000000000, 0.9330127084266226500, 0.9330127018922199644 ) ) 
 REPRESENTATION_ITEM ( '' )  );
#22700=CARTESIAN_POINT ( 'NONE',  ( 45.35708200440645044, 25.59118040159426855, 45.92000246470679770 ) ) ;
#22710=VERTEX_POINT ( 'NONE', #3690 ) ;
#22735=CYLINDRICAL_SURFACE ( 'NONE', #11500, 4.200000000000000178 ) ;
#22742=ORIENTED_EDGE ( 'NONE', *, *, #26524, .F. ) ;
#22761=FACE_OUTER_BOUND ( 'NONE', #6553, .T. ) ;
#22765=CARTESIAN_POINT ( 'NONE',  ( 44.70507715278255745, 27.66291119454915304, 46.92503878583764987 ) ) ;
#22781=CARTESIAN_POINT ( 'NONE',  ( 45.50623141997586174, 22.89977464660286444, 48.01957109218837871 ) ) ;
#22789=CARTESIAN_POINT ( 'NONE',  ( 47.22751897799751220, 26.54253733014356342, 44.55267275764142454 ) ) ;
#22792=CARTESIAN_POINT ( 'NONE',  ( 44.70507715278255745, 25.56291119454915517, 46.92503878583764987 ) ) ;
#22793=ORIENTED_EDGE ( 'NONE', *, *, #25570, .T. ) ;
#22804=CARTESIAN_POINT ( 'NONE',  ( 47.33512057650604277, 22.89977464660286444, 45.20042056806582309 ) ) ;
#22809=CARTESIAN_POINT ( 'NONE',  ( 45.52675994804781112, 28.93420399681022559, 49.47108226228596806 ) ) ;
#22811=CARTESIAN_POINT ( 'NONE',  ( 48.83862994770794330, 29.44118040159425931, 48.17861352429476796 ) ) ;
#22839=CARTESIAN_POINT ( 'NONE',  ( 48.46535932150934656, 28.98954579807170617, 49.73005965046827015 ) ) ;
#22856=CARTESIAN_POINT ( 'NONE',  ( 48.40186567930498285, 28.21618040159426499, 45.03923535223908203 ) ) ;
#22857=CARTESIAN_POINT ( 'NONE',  ( 44.70507715278255745, 29.06291119454914451, 46.92503878583764987 ) ) ;
#22874=CARTESIAN_POINT ( 'NONE',  ( 45.39969523643555505, 22.86454579224779948, 45.99212200068701861 ) ) ;
#22886=CARTESIAN_POINT ( 'NONE',  ( 49.98072202819531640, 26.24488759933319670, 47.19902993264913960 ) ) ;
#22887=ORIENTED_EDGE ( 'NONE', *, *, #25090, .T. ) ;
#22900=ORIENTED_EDGE ( 'NONE', *, *, #21822, .T. ) ;
#22914=CARTESIAN_POINT ( 'NONE',  ( 47.91579473090698116, 29.86454579224779948, 48.65273438611181689 ) ) ;
#22919=CARTESIAN_POINT ( 'NONE',  ( 47.59771343202220351, 22.98879437201065912, 45.66843904406525922 ) ) ;
#22923=CARTESIAN_POINT ( 'NONE',  ( 48.94625023931840246, 29.47124452788248306, 46.10640627770150246 ) ) ;
#22926=ORIENTED_EDGE ( 'NONE', *, *, #4000, .T. ) ;
#22944=FACE_OUTER_BOUND ( 'NONE', #25256, .T. ) ;
#22945=CARTESIAN_POINT ( 'NONE',  ( 44.74832014356462651, 26.28456182964376353, 46.92728461490987257 ) ) ;
#22951=CARTESIAN_POINT ( 'NONE',  ( 49.87408856414482727, 24.84440440346269341, 46.61556741858395725 ) ) ;
#22964=CARTESIAN_POINT ( 'NONE',  ( 48.18662509608405742, 26.58284706826093569, 49.18364984542562013 ) ) ;
#22967=CARTESIAN_POINT ( 'NONE',  ( 47.09785597605719687, 20.36454579224780304, 47.04930799450078638 ) ) ;
#22968=EDGE_CURVE ( 'NONE', #4406, #3003, #23951, .T. ) ;
#22977=ORIENTED_EDGE ( 'NONE', *, *, #982, .T. ) ;
#22979=AXIS2_PLACEMENT_3D ( 'NONE', #3390, #7847, #18009 ) ;
#22998=CARTESIAN_POINT ( 'NONE',  ( 47.23302798462060537, 28.58121246473837473, 44.44659793406428605 ) ) ;
#23010=CARTESIAN_POINT ( 'NONE',  ( 47.43556129377199682, 23.11533908250407165, 46.87703799288242124 ) ) ;
#23015=CARTESIAN_POINT ( 'NONE',  ( 48.40186567930498285, 26.11618040159426357, 45.03923535223908203 ) ) ;
#23016=CARTESIAN_POINT ( 'NONE',  ( 45.24946171279598417, 29.12124452788248163, 47.99220971130007030 ) ) ;
#23025=CARTESIAN_POINT ( 'NONE',  ( 45.00053793792376666, 26.65920399681023056, 45.68869892245983522 ) ) ;
#23027=EDGE_CURVE ( 'NONE', #26705, #7293, #17757, .T. ) ;
#23056=CARTESIAN_POINT ( 'NONE',  ( 48.78406556707242459, 22.93807716476589675, 47.13688154746046166 ) ) ;
#23081=VERTEX_POINT ( 'NONE', #21650 ) ;
#23084=EDGE_CURVE ( 'NONE', #5136, #10913, #12326, .T. ) ;
#23093=CARTESIAN_POINT ( 'NONE',  ( 48.23388202445966755, 15.77906836436399374, 49.27628909396055690 ) ) ;
#23119=CARTESIAN_POINT ( 'NONE',  ( 45.38854177497844944, 26.22622849631042996, 45.94041160078741370 ) ) ;
#23125=ORIENTED_EDGE ( 'NONE', *, *, #30698, .F. ) ;
#23129=MANIFOLD_SOLID_BREP ( 'Stock-MAT-060-1', #15277 ) ;
#23153=AXIS2_PLACEMENT_3D ( 'NONE', #24043, #27002, #6654 ) ;
#23164=CARTESIAN_POINT ( 'NONE',  ( 48.10030433005226769, 29.45850404830353142, 49.01443330185325920 ) ) ;
#23183=CARTESIAN_POINT ( 'NONE',  ( 48.40186567930498285, 27.51618040159426570, 45.03923535223908203 ) ) ;
#23184=CARTESIAN_POINT ( 'NONE',  ( 45.24946171279598417, 28.42124452788248234, 47.99220971130007030 ) ) ;
#23201=ADVANCED_FACE ( 'NONE', ( #3566 ), #2766, .T. ) ;
#23230=EDGE_LOOP ( 'NONE', ( #30094, #5183, #17065, #21931, #20915 ) ) ;
#23250=ORIENTED_EDGE ( 'NONE', *, *, #24310, .F. ) ;
#23263=CYLINDRICAL_SURFACE ( 'NONE', #22979, 2.499999999999997335 ) ;
#23270=UNCERTAINTY_MEASURE_WITH_UNIT (LENGTH_MEASURE( 1.000000000000000082E-05 ), #13173, 'distance_accuracy_value', 'NONE');
#23284=CARTESIAN_POINT ( 'NONE',  ( 44.74832014356462651, 26.98456182964376637, 46.92728461490987257 ) ) ;
#23285=EDGE_CURVE ( 'NONE', #16262, #6052, #11441, .T. ) ;
#23291=CYLINDRICAL_SURFACE ( 'NONE', #13280, 7.999999999999999112 ) ;
#23294=DIRECTION ( 'NONE',  ( 0.2155021956183755527, 0.9702957262759969170, -0.1099318300320483582 ) ) ;
#23303=EDGE_CURVE ( 'NONE', #7375, #306, #4664, .T. ) ;
#23321=ORIENTED_EDGE ( 'NONE', *, *, #16555, .T. ) ;
#23344=CARTESIAN_POINT ( 'NONE',  ( 45.73035263060504718, 28.63954579807170475, 44.36855633853329550 ) ) ;
#23347=CARTESIAN_POINT ( 'NONE',  ( 48.83862994770794330, 29.35457786121581591, 48.17861352429476796 ) ) ;
#23369=CARTESIAN_POINT ( 'NONE',  ( 46.45294456288812057, 23.04411657098542676, 46.11470425768455783 ) ) ;
#23394=CARTESIAN_POINT ( 'NONE',  ( 48.23388202445966755, 27.52822092656774089, 49.27628909396054979 ) ) ;
#23403=EDGE_CURVE ( 'NONE', #13392, #10357, #1252, .T. ) ;
#23404=DIRECTION ( 'NONE',  ( 0.3935310072385435620, 0.5000000000000002220, 0.7714488617801035231 ) ) ;
#23409=VECTOR ( 'NONE', #11631, 1000.000000000000114 ) ;
#23418=CARTESIAN_POINT ( 'NONE',  ( 45.52675994804781112, 28.81155426599984892, 49.47108226228597516 ) ) ;
#23438=DIRECTION ( 'NONE',  ( 0.4544104193609903586, 0.000000000000000000, 0.8907924397839087627 ) ) ;
#23440=CARTESIAN_POINT ( 'NONE',  ( 45.81741271322955100, 27.80122849631042925, 49.02305402274571122 ) ) ;
#23453=EDGE_LOOP ( 'NONE', ( #27688, #25377, #9269, #2839, #15956, #13188 ) ) ;
#23460=CARTESIAN_POINT ( 'NONE',  ( 49.32483701613094240, 25.60322093266652743, 45.91328182968236860 ) ) ;
#23461=CARTESIAN_POINT ( 'NONE',  ( 46.00908685603032922, 25.53284706826093498, 44.91496614357595263 ) ) ;
#23482=CARTESIAN_POINT ( 'NONE',  ( 47.86511985000206693, 22.93807716476589320, 48.55339511290479493 ) ) ;
#23495=ADVANCED_FACE ( 'NONE', ( #15370 ), #32287, .F. ) ;
#23497=EDGE_LOOP ( 'NONE', ( #22977, #5408, #5894, #30487 ) ) ;
#23502=CARTESIAN_POINT ( 'NONE',  ( 44.09250526802607340, 28.75621246473837189, 46.89322480343881949 ) ) ;
#23526=VERTEX_POINT ( 'NONE', #3530 ) ;
#23527=CARTESIAN_POINT ( 'NONE',  ( 46.04844006429464542, 22.80400562401889530, 44.99211097489548905 ) ) ;
#23533=CARTESIAN_POINT ( 'NONE',  ( 47.20987246576030572, 29.61033276412549142, 44.99785217098620649 ) ) ;
#23546=( BOUNDED_CURVE ( )  B_SPLINE_CURVE ( 2, ( #25100, #27724, #22789, #19837, #4579, #27228, #2289, #4917, #5242 ),
 .UNSPECIFIED., .F., .F. ) 
 B_SPLINE_CURVE_WITH_KNOTS ( ( 3, 2, 2, 2, 3 ),
 ( 0.6071428583041297289, 0.6190476190476190688, 0.6428571428571429047, 0.6666666666666666297, 0.6785714297327011257 ),
 .UNSPECIFIED. ) 
 CURVE ( )  GEOMETRIC_REPRESENTATION_ITEM ( )  RATIONAL_B_SPLINE_CURVE ( ( 0.9330127018922200755, 0.9330127084266224280, 1.000000000000000000, 0.8660254037844388186, 1.000000000000000000, 0.8660254037844388186, 1.000000000000000000, 0.9330126953578163906, 0.9330127018922200755 ) ) 
 REPRESENTATION_ITEM ( '' )  );
#23551=CARTESIAN_POINT ( 'NONE',  ( 49.19517401419062708, 26.88655426599985887, 48.40991706654173754 ) ) ;
#23560=FACE_OUTER_BOUND ( 'NONE', #11469, .T. ) ;
#23573=CARTESIAN_POINT ( 'NONE',  ( 45.24946171279598417, 25.62124452788248874, 47.99220971130007030 ) ) ;
#23574=EDGE_CURVE ( 'NONE', #5630, #10357, #31034, .T. ) ;
#23580=CARTESIAN_POINT ( 'NONE',  ( 47.94855545692534093, 23.24793988701932435, 46.58741075937935250 ) ) ;
#23589=PRODUCT_DEFINITION_CONTEXT ( 'detailed design', #1945, 'design' ) ;
#23597=CARTESIAN_POINT ( 'NONE',  ( 48.15269122424245296, 22.93328494799376216, 48.40553779021257697 ) ) ;
#23601=CARTESIAN_POINT ( 'NONE',  ( 48.16694854572211426, 25.11789516297710279, 49.14507740233662503 ) ) ;
#23610=DIRECTION ( 'NONE',  ( 0.5319835227803570987, 0.2110602665713105230, -0.8200287161831887328 ) ) ;
#23634=CARTESIAN_POINT ( 'NONE',  ( 48.15243707092404435, 22.93807716476589675, 45.72078620869762489 ) ) ;
#23649=CARTESIAN_POINT ( 'NONE',  ( 46.99448882228015378, 29.20566913182630131, 44.58373285574925404 ) ) ;
#23665=CARTESIAN_POINT ( 'NONE',  ( 46.96268396749378127, 26.83121246473837473, 49.65201805493727960 ) ) ;
#23667=DIRECTION ( 'NONE',  ( 0.05186525298099653458, 6.405245952009083202E-18, -0.9986540920324801229 ) ) ;
#23691=CARTESIAN_POINT ( 'NONE',  ( 47.20547626766765603, 26.78791119454915659, 44.97710074790751378 ) ) ;
#23694=CARTESIAN_POINT ( 'NONE',  ( 45.96182992765472619, 26.47822092656774728, 44.82232689504103007 ) ) ;
#23697=CARTESIAN_POINT ( 'NONE',  ( 47.15748190832469078, 29.60686683473450742, 44.99247469298313717 ) ) ;
#23706=CARTESIAN_POINT ( 'NONE',  ( 48.10030433005226769, 29.45850404830353142, 49.01443330185325920 ) ) ;
#23741=( BOUNDED_CURVE ( )  B_SPLINE_CURVE ( 2, ( #5508, #26159, #31102, #18129, #30459, #17967, #15513 ),
 .UNSPECIFIED., .F., .F. ) 
 B_SPLINE_CURVE_WITH_KNOTS ( ( 3, 2, 2, 3 ),
 ( 0.7499999988387272554, 0.7619047619047618625, 0.7857142857142856984, 0.7981887600530632731 ),
 .UNSPECIFIED. ) 
 CURVE ( )  GEOMETRIC_REPRESENTATION_ITEM ( )  RATIONAL_B_SPLINE_CURVE ( ( 0.9330127018922199644, 0.9330126953578153914, 1.000000000000000000, 0.8660254037844387076, 1.000000000000000000, 0.9298069681733576175, 0.9331661149864407534 ) ) 
 REPRESENTATION_ITEM ( '' )  );
#23743=ORIENTED_EDGE ( 'NONE', *, *, #29615, .T. ) ;
#23753=CARTESIAN_POINT ( 'NONE',  ( 47.87652597323660331, 22.99884124225578219, 48.23166275730290664 ) ) ;
#23757=CARTESIAN_POINT ( 'NONE',  ( 46.99218062947583974, 27.90286309983298096, 49.08406571254116102 ) ) ;
#23782=AXIS2_PLACEMENT_3D ( 'NONE', #5626, #23667, #20393 ) ;
#23813=CARTESIAN_POINT ( 'NONE',  ( 46.96268396749378127, 28.23121246473836976, 49.65201805493727960 ) ) ;
#23819=CIRCLE ( 'NONE', #11764, 0.3000000000000017653 ) ;
#23827=CARTESIAN_POINT ( 'NONE',  ( 48.83059987400639557, 28.38213139976339860, 48.97189179988551899 ) ) ;
#23828=CARTESIAN_POINT ( 'NONE',  ( 44.70507715278255745, 29.14951373492759146, 46.92503878583764987 ) ) ;
#23842=CARTESIAN_POINT ( 'NONE',  ( 46.99023568444673060, 28.53791119454914949, 49.12151524109405898 ) ) ;
#23851=CARTESIAN_POINT ( 'NONE',  ( 47.41914917073021485, 29.61434127664690763, 45.02321843626506137 ) ) ;
#23864=ORIENTED_EDGE ( 'NONE', *, *, #27068, .T. ) ;
#23887=CARTESIAN_POINT ( 'NONE',  ( 45.45032030167665482, 22.91413368675619111, 46.31675765204602868 ) ) ;
#23897=CARTESIAN_POINT ( 'NONE',  ( 47.09785597605719687, 15.77906836436399374, 47.04930799450078638 ) ) ;
#23917=CARTESIAN_POINT ( 'NONE',  ( 48.80717017713595141, 26.61952976649964953, 48.15820438821415195 ) ) ;
#23927=CARTESIAN_POINT ( 'NONE',  ( 46.96268396749378127, 26.13121246473837544, 49.65201805493727960 ) ) ;
#23942=DIRECTION ( 'NONE',  ( 0.5442436726714897643, 6.721291001053910056E-17, -0.8389271868029121171 ) ) ;
#23951=LINE ( 'NONE', #21482, #17202 ) ;
#23959=CARTESIAN_POINT ( 'NONE',  ( 49.19517401419062708, 29.10920399681022630, 48.40991706654173754 ) ) ;
#23962=SHAPE_REPRESENTATION_RELATIONSHIP ( 'NONE' , 'NONE' ,  #5723, #30825 ) ;
#23977=EDGE_CURVE ( 'NONE', #15887, #11490, #31081, .T. ) ;
#23978=CARTESIAN_POINT ( 'NONE',  ( 48.73570333863616355, 29.22287913140504045, 44.52463952959527660 ) ) ;
#23987=CARTESIAN_POINT ( 'NONE',  ( 45.24946171279598417, 29.90784706826092076, 47.99220971130007030 ) ) ;
#24001=CARTESIAN_POINT ( 'NONE',  ( 45.61530479625130852, 22.89977464660286444, 45.91938710987583505 ) ) ;
#24003=CARTESIAN_POINT ( 'NONE',  ( 49.49063479933183629, 28.71291119454914664, 47.17357720316391578 ) ) ;
#24034=VERTEX_POINT ( 'NONE', #386 ) ;
#24043=CARTESIAN_POINT ( 'NONE',  ( 47.09785597605719687, 19.86454579224779948, 47.04930799450078638 ) ) ;
#24056=AXIS2_PLACEMENT_3D ( 'NONE', #31521, #2125, #12144 ) ;
#24075=CARTESIAN_POINT ( 'NONE',  ( 49.44739180854976013, 29.47786309983297670, 47.17133137409169308 ) ) ;
#24087=CARTESIAN_POINT ( 'NONE',  ( 48.46535932150934656, 24.78954579807171754, 49.73005965046827015 ) ) ;
#24089=CARTESIAN_POINT ( 'NONE',  ( 46.61092110408701217, 23.04411657098542676, 48.07511952990385851 ) ) ;
#24091=VERTEX_POINT ( 'NONE', #26142 ) ;
#24118=( BOUNDED_SURFACE ( )  B_SPLINE_SURFACE ( 1, 2, ( 
 ( #7751, #13171, #30728, #17753, #7921, #8239, #2821, #27771, #12848, #22839, #5610, #353, #27937, #5456, #15458, #25470, #22998, #25629, #512, #10550, #30570, #3131, #21453, #18825, #29022, #4239, #16375, #14256, #9318, #24251, #29342, #9491, #28865, #24414, #16863, #13933, #12120, #6376, #27042, #26881, #26717, #11946, #7022, #9158, #6694, #19489, #1771, #6537, #29516, #26397, #17016, #19156, #14413, #8997, #4556, #14574, #1605, #21942, #23927, #24578, #31655, #14092, #11626, #31489, #4394, #3906, #1439, #11788, #31970, #11456, #26555, #21622, #2094, #16536, #19318, #29182, #18992, #22110, #21784, #4063, #31808, #24087, #6866, #32140, #16692 ),
 ( #1928, #17352, #12777, #7684, #9651, #17841, #22923, #20295, #5055, #29677, #19978, #27536, #30007, #15386, #27864, #24914, #27694, #30170, #15065, #2262, #20139, #25071, #7519, #9814, #9978, #125, #5383, #27373, #12282, #10143, #4890, #2583, #30327, #5215, #15223, #12936, #2429, #22765, #14905, #17520, #7841, #24748, #12612, #17676, #25393, #282, #2905, #22603, #19808, #12445, #29842, #22273, #25239, #7351, #2751, #10308, #19644, #7183, #17180, #32304, #27200, #4724, #14742, #22428, #32465, #16178, #3386, #3545, #26192, #3711, #8320, #25877, #23573, #13736, #18159, #20464, #1088, #20789, #15702, #441, #8646, #6023, #13419, #10470, #30495 ) ),
 .UNSPECIFIED., .F., .F., .F. ) 
 B_SPLINE_SURFACE_WITH_KNOTS ( ( 2, 2 ),
 ( 3, 2, 2, 2, 2, 2, 2, 2, 2, 2, 2, 2, 2, 2, 2, 2, 2, 2, 2, 2, 2, 2, 2, 2, 2, 2, 2, 2, 2, 2, 2, 2, 2, 2, 2, 2, 2, 2, 2, 2, 2, 2, 3 ),
 ( 0.000000000000000000, 1.000000000000000000 ),
 ( 0.000000000000000000, 0.02380952380952380820, 0.04761904761904761640, 0.07142857142857142461, 0.09523809523809523281, 0.1190476190476190410, 0.1428571428571428492, 0.1666666666666666574, 0.1904761904761904656, 0.2142857142857142738, 0.2380952380952380820, 0.2619047619047619180, 0.2857142857142856984, 0.3095238095238095344, 0.3333333333333333148, 0.3571428571428571508, 0.3809523809523809312, 0.4047619047619047672, 0.4285714285714285476, 0.4523809523809523836, 0.4761904761904761640, 0.5000000000000000000, 0.5238095238095238360, 0.5476190476190476719, 0.5714285714285713969, 0.5952380952380952328, 0.6190476190476190688, 0.6428571428571429047, 0.6666666666666666297, 0.6904761904761904656, 0.7142857142857143016, 0.7380952380952381375, 0.7619047619047618625, 0.7857142857142856984, 0.8095238095238095344, 0.8333333333333333703, 0.8571428571428570953, 0.8809523809523809312, 0.9047619047619047672, 0.9285714285714286031, 0.9523809523809523281, 0.9761904761904761640, 1.000000000000000000 ),
 .UNSPECIFIED. ) 
 GEOMETRIC_REPRESENTATION_ITEM ( )  RATIONAL_B_SPLINE_SURFACE ( (
 ( 1.000000000000000000, 0.8660254037844387076, 1.000000000000000000, 0.8660254037844387076, 1.000000000000000000, 0.8660254037844387076, 1.000000000000000000, 0.8660254037844387076, 1.000000000000000000, 0.8660254037844387076, 1.000000000000000000, 0.8660254037844387076, 1.000000000000000000, 0.8660254037844387076, 1.000000000000000000, 0.8660254037844387076, 1.000000000000000000, 0.8660254037844387076, 1.000000000000000000, 0.8660254037844387076, 1.000000000000000000, 0.8660254037844387076, 1.000000000000000000, 0.8660254037844387076, 1.000000000000000000, 0.8660254037844387076, 1.000000000000000000, 0.8660254037844387076, 1.000000000000000000, 0.8660254037844387076, 1.000000000000000000, 0.8660254037844387076, 1.000000000000000000, 0.8660254037844387076, 1.000000000000000000, 0.8660254037844387076, 1.000000000000000000, 0.8660254037844387076, 1.000000000000000000, 0.8660254037844387076, 1.000000000000000000, 0.8660254037844387076, 1.000000000000000000, 0.8660254037844387076, 1.000000000000000000, 0.8660254037844387076, 1.000000000000000000, 0.8660254037844387076, 1.000000000000000000, 0.8660254037844387076, 1.000000000000000000, 0.8660254037844387076, 1.000000000000000000, 0.8660254037844387076, 1.000000000000000000, 0.8660254037844387076, 1.000000000000000000, 0.8660254037844387076, 1.000000000000000000, 0.8660254037844387076, 1.000000000000000000, 0.8660254037844387076, 1.000000000000000000, 0.8660254037844387076, 1.000000000000000000, 0.8660254037844387076, 1.000000000000000000, 0.8660254037844387076, 1.000000000000000000, 0.8660254037844387076, 1.000000000000000000, 0.8660254037844387076, 1.000000000000000000, 0.8660254037844387076, 1.000000000000000000, 0.8660254037844387076, 1.000000000000000000, 0.8660254037844387076, 1.000000000000000000, 0.8660254037844387076, 1.000000000000000000, 0.8660254037844387076, 1.000000000000000000, 0.8660254037844387076, 1.000000000000000000),
 ( 1.000000000000000000, 0.8660254037844387076, 1.000000000000000000, 0.8660254037844387076, 1.000000000000000000, 0.8660254037844387076, 1.000000000000000000, 0.8660254037844387076, 1.000000000000000000, 0.8660254037844387076, 1.000000000000000000, 0.8660254037844387076, 1.000000000000000000, 0.8660254037844387076, 1.000000000000000000, 0.8660254037844387076, 1.000000000000000000, 0.8660254037844387076, 1.000000000000000000, 0.8660254037844387076, 1.000000000000000000, 0.8660254037844387076, 1.000000000000000000, 0.8660254037844387076, 1.000000000000000000, 0.8660254037844387076, 1.000000000000000000, 0.8660254037844387076, 1.000000000000000000, 0.8660254037844387076, 1.000000000000000000, 0.8660254037844387076, 1.000000000000000000, 0.8660254037844387076, 1.000000000000000000, 0.8660254037844387076, 1.000000000000000000, 0.8660254037844387076, 1.000000000000000000, 0.8660254037844387076, 1.000000000000000000, 0.8660254037844387076, 1.000000000000000000, 0.8660254037844387076, 1.000000000000000000, 0.8660254037844387076, 1.000000000000000000, 0.8660254037844387076, 1.000000000000000000, 0.8660254037844387076, 1.000000000000000000, 0.8660254037844387076, 1.000000000000000000, 0.8660254037844387076, 1.000000000000000000, 0.8660254037844387076, 1.000000000000000000, 0.8660254037844387076, 1.000000000000000000, 0.8660254037844387076, 1.000000000000000000, 0.8660254037844387076, 1.000000000000000000, 0.8660254037844387076, 1.000000000000000000, 0.8660254037844387076, 1.000000000000000000, 0.8660254037844387076, 1.000000000000000000, 0.8660254037844387076, 1.000000000000000000, 0.8660254037844387076, 1.000000000000000000, 0.8660254037844387076, 1.000000000000000000, 0.8660254037844387076, 1.000000000000000000, 0.8660254037844387076, 1.000000000000000000, 0.8660254037844387076, 1.000000000000000000, 0.8660254037844387076, 1.000000000000000000, 0.8660254037844387076, 1.000000000000000000) ) ) 
 REPRESENTATION_ITEM ( '' )  SURFACE ( )  );
#24132=CARTESIAN_POINT ( 'NONE',  ( 46.04844006429464542, 22.80400562401889530, 44.99211097489548905 ) ) ;
#24140=VECTOR ( 'NONE', #23404, 999.9999999999998863 ) ;
#24150=CARTESIAN_POINT ( 'NONE',  ( 45.79384627280941089, 27.86618040159426357, 49.05938063676249072 ) ) ;
#24165=CARTESIAN_POINT ( 'NONE',  ( 44.21498992391907024, 27.99488759933318605, 46.89958605635244027 ) ) ;
#24167=CARTESIAN_POINT ( 'NONE',  ( 46.15191711366536254, 22.98879437201065912, 45.92598426414627255 ) ) ;
#24187=EDGE_CURVE ( 'NONE', #4406, #26923, #26309, .T. ) ;
#24200=EDGE_LOOP ( 'NONE', ( #32195, #10850, #27260 ) ) ;
#24221=DIRECTION ( 'NONE',  ( 0.4544104193609903586, 0.000000000000000000, 0.8907924397839087627 ) ) ;
#24226=ORIENTED_EDGE ( 'NONE', *, *, #16552, .F. ) ;
#24240=CARTESIAN_POINT ( 'NONE',  ( 46.99218062947583974, 28.60286309983298381, 49.08406571254116102 ) ) ;
#24241=ORIENTED_EDGE ( 'NONE', *, *, #12015, .F. ) ;
#24246=CARTESIAN_POINT ( 'NONE',  ( 48.71516269694878076, 29.58372224308939025, 45.72934403980688955 ) ) ;
#24251=CARTESIAN_POINT ( 'NONE',  ( 48.73570333863616355, 27.82287913140503832, 44.52463952959527660 ) ) ;
#24253=CARTESIAN_POINT ( 'NONE',  ( 47.28721660713063812, 22.91413368675619111, 48.84239091338285732 ) ) ;
#24265=EDGE_LOOP ( 'NONE', ( #28160, #1106, #24241, #20110, #31041, #7405, #19186, #30526, #8615, #5598, #25287, #7190, #22742, #30877, #15356, #2315, #1373, #31748 ) ) ;
#24275=AXIS2_PLACEMENT_3D ( 'NONE', #14258, #24750, #31657 ) ;
#24276=ORIENTED_EDGE ( 'NONE', *, *, #12036, .F. ) ;
#24285=EDGE_LOOP ( 'NONE', ( #28728, #6367 ) ) ;
#24286=CARTESIAN_POINT ( 'NONE',  ( 45.50174972710295407, 22.86454579224779593, 48.32172736629423326 ) ) ;
#24296=CARTESIAN_POINT ( 'NONE',  ( 46.92175814837349179, 22.74928388133296764, 44.57455356976052485 ) ) ;
#24307=CARTESIAN_POINT ( 'NONE',  ( 44.91142894931555674, 25.89787913140504472, 45.63089057098605394 ) ) ;
#24310=EDGE_CURVE ( 'NONE', #5411, #4161, #25145, .T. ) ;
#24315=CARTESIAN_POINT ( 'NONE',  ( 47.20547626766766314, 27.57451373492759572, 44.97710074790751378 ) ) ;
#24316=ORIENTED_EDGE ( 'NONE', *, *, #26978, .F. ) ;
#24335=EDGE_LOOP ( 'NONE', ( #18402, #12488 ) ) ;
#24338=CARTESIAN_POINT ( 'NONE',  ( 48.23388202445966755, 15.77906836436399374, 49.27628909396055690 ) ) ;
#24341=ADVANCED_FACE ( 'NONE', ( #2660 ), #4470, .F. ) ;
#24344=ADVANCED_FACE ( 'NONE', ( #5123 ), #32213, .F. ) ;
#24351=ORIENTED_EDGE ( 'NONE', *, *, #27990, .F. ) ;
#24400=CARTESIAN_POINT ( 'NONE',  ( 47.20353132263855400, 27.55286309983298310, 45.01455027646040463 ) ) ;
#24411=CARTESIAN_POINT ( 'NONE',  ( 48.35473289974373756, 22.80400562401889530, 45.11188864597615833 ) ) ;
#24414=CARTESIAN_POINT ( 'NONE',  ( 48.46535932150934656, 27.58954579807170759, 49.73005965046827015 ) ) ;
#24415=CARTESIAN_POINT ( 'NONE',  ( 47.07819351491129822, 23.11533908250407165, 47.42790437944410087 ) ) ;
#24422=CARTESIAN_POINT ( 'NONE',  ( 48.00894325680572194, 23.03451764446789696, 46.25432281694521919 ) ) ;
#24430=STYLED_ITEM ( 'NONE', ( #29556 ), #30825 ) ;
#24432=EDGE_CURVE ( 'NONE', #26305, #15887, #5820, .T. ) ;
#24458=CARTESIAN_POINT ( 'NONE',  ( 46.04844006429464542, 22.86454579224779948, 44.99211097489548905 ) ) ;
#24474=CARTESIAN_POINT ( 'NONE',  ( 45.28286642839709231, 25.68619643316632306, 47.97516931882780966 ) ) ;
#24491=CARTESIAN_POINT ( 'NONE',  ( 49.70056603649367588, 24.90621246473837047, 47.18448000306445067 ) ) ;
#24502=CARTESIAN_POINT ( 'NONE',  ( 44.70507715278255745, 29.14951373492759146, 46.92503878583764987 ) ) ;
#24523=ORIENTED_EDGE ( 'NONE', *, *, #14987, .F. ) ;
#24578=CARTESIAN_POINT ( 'NONE',  ( 45.46000861347822308, 26.07287913140504543, 49.57397645940629616 ) ) ;
#24579=CARTESIAN_POINT ( 'NONE',  ( 46.99747725352182925, 22.88065857334294861, 48.98207832244369087 ) ) ;
#24584=DIRECTION ( 'NONE',  ( 0.4544104193609903586, 0.000000000000000000, 0.8907924397839087627 ) ) ;
#24589=VERTEX_POINT ( 'NONE', #21012 ) ;
#24595=( BOUNDED_SURFACE ( )  B_SPLINE_SURFACE ( 3, 2, ( 
 ( #25805, #3148, #20555, #7939, #856, #25331, #30745, #25488, #23347, #2989, #17934, #10724, #23016, #22857, #8253, #30586, #18239, #12868, #28120, #3316, #10393, #15477, #5625, #20391, #23184, #28273, #30422, #5473, #535, #5795, #13023, #15626, #20872, #10566, #13346, #15799, #25646, #13193, #10881, #20719, #22307, #15089, #27403, #15252, #10172, #20005, #7387, #20320, #17381, #5407, #19839, #30193, #15410, #27229, #14929, #10009, #25422, #12802, #2930, #25101, #2776, #24941, #10330, #7704, #17699, #9680, #29705, #2455, #12306, #22138, #17546, #27725, #5243, #22792, #19676, #30353, #17212, #7549, #27891, #32167, #14772, #22629, #7211, #152, #12473 ),
 ( #4756, #25263, #309, #24774, #32332, #7871, #2290, #9840, #17873, #29870, #4918, #22459, #32493, #30036, #27563, #5078, #2612, #12641, #20168, #16049, #3084, #25578, #20494, #18181, #796, #3415, #28534, #16203, #11141, #10496, #30521, #13292, #8038, #28050, #5893, #23440, #6050, #28683, #20813, #13122, #18026, #6198, #10822, #18662, #5565, #12961, #21124, #31158, #26220, #23284, #15565, #20655, #8192, #30836, #8672, #31000, #28211, #15899, #8347, #18346, #28376, #22945, #23119, #25903, #8512, #637, #13445, #10668, #949, #10976, #20972, #30680, #18506, #26054, #469, #5726, #15731, #3570, #25746, #3255, #13596, #23601, #1116, #7010, #18979 ),
 ( #6528, #9478, #21609, #26702, #31958, #26870, #13762, #24075, #17005, #21284, #4226, #3736, #29011, #13921, #16851, #9145, #1263, #16678, #3897, #29170, #8985, #29329, #24240, #1591, #21442, #1914, #31476, #19475, #1428, #11775, #29506, #8817, #16524, #11614, #23757, #4383, #11294, #6684, #14402, #26544, #24400, #21769, #31796, #31317, #18814, #4053, #26388, #28853, #31642, #9307, #19304, #11934, #6365, #21930, #16364, #19143, #23917, #11444, #14079, #14243, #1759, #6852, #11851, #18893, #28929, #6438, #14481, #14316, #16756, #1992, #31387, #29411, #24474, #12011, #19384, #16440, #18723, #6273, #26297, #31870, #1501, #22005, #31555, #13832, #26780 ),
 ( #23987, #21846, #8732, #1344, #11517, #28758, #26615, #31713, #4461, #9385, #16277, #29083, #3806, #23828, #9224, #11361, #21517, #26458, #6922, #14152, #21347, #21684, #8896, #1670, #13995, #1834, #29240, #6601, #3973, #16921, #9058, #19052, #16595, #4297, #4129, #24150, #11692, #19215, #6758, #26943, #24315, #24969, #12676, #24810, #20205, #7580, #17579, #19545, #7086, #2326, #22173, #12835, #27436, #27595, #5109, #185, #29576, #7737, #27102, #17416, #5280, #32036, #24644, #24, #9554, #10043, #15124, #14967, #25135, #4787, #4618, #7420, #2649, #14640, #22666, #10204, #17086, #30227, #22494, #9874, #12180, #25299, #2164, #17735, #29738 ) ),
 .UNSPECIFIED., .F., .F., .F. ) 
 B_SPLINE_SURFACE_WITH_KNOTS ( ( 4, 4 ),
 ( 3, 2, 2, 2, 2, 2, 2, 2, 2, 2, 2, 2, 2, 2, 2, 2, 2, 2, 2, 2, 2, 2, 2, 2, 2, 2, 2, 2, 2, 2, 2, 2, 2, 2, 2, 2, 2, 2, 2, 2, 2, 2, 3 ),
 ( 0.000000000000000000, 1.000000000000000000 ),
 ( 0.000000000000000000, 0.02380952380952380820, 0.04761904761904761640, 0.07142857142857142461, 0.09523809523809523281, 0.1190476190476190410, 0.1428571428571428492, 0.1666666666666666574, 0.1904761904761904656, 0.2142857142857142738, 0.2380952380952380820, 0.2619047619047619180, 0.2857142857142856984, 0.3095238095238095344, 0.3333333333333333148, 0.3571428571428571508, 0.3809523809523809312, 0.4047619047619047672, 0.4285714285714285476, 0.4523809523809523836, 0.4761904761904761640, 0.5000000000000000000, 0.5238095238095238360, 0.5476190476190476719, 0.5714285714285713969, 0.5952380952380952328, 0.6190476190476190688, 0.6428571428571429047, 0.6666666666666666297, 0.6904761904761904656, 0.7142857142857143016, 0.7380952380952381375, 0.7619047619047618625, 0.7857142857142856984, 0.8095238095238095344, 0.8333333333333333703, 0.8571428571428570953, 0.8809523809523809312, 0.9047619047619047672, 0.9285714285714286031, 0.9523809523809523281, 0.9761904761904761640, 1.000000000000000000 ),
 .UNSPECIFIED. ) 
 GEOMETRIC_REPRESENTATION_ITEM ( )  RATIONAL_B_SPLINE_SURFACE ( (
 ( 1.000000000000000000, 0.8660254037844387076, 1.000000000000000000, 0.8660254037844387076, 1.000000000000000000, 0.8660254037844387076, 1.000000000000000000, 0.8660254037844387076, 1.000000000000000000, 0.8660254037844387076, 1.000000000000000000, 0.8660254037844387076, 1.000000000000000000, 0.8660254037844387076, 1.000000000000000000, 0.8660254037844387076, 1.000000000000000000, 0.8660254037844387076, 1.000000000000000000, 0.8660254037844387076, 1.000000000000000000, 0.8660254037844387076, 1.000000000000000000, 0.8660254037844387076, 1.000000000000000000, 0.8660254037844387076, 1.000000000000000000, 0.8660254037844387076, 1.000000000000000000, 0.8660254037844387076, 1.000000000000000000, 0.8660254037844387076, 1.000000000000000000, 0.8660254037844387076, 1.000000000000000000, 0.8660254037844387076, 1.000000000000000000, 0.8660254037844387076, 1.000000000000000000, 0.8660254037844387076, 1.000000000000000000, 0.8660254037844387076, 1.000000000000000000, 0.8660254037844387076, 1.000000000000000000, 0.8660254037844387076, 1.000000000000000000, 0.8660254037844387076, 1.000000000000000000, 0.8660254037844387076, 1.000000000000000000, 0.8660254037844387076, 1.000000000000000000, 0.8660254037844387076, 1.000000000000000000, 0.8660254037844387076, 1.000000000000000000, 0.8660254037844387076, 1.000000000000000000, 0.8660254037844387076, 1.000000000000000000, 0.8660254037844387076, 1.000000000000000000, 0.8660254037844387076, 1.000000000000000000, 0.8660254037844387076, 1.000000000000000000, 0.8660254037844387076, 1.000000000000000000, 0.8660254037844387076, 1.000000000000000000, 0.8660254037844387076, 1.000000000000000000, 0.8660254037844387076, 1.000000000000000000, 0.8660254037844387076, 1.000000000000000000, 0.8660254037844387076, 1.000000000000000000, 0.8660254037844387076, 1.000000000000000000, 0.8660254037844387076, 1.000000000000000000, 0.8660254037844387076, 1.000000000000000000),
 ( 0.6666666666666665186, 0.5773502691896257311, 0.6666666666666665186, 0.5773502691896257311, 0.6666666666666665186, 0.5773502691896257311, 0.6666666666666665186, 0.5773502691896257311, 0.6666666666666665186, 0.5773502691896257311, 0.6666666666666665186, 0.5773502691896257311, 0.6666666666666665186, 0.5773502691896257311, 0.6666666666666665186, 0.5773502691896257311, 0.6666666666666665186, 0.5773502691896257311, 0.6666666666666665186, 0.5773502691896257311, 0.6666666666666665186, 0.5773502691896257311, 0.6666666666666665186, 0.5773502691896257311, 0.6666666666666665186, 0.5773502691896257311, 0.6666666666666665186, 0.5773502691896257311, 0.6666666666666665186, 0.5773502691896257311, 0.6666666666666665186, 0.5773502691896257311, 0.6666666666666665186, 0.5773502691896257311, 0.6666666666666665186, 0.5773502691896257311, 0.6666666666666665186, 0.5773502691896257311, 0.6666666666666665186, 0.5773502691896257311, 0.6666666666666665186, 0.5773502691896257311, 0.6666666666666665186, 0.5773502691896257311, 0.6666666666666665186, 0.5773502691896257311, 0.6666666666666665186, 0.5773502691896257311, 0.6666666666666665186, 0.5773502691896257311, 0.6666666666666665186, 0.5773502691896257311, 0.6666666666666665186, 0.5773502691896257311, 0.6666666666666665186, 0.5773502691896257311, 0.6666666666666665186, 0.5773502691896257311, 0.6666666666666665186, 0.5773502691896257311, 0.6666666666666665186, 0.5773502691896257311, 0.6666666666666665186, 0.5773502691896257311, 0.6666666666666665186, 0.5773502691896257311, 0.6666666666666665186, 0.5773502691896257311, 0.6666666666666665186, 0.5773502691896257311, 0.6666666666666665186, 0.5773502691896257311, 0.6666666666666665186, 0.5773502691896257311, 0.6666666666666665186, 0.5773502691896257311, 0.6666666666666665186, 0.5773502691896257311, 0.6666666666666665186, 0.5773502691896257311, 0.6666666666666665186, 0.5773502691896257311, 0.6666666666666665186, 0.5773502691896257311, 0.6666666666666665186),
 ( 0.6666666666666665186, 0.5773502691896257311, 0.6666666666666665186, 0.5773502691896257311, 0.6666666666666665186, 0.5773502691896257311, 0.6666666666666665186, 0.5773502691896257311, 0.6666666666666665186, 0.5773502691896257311, 0.6666666666666665186, 0.5773502691896257311, 0.6666666666666665186, 0.5773502691896257311, 0.6666666666666665186, 0.5773502691896257311, 0.6666666666666665186, 0.5773502691896257311, 0.6666666666666665186, 0.5773502691896257311, 0.6666666666666665186, 0.5773502691896257311, 0.6666666666666665186, 0.5773502691896257311, 0.6666666666666665186, 0.5773502691896257311, 0.6666666666666665186, 0.5773502691896257311, 0.6666666666666665186, 0.5773502691896257311, 0.6666666666666665186, 0.5773502691896257311, 0.6666666666666665186, 0.5773502691896257311, 0.6666666666666665186, 0.5773502691896257311, 0.6666666666666665186, 0.5773502691896257311, 0.6666666666666665186, 0.5773502691896257311, 0.6666666666666665186, 0.5773502691896257311, 0.6666666666666665186, 0.5773502691896257311, 0.6666666666666665186, 0.5773502691896257311, 0.6666666666666665186, 0.5773502691896257311, 0.6666666666666665186, 0.5773502691896257311, 0.6666666666666665186, 0.5773502691896257311, 0.6666666666666665186, 0.5773502691896257311, 0.6666666666666665186, 0.5773502691896257311, 0.6666666666666665186, 0.5773502691896257311, 0.6666666666666665186, 0.5773502691896257311, 0.6666666666666665186, 0.5773502691896257311, 0.6666666666666665186, 0.5773502691896257311, 0.6666666666666665186, 0.5773502691896257311, 0.6666666666666665186, 0.5773502691896257311, 0.6666666666666665186, 0.5773502691896257311, 0.6666666666666665186, 0.5773502691896257311, 0.6666666666666665186, 0.5773502691896257311, 0.6666666666666665186, 0.5773502691896257311, 0.6666666666666665186, 0.5773502691896257311, 0.6666666666666665186, 0.5773502691896257311, 0.6666666666666665186, 0.5773502691896257311, 0.6666666666666665186, 0.5773502691896257311, 0.6666666666666665186),
 ( 1.000000000000000000, 0.8660254037844387076, 1.000000000000000000, 0.8660254037844387076, 1.000000000000000000, 0.8660254037844387076, 1.000000000000000000, 0.8660254037844387076, 1.000000000000000000, 0.8660254037844387076, 1.000000000000000000, 0.8660254037844387076, 1.000000000000000000, 0.8660254037844387076, 1.000000000000000000, 0.8660254037844387076, 1.000000000000000000, 0.8660254037844387076, 1.000000000000000000, 0.8660254037844387076, 1.000000000000000000, 0.8660254037844387076, 1.000000000000000000, 0.8660254037844387076, 1.000000000000000000, 0.8660254037844387076, 1.000000000000000000, 0.8660254037844387076, 1.000000000000000000, 0.8660254037844387076, 1.000000000000000000, 0.8660254037844387076, 1.000000000000000000, 0.8660254037844387076, 1.000000000000000000, 0.8660254037844387076, 1.000000000000000000, 0.8660254037844387076, 1.000000000000000000, 0.8660254037844387076, 1.000000000000000000, 0.8660254037844387076, 1.000000000000000000, 0.8660254037844387076, 1.000000000000000000, 0.8660254037844387076, 1.000000000000000000, 0.8660254037844387076, 1.000000000000000000, 0.8660254037844387076, 1.000000000000000000, 0.8660254037844387076, 1.000000000000000000, 0.8660254037844387076, 1.000000000000000000, 0.8660254037844387076, 1.000000000000000000, 0.8660254037844387076, 1.000000000000000000, 0.8660254037844387076, 1.000000000000000000, 0.8660254037844387076, 1.000000000000000000, 0.8660254037844387076, 1.000000000000000000, 0.8660254037844387076, 1.000000000000000000, 0.8660254037844387076, 1.000000000000000000, 0.8660254037844387076, 1.000000000000000000, 0.8660254037844387076, 1.000000000000000000, 0.8660254037844387076, 1.000000000000000000, 0.8660254037844387076, 1.000000000000000000, 0.8660254037844387076, 1.000000000000000000, 0.8660254037844387076, 1.000000000000000000, 0.8660254037844387076, 1.000000000000000000, 0.8660254037844387076, 1.000000000000000000) ) ) 
 REPRESENTATION_ITEM ( '' )  SURFACE ( )  );
#24607=LINE ( 'NONE', #2126, #14436 ) ;
#24618=CARTESIAN_POINT ( 'NONE',  ( 48.18662509608405031, 28.59624452788247950, 49.18364984542562013 ) ) ;
#24644=CARTESIAN_POINT ( 'NONE',  ( 45.35708200440645044, 26.29118040159426428, 45.92000246470679770 ) ) ;
#24665=CARTESIAN_POINT ( 'NONE',  ( 49.92650180258424086, 24.88153309617948139, 45.60636096795945349 ) ) ;
#24680=CARTESIAN_POINT ( 'NONE',  ( 45.39362547348767407, 29.25948157811722083, 45.34546605000252839 ) ) ;
#24695=CONICAL_SURFACE ( 'NONE', #9515, 1.799999999999998490, 0.7853981633974489451 ) ;
#24722=EDGE_CURVE ( 'NONE', #7173, #15510, #25235, .T. ) ;
#24733=CARTESIAN_POINT ( 'NONE',  ( 45.96182992765471909, 15.77906836436399374, 44.82232689504101586 ) ) ;
#24739=CARTESIAN_POINT ( 'NONE',  ( 47.09785597605719687, 24.76454579224779806, 47.04930799450078638 ) ) ;
#24745=CARTESIAN_POINT ( 'NONE',  ( 47.35361591473682097, 23.10527845304106265, 47.55068078453451363 ) ) ;
#24746=CARTESIAN_POINT ( 'NONE',  ( 46.17891025898683921, 22.93807716476589675, 48.46582155994513386 ) ) ;
#24748=CARTESIAN_POINT ( 'NONE',  ( 48.40186567930498285, 27.42957786121582231, 45.03923535223908203 ) ) ;
#24750=DIRECTION ( 'NONE',  ( 1.234978253042719660E-16, -1.000000000000000000, -1.109335647967047851E-31 ) ) ;
#24764=ORIENTED_EDGE ( 'NONE', *, *, #12356, .F. ) ;
#24774=CARTESIAN_POINT ( 'NONE',  ( 46.02876340639226527, 29.66789516297708929, 44.95353858666495483 ) ) ;
#24782=CARTESIAN_POINT ( 'NONE',  ( 45.24946171279598417, 29.12124452788248163, 47.99220971130007030 ) ) ;
#24791=CARTESIAN_POINT ( 'NONE',  ( 45.35708200440645044, 29.09118040159425789, 45.92000246470680480 ) ) ;
#24796=CARTESIAN_POINT ( 'NONE',  ( 44.77625694075214824, 26.01454579807171186, 48.23360063142255427 ) ) ;
#24802=( BOUNDED_CURVE ( )  B_SPLINE_CURVE ( 2, ( #10187, #2791, #25281, #22809, #32347, #323, #17560, #9856, #7887 ),
 .UNSPECIFIED., .F., .F. ) 
 B_SPLINE_CURVE_WITH_KNOTS ( ( 3, 2, 2, 2, 3 ),
 ( 0.1071428583041297289, 0.1190476190476190410, 0.1428571428571428492, 0.1666666666666666574, 0.1785714297327012090 ),
 .UNSPECIFIED. ) 
 CURVE ( )  GEOMETRIC_REPRESENTATION_ITEM ( )  RATIONAL_B_SPLINE_CURVE ( ( 0.9330127018922200755, 0.9330127084266225390, 1.000000000000000000, 0.8660254037844388186, 1.000000000000000000, 0.8660254037844388186, 1.000000000000000000, 0.9330126953578159466, 0.9330127018922200755 ) ) 
 REPRESENTATION_ITEM ( '' )  );
#24803=AXIS2_PLACEMENT_3D ( 'NONE', #21787, #31810, #19491 ) ;
#24810=CARTESIAN_POINT ( 'NONE',  ( 49.49063479933183629, 27.39951373492759856, 47.17357720316391578 ) ) ;
#24832=CARTESIAN_POINT ( 'NONE',  ( 44.49514591562071075, 25.25621246473836834, 46.91413598593712209 ) ) ;
#24834=DIRECTION ( 'NONE',  ( 0.4544104193609900810, 5.611869858668441979E-17, 0.8907924397839090958 ) ) ;
#24846=CARTESIAN_POINT ( 'NONE',  ( 45.78890401032107604, 29.38203082867340044, 48.92530043617153979 ) ) ;
#24847=EDGE_LOOP ( 'NONE', ( #7245, #8971, #19340, #27455 ) ) ;
#24878=ORIENTED_EDGE ( 'NONE', *, *, #10696, .T. ) ;
#24880=B_SPLINE_CURVE_WITH_KNOTS ( 'NONE', 3,
 ( #827, #23634, #3766, #3115, #10851, #26258 ),
 .UNSPECIFIED., .F., .F.,
 ( 4, 2, 4 ),
 ( 0.000000000000000000, 0.5000000000000000000, 1.000000000000000000 ),
 .UNSPECIFIED. ) ;
#24914=CARTESIAN_POINT ( 'NONE',  ( 46.00908685603034343, 28.94624452788248092, 44.91496614357595263 ) ) ;
#24927=VERTEX_POINT ( 'NONE', #9069 ) ;
#24941=CARTESIAN_POINT ( 'NONE',  ( 44.70507715278255745, 26.26291119454915801, 46.92503878583765697 ) ) ;
#24942=ORIENTED_EDGE ( 'NONE', *, *, #1951, .F. ) ;
#24959=CARTESIAN_POINT ( 'NONE',  ( 46.99023568444673771, 27.22451373492759785, 49.12151524109405898 ) ) ;
#24969=CARTESIAN_POINT ( 'NONE',  ( 48.40186567930498285, 27.51618040159426570, 45.03923535223908203 ) ) ;
#24970=ORIENTED_EDGE ( 'NONE', *, *, #28673, .T. ) ;
#24973=CIRCLE ( 'NONE', #17644, 0.4999999999999988343 ) ;
#24992=CARTESIAN_POINT ( 'NONE',  ( 47.03171727263369206, 25.15018075992191982, 44.52927784484388241 ) ) ;
#25000=ORIENTED_EDGE ( 'NONE', *, *, #15281, .T. ) ;
#25006=CARTESIAN_POINT ( 'NONE',  ( 44.90600895698101169, 29.28496411753620876, 46.11062626847921564 ) ) ;
#25020=EDGE_CURVE ( 'NONE', #4178, #32468, #11191, .T. ) ;
#25028=CARTESIAN_POINT ( 'NONE',  ( 49.00637973737335074, 15.77906836436399374, 50.79063624159320511 ) ) ;
#25036=B_SPLINE_CURVE_WITH_KNOTS ( 'NONE', 3,
 ( #8445, #25676, #28624, #5827, #566, #5655, #3018, #3181, #30771, #18124, #21061, #3671, #18595, #26154, #30933, #15661 ),
 .UNSPECIFIED., .F., .F.,
 ( 4, 2, 2, 2, 2, 2, 2, 4 ),
 ( 0.000000000000000000, 0.0003391165876995429857, 0.0004238957346244386255, 0.0005086748815493342653, 0.0005298696682805630271, 0.0005510644550117917888, 0.0005934540284742352177, 0.0006782331753991313996 ),
 .UNSPECIFIED. ) ;
#25071=CARTESIAN_POINT ( 'NONE',  ( 48.18662509608405031, 28.59624452788247950, 49.18364984542562013 ) ) ;
#25076=LINE ( 'NONE', #29847, #21894 ) ;
#25088=CIRCLE ( 'NONE', #970, 4.200000000000000178 ) ;
#25090=EDGE_CURVE ( 'NONE', #456, #5630, #9390, .T. ) ;
#25100=CARTESIAN_POINT ( 'NONE',  ( 45.96182992765471909, 26.60087065737812040, 44.82232689504102296 ) ) ;
#25101=CARTESIAN_POINT ( 'NONE',  ( 45.79384627280941089, 26.37957786121582160, 49.05938063676249072 ) ) ;
#25103=ORIENTED_EDGE ( 'NONE', *, *, #29521, .F. ) ;
#25109=DIRECTION ( 'NONE',  ( -0.09590798424311161585, 0.9774730502038649904, -0.1880108898004995421 ) ) ;
#25119=CARTESIAN_POINT ( 'NONE',  ( 44.70507715278255034, 28.44951373492759217, 46.92503878583765697 ) ) ;
#25120=ADVANCED_FACE ( 'NONE', ( #9151 ), #24695, .T. ) ;
#25135=CARTESIAN_POINT ( 'NONE',  ( 48.83862994770794330, 25.94118040159426641, 48.17861352429476796 ) ) ;
#25141=FACE_OUTER_BOUND ( 'NONE', #8487, .T. ) ;
#25145=LINE ( 'NONE', #29748, #10512 ) ;
#25147=LINE ( 'NONE', #10867, #4748 ) ;
#25164=CARTESIAN_POINT ( 'NONE',  ( 44.70507715278255745, 25.64951373492759856, 46.92503878583764987 ) ) ;
#25165=CIRCLE ( 'NONE', #16750, 2.499999999999997335 ) ;
#25166=DIRECTION ( 'NONE',  ( -0.9761574614375595482, -0.2110602665713100512, -0.05069688703093144094 ) ) ;
#25175=VECTOR ( 'NONE', #25166, 1000.000000000000114 ) ;
#25183=DIRECTION ( 'NONE',  ( -0.2029548553014555723, 0.9702957262759968060, -0.1316644609608115524 ) ) ;
#25184=ORIENTED_EDGE ( 'NONE', *, *, #6521, .T. ) ;
#25200=ORIENTED_EDGE ( 'NONE', *, *, #1951, .T. ) ;
#25201=CARTESIAN_POINT ( 'NONE',  ( 47.09785597605719687, 24.86454579224779593, 47.04930799450078638 ) ) ;
#25202=EDGE_CURVE ( 'NONE', #11589, #13067, #29404, .T. ) ;
#25218=CARTESIAN_POINT ( 'NONE',  ( 46.96819297411687444, 26.06988759933319244, 49.54594323136014822 ) ) ;
#25230=LINE ( 'NONE', #5205, #29075 ) ;
#25235=LINE ( 'NONE', #5052, #17878 ) ;
#25239=CARTESIAN_POINT ( 'NONE',  ( 47.20547626766766314, 26.78791119454915659, 44.97710074790751378 ) ) ;
#25256=EDGE_LOOP ( 'NONE', ( #3951, #30894, #23864, #8762, #15244, #29268, #15038, #24226 ) ) ;
#25257=CARTESIAN_POINT ( 'NONE',  ( 46.04327488119035650, 22.93807716476589675, 48.37782978030396208 ) ) ;
#25260=CARTESIAN_POINT ( 'NONE',  ( 47.78944874062793247, 29.51560991843770765, 45.00889955171861345 ) ) ;
#25263=CARTESIAN_POINT ( 'NONE',  ( 44.74832014356462651, 29.78456182964375643, 46.92728461490987257 ) ) ;
#25281=CARTESIAN_POINT ( 'NONE',  ( 46.96819297411687444, 28.99253733014355561, 49.54594323136014822 ) ) ;
#25286=CARTESIAN_POINT ( 'NONE',  ( 45.79384627280941089, 27.86618040159426357, 49.05938063676250493 ) ) ;
#25287=ORIENTED_EDGE ( 'NONE', *, *, #30507, .F. ) ;
#25288=CARTESIAN_POINT ( 'NONE',  ( 44.79156314060809763, 19.96454579224779380, 46.92953032342012420 ) ) ;
#25299=CARTESIAN_POINT ( 'NONE',  ( 48.18662509608405031, 25.18284706826093355, 49.18364984542562013 ) ) ;
#25305=DIRECTION ( 'NONE',  ( 1.234978253042719660E-16, -1.000000000000000000, -1.109335647967047851E-31 ) ) ;
#25306=ADVANCED_FACE ( 'NONE', ( #16858 ), #15812, .F. ) ;
#25313=FACE_OUTER_BOUND ( 'NONE', #24265, .T. ) ;
#25330=CARTESIAN_POINT ( 'NONE',  ( 48.83862994770794330, 27.34118040159426499, 48.17861352429476796 ) ) ;
#25331=CARTESIAN_POINT ( 'NONE',  ( 48.40186567930498285, 29.52957786121581307, 45.03923535223908203 ) ) ;
#25360=VERTEX_POINT ( 'NONE', #15697 ) ;
#25365=DIRECTION ( 'NONE',  ( 0.4544104193609900810, 0.000000000000000000, 0.8907924397839089847 ) ) ;
#25372=VERTEX_POINT ( 'NONE', #25872 ) ;
#25377=ORIENTED_EDGE ( 'NONE', *, *, #19135, .T. ) ;
#25388=CARTESIAN_POINT ( 'NONE',  ( 47.45244889970129520, 23.03451764446790051, 45.89330396155958169 ) ) ;
#25393=CARTESIAN_POINT ( 'NONE',  ( 48.83862994770794330, 27.25457786121582160, 48.17861352429476796 ) ) ;
#25402=CARTESIAN_POINT ( 'NONE',  ( 45.52675994804781112, 28.23420399681022275, 49.47108226228596806 ) ) ;
#25412=ORIENTED_EDGE ( 'NONE', *, *, #21958, .F. ) ;
#25422=CARTESIAN_POINT ( 'NONE',  ( 48.83862994770794330, 26.55457786121582231, 48.17861352429476796 ) ) ;
#25433=CARTESIAN_POINT ( 'NONE',  ( 47.19823469859255738, 22.88065857334294861, 45.11653766655789610 ) ) ;
#25440=CARTESIAN_POINT ( 'NONE',  ( 48.18662509608405742, 27.28284706826093142, 49.18364984542562013 ) ) ;
#25443=PLANE ( 'NONE',  #20348 ) ;
#25450=ADVANCED_FACE ( 'NONE', ( #22761 ), #5125, .T. ) ;
#25470=CARTESIAN_POINT ( 'NONE',  ( 45.73035263060504718, 28.63954579807170475, 44.36855633853329550 ) ) ;
#25477=CARTESIAN_POINT ( 'NONE',  ( 49.53646239908485427, 24.96864685363938818, 46.22604428272304489 ) ) ;
#25482=FACE_OUTER_BOUND ( 'NONE', #18471, .T. ) ;
#25487=CARTESIAN_POINT ( 'NONE',  ( 45.35708200440645044, 27.69118040159426286, 45.92000246470679770 ) ) ;
#25488=CARTESIAN_POINT ( 'NONE',  ( 49.49063479933183629, 29.41291119454914593, 47.17357720316391578 ) ) ;
#25496=CARTESIAN_POINT ( 'NONE',  ( 47.40175035182062402, 22.86454579224780659, 49.06778623913097448 ) ) ;
#25526=CARTESIAN_POINT ( 'NONE',  ( 48.73394074504988538, 22.89977464660286444, 47.94256374451057212 ) ) ;
#25543=VERTEX_POINT ( 'NONE', #31287 ) ;
#25544=CARTESIAN_POINT ( 'NONE',  ( 47.09785597605719687, 15.77906836436399374, 47.04930799450078638 ) ) ;
#25546=FACE_BOUND ( 'NONE', #10023, .T. ) ;
#25554=CARTESIAN_POINT ( 'NONE',  ( 48.23388202445966044, 28.92822092656773947, 49.27628909396054979 ) ) ;
#25558=CARTESIAN_POINT ( 'NONE',  ( 44.87087493598345134, 28.17587066347689273, 48.18533415931919706 ) ) ;
#25570=EDGE_CURVE ( 'NONE', #26305, #28677, #28821, .T. ) ;
#25578=CARTESIAN_POINT ( 'NONE',  ( 48.16694854572211426, 28.61789516297709568, 49.14507740233662503 ) ) ;
#25587=DIRECTION ( 'NONE',  ( 0.4544104193609900810, 5.611869858668441979E-17, 0.8907924397839090958 ) ) ;
#25629=CARTESIAN_POINT ( 'NONE',  ( 48.73570333863616355, 28.52287913140503761, 44.52463952959527660 ) ) ;
#25639=CARTESIAN_POINT ( 'NONE',  ( 49.19517401419062708, 28.28655426599985390, 48.40991706654173754 ) ) ;
#25643=CARTESIAN_POINT ( 'NONE',  ( 45.24946171279598417, 28.50784706826092929, 47.99220971130007030 ) ) ;
#25646=CARTESIAN_POINT ( 'NONE',  ( 45.24946171279598417, 27.72124452788248661, 47.99220971130007030 ) ) ;
#25651=CARTESIAN_POINT ( 'NONE',  ( 47.09785597605719687, 15.77906836436399374, 47.04930799450078638 ) ) ;
#25676=CARTESIAN_POINT ( 'NONE',  ( 49.69886365972154607, 24.87071433478734406, 46.18560630082799889 ) ) ;
#25698=CARTESIAN_POINT ( 'NONE',  ( 47.20677300731728820, 19.86454579224779948, 44.95213440123257698 ) ) ;
#25730=EDGE_CURVE ( 'NONE', #7293, #15887, #31051, .T. ) ;
#25743=CARTESIAN_POINT ( 'NONE',  ( 48.50919455764776700, 22.98879437201065912, 47.45523895251538704 ) ) ;
#25744=CARTESIAN_POINT ( 'NONE',  ( 49.56570964645655408, 29.19876898723385139, 46.93360586032942194 ) ) ;
#25746=CARTESIAN_POINT ( 'NONE',  ( 48.91284552371730143, 25.29289516297709994, 46.12344667017377020 ) ) ;
#25764=VERTEX_POINT ( 'NONE', #30128 ) ;
#25799=CARTESIAN_POINT ( 'NONE',  ( 45.82550680184641578, 24.86454579224779593, 44.55508916310584056 ) ) ;
#25804=CARTESIAN_POINT ( 'NONE',  ( 44.77625694075214824, 29.51454579807170120, 48.23360063142255427 ) ) ;
#25805=CARTESIAN_POINT ( 'NONE',  ( 45.24946171279598417, 29.82124452788248092, 47.99220971130007030 ) ) ;
#25813=VECTOR ( 'NONE', #21820, 1000.000000000000000 ) ;
#25816=CARTESIAN_POINT ( 'NONE',  ( 46.33206787849857022, 22.99884124225578574, 48.22973596570440691 ) ) ;
#25828=CARTESIAN_POINT ( 'NONE',  ( 46.81682104422132085, 23.12036939723557083, 47.03471240234085116 ) ) ;
#25848=( BOUNDED_CURVE ( )  B_SPLINE_CURVE ( 3, ( #19014, #14279, #18852, #6716 ),
 .UNSPECIFIED., .F., .F. ) 
 B_SPLINE_CURVE_WITH_KNOTS ( ( 4, 4 ),
 ( 5.062864179022700029, 5.184122060454620318 ),
 .UNSPECIFIED. ) 
 CURVE ( )  GEOMETRIC_REPRESENTATION_ITEM ( )  RATIONAL_B_SPLINE_CURVE ( ( 1.000000000000000000, 0.9987750858034806223, 0.9987750858034806223, 1.000000000000000000 ) ) 
 REPRESENTATION_ITEM ( '' )  );
#25854=CARTESIAN_POINT ( 'NONE',  ( 48.66895200406656841, 27.06155426599985958, 44.62753372671560470 ) ) ;
#25862=DIRECTION ( 'NONE',  ( 0.4544104193609903586, 0.000000000000000000, 0.8907924397839087627 ) ) ;
#25866=ORIENTED_EDGE ( 'NONE', *, *, #17634, .F. ) ;
#25872=CARTESIAN_POINT ( 'NONE',  ( 48.23388202445966755, 26.95087065737812182, 49.27628909396054979 ) ) ;
#25873=LINE ( 'NONE', #20461, #12098 ) ;
#25877=CARTESIAN_POINT ( 'NONE',  ( 45.79384627280941089, 25.67957786121582231, 49.05938063676249072 ) ) ;
#25881=CARTESIAN_POINT ( 'NONE',  ( 49.40414881150629611, 22.80400562401889530, 47.16908566558144855 ) ) ;
#25883=B_SPLINE_CURVE_WITH_KNOTS ( 'NONE', 3,
 ( #7683, #9650, #7182, #19807, #27196, #24746 ),
 .UNSPECIFIED., .F., .F.,
 ( 4, 2, 4 ),
 ( 0.000000000000000000, 0.5000000000000000000, 1.000000000000000000 ),
 .UNSPECIFIED. ) ;
#25898=ORIENTED_EDGE ( 'NONE', *, *, #11930, .F. ) ;
#25903=CARTESIAN_POINT ( 'NONE',  ( 46.02876340639226527, 26.16789516297709639, 44.95353858666495483 ) ) ;
#25915=AXIS2_PLACEMENT_3D ( 'NONE', #10053, #14813, #29583 ) ;
#25918=CARTESIAN_POINT ( 'NONE',  ( 46.99023568444674481, 25.82451373492760283, 49.12151524109405898 ) ) ;
#25940=ORIENTED_EDGE ( 'NONE', *, *, #26011, .F. ) ;
#25941=CARTESIAN_POINT ( 'NONE',  ( 45.36511207810799107, 27.33213139976340500, 45.12672418911605376 ) ) ;
#25953=CARTESIAN_POINT ( 'NONE',  ( 47.22751897799751220, 28.51988759933318818, 44.55267275764142454 ) ) ;
#25958=CARTESIAN_POINT ( 'NONE',  ( 48.73570333863616355, 27.82287913140503832, 44.52463952959527660 ) ) ;
#25960=AXIS2_PLACEMENT_3D ( 'NONE', #15864, #10631, #5864 ) ;
#25985=CARTESIAN_POINT ( 'NONE',  ( 47.20547626766765603, 29.58791119454915020, 44.97710074790751378 ) ) ;
#25991=CARTESIAN_POINT ( 'NONE',  ( 47.24492228087488144, 29.61131241985434670, 45.00104688274142006 ) ) ;
#25996=CARTESIAN_POINT ( 'NONE',  ( 48.23388202445966755, 15.77906836436399374, 49.27628909396055690 ) ) ;
#26011=EDGE_CURVE ( 'NONE', #16189, #32468, #9893, .T. ) ;
#26022=DIRECTION ( 'NONE',  ( 0.4114095458597712973, 0.6546536707079773088, -0.6341693441061526659 ) ) ;
#26044=ADVANCED_FACE ( 'NONE', ( #29928 ), #22295, .T. ) ;
#26054=CARTESIAN_POINT ( 'NONE',  ( 44.74832014356462651, 25.58456182964376779, 46.92728461490987257 ) ) ;
#26062=CARTESIAN_POINT ( 'NONE',  ( 49.40414881150629611, 22.80400562401889530, 47.16908566558144855 ) ) ;
#26073=CARTESIAN_POINT ( 'NONE',  ( 48.79980305660560447, 22.93328494799376571, 46.81390877062097644 ) ) ;
#26077=ORIENTED_EDGE ( 'NONE', *, *, #14891, .T. ) ;
#26098=CARTESIAN_POINT ( 'NONE',  ( 47.23884743062419744, 22.86454579224779948, 45.05393496349946503 ) ) ;
#26108=ORIENTED_EDGE ( 'NONE', *, *, #23027, .F. ) ;
#26115=DIRECTION ( 'NONE',  ( 0.4544104193609905806, 5.611869858668446909E-17, 0.8907924397839086517 ) ) ;
#26118=CARTESIAN_POINT ( 'NONE',  ( 45.46000861347822308, 27.47287913140503690, 49.57397645940629616 ) ) ;
#26122=AXIS2_PLACEMENT_3D ( 'NONE', #22967, #2949, #2637 ) ;
#26124=EDGE_CURVE ( 'NONE', #25360, #15904, #12490, .T. ) ;
#26131=CARTESIAN_POINT ( 'NONE',  ( 49.32483701613094240, 28.52587066347689415, 45.91328182968236860 ) ) ;
#26142=CARTESIAN_POINT ( 'NONE',  ( 48.23388202445966044, 28.35087065737811685, 49.27628909396054979 ) ) ;
#26153=CARTESIAN_POINT ( 'NONE',  ( 48.15252827834996907, 29.60698769386672424, 45.26040870260538895 ) ) ;
#26154=CARTESIAN_POINT ( 'NONE',  ( 49.66186032787856419, 24.92772031883689010, 46.53160128828346132 ) ) ;
#26155=CARTESIAN_POINT ( 'NONE',  ( 48.41757674592806637, 19.86454579224779948, 45.01501767854993119 ) ) ;
#26158=CARTESIAN_POINT ( 'NONE',  ( 48.19974268340787660, 19.86454579224779948, 49.20936486508634289 ) ) ;
#26159=CARTESIAN_POINT ( 'NONE',  ( 48.83059987400639557, 28.95948166895302833, 48.97189179988551899 ) ) ;
#26192=CARTESIAN_POINT ( 'NONE',  ( 48.83862994770794330, 25.85457786121582302, 48.17861352429476796 ) ) ;
#26194=CARTESIAN_POINT ( 'NONE',  ( 47.37889090789306579, 23.12036939723557083, 47.06390358666074292 ) ) ;
#26197=FACE_OUTER_BOUND ( 'NONE', #30371, .T. ) ;
#26212=ORIENTED_EDGE ( 'NONE', *, *, #15958, .F. ) ;
#26217=CARTESIAN_POINT ( 'NONE',  ( 48.54667866842090973, 22.95310733321322161, 47.81819468219185865 ) ) ;
#26220=CARTESIAN_POINT ( 'NONE',  ( 45.28286642839709231, 27.04289516297709639, 47.97516931882780966 ) ) ;
#26228=VECTOR ( 'NONE', #612, 1000.000000000000000 ) ;
#26234=( BOUNDED_SURFACE ( )  B_SPLINE_SURFACE ( 1, 2, ( 
 ( #29443, #27132, #29937, #7451, #26811, #2359, #4328, #32235, #12378, #17278, #9415, #12040, #6952, #24502, #7114, #27300, #4817, #22365, #5472, #5623, #28272, #18238, #10391, #27952, #25643, #5791, #20232, #22527, #3146, #22856, #17770, #2512, #10723, #8097, #15473, #15797, #12539, #58, #25487, #12711, #369, #23183, #5142, #20073, #25330, #20390, #13191, #5311, #10564, #27789, #10076, #2680, #30102, #698, #7610, #2988, #20716, #13019, #17933, #15624, #30744, #30257, #2833, #17609, #27626, #23015, #15316, #8251, #15155, #7769, #20554, #12865, #533, #25164, #22700, #216, #10236, #30420, #7937, #30585, #18091, #28118, #13822, #28436, #3638 ),
 ( #8570, #28921, #18562, #28591, #30898, #11507, #11196, #16269, #21506, #16430, #13345, #6103, #25804, #26288, #29069, #16104, #3315, #23978, #8411, #21027, #18406, #5956, #31544, #6428, #1489, #23502, #15950, #23344, #3474, #21179, #855, #31225, #3795, #8726, #23813, #26444, #10880, #31376, #1331, #20870, #19044, #25958, #9050, #11353, #1169, #18882, #13983, #26118, #13663, #3962, #18714, #13502, #6590, #1015, #11041, #28745, #6263, #31060, #23665, #21338, #8884, #9705, #11682, #12333, #29403, #11842, #9374, #29231, #2154, #16584, #19370, #6745, #24796, #21835, #24307, #31858, #32355, #14307, #7074, #26934, #16745, #9864, #21992, #26771, #29569 ) ),
 .UNSPECIFIED., .F., .F., .F. ) 
 B_SPLINE_SURFACE_WITH_KNOTS ( ( 2, 2 ),
 ( 3, 2, 2, 2, 2, 2, 2, 2, 2, 2, 2, 2, 2, 2, 2, 2, 2, 2, 2, 2, 2, 2, 2, 2, 2, 2, 2, 2, 2, 2, 2, 2, 2, 2, 2, 2, 2, 2, 2, 2, 2, 2, 3 ),
 ( 0.000000000000000000, 1.000000000000000000 ),
 ( 0.000000000000000000, 0.02380952380952380820, 0.04761904761904761640, 0.07142857142857142461, 0.09523809523809523281, 0.1190476190476190410, 0.1428571428571428492, 0.1666666666666666574, 0.1904761904761904656, 0.2142857142857142738, 0.2380952380952380820, 0.2619047619047619180, 0.2857142857142856984, 0.3095238095238095344, 0.3333333333333333148, 0.3571428571428571508, 0.3809523809523809312, 0.4047619047619047672, 0.4285714285714285476, 0.4523809523809523836, 0.4761904761904761640, 0.5000000000000000000, 0.5238095238095238360, 0.5476190476190476719, 0.5714285714285713969, 0.5952380952380952328, 0.6190476190476190688, 0.6428571428571429047, 0.6666666666666666297, 0.6904761904761904656, 0.7142857142857143016, 0.7380952380952381375, 0.7619047619047618625, 0.7857142857142856984, 0.8095238095238095344, 0.8333333333333333703, 0.8571428571428570953, 0.8809523809523809312, 0.9047619047619047672, 0.9285714285714286031, 0.9523809523809523281, 0.9761904761904761640, 1.000000000000000000 ),
 .UNSPECIFIED. ) 
 GEOMETRIC_REPRESENTATION_ITEM ( )  RATIONAL_B_SPLINE_SURFACE ( (
 ( 1.000000000000000000, 0.8660254037844387076, 1.000000000000000000, 0.8660254037844387076, 1.000000000000000000, 0.8660254037844387076, 1.000000000000000000, 0.8660254037844387076, 1.000000000000000000, 0.8660254037844387076, 1.000000000000000000, 0.8660254037844387076, 1.000000000000000000, 0.8660254037844387076, 1.000000000000000000, 0.8660254037844387076, 1.000000000000000000, 0.8660254037844387076, 1.000000000000000000, 0.8660254037844387076, 1.000000000000000000, 0.8660254037844387076, 1.000000000000000000, 0.8660254037844387076, 1.000000000000000000, 0.8660254037844387076, 1.000000000000000000, 0.8660254037844387076, 1.000000000000000000, 0.8660254037844387076, 1.000000000000000000, 0.8660254037844387076, 1.000000000000000000, 0.8660254037844387076, 1.000000000000000000, 0.8660254037844387076, 1.000000000000000000, 0.8660254037844387076, 1.000000000000000000, 0.8660254037844387076, 1.000000000000000000, 0.8660254037844387076, 1.000000000000000000, 0.8660254037844387076, 1.000000000000000000, 0.8660254037844387076, 1.000000000000000000, 0.8660254037844387076, 1.000000000000000000, 0.8660254037844387076, 1.000000000000000000, 0.8660254037844387076, 1.000000000000000000, 0.8660254037844387076, 1.000000000000000000, 0.8660254037844387076, 1.000000000000000000, 0.8660254037844387076, 1.000000000000000000, 0.8660254037844387076, 1.000000000000000000, 0.8660254037844387076, 1.000000000000000000, 0.8660254037844387076, 1.000000000000000000, 0.8660254037844387076, 1.000000000000000000, 0.8660254037844387076, 1.000000000000000000, 0.8660254037844387076, 1.000000000000000000, 0.8660254037844387076, 1.000000000000000000, 0.8660254037844387076, 1.000000000000000000, 0.8660254037844387076, 1.000000000000000000, 0.8660254037844387076, 1.000000000000000000, 0.8660254037844387076, 1.000000000000000000, 0.8660254037844387076, 1.000000000000000000, 0.8660254037844387076, 1.000000000000000000),
 ( 1.000000000000000000, 0.8660254037844387076, 1.000000000000000000, 0.8660254037844387076, 1.000000000000000000, 0.8660254037844387076, 1.000000000000000000, 0.8660254037844387076, 1.000000000000000000, 0.8660254037844387076, 1.000000000000000000, 0.8660254037844387076, 1.000000000000000000, 0.8660254037844387076, 1.000000000000000000, 0.8660254037844387076, 1.000000000000000000, 0.8660254037844387076, 1.000000000000000000, 0.8660254037844387076, 1.000000000000000000, 0.8660254037844387076, 1.000000000000000000, 0.8660254037844387076, 1.000000000000000000, 0.8660254037844387076, 1.000000000000000000, 0.8660254037844387076, 1.000000000000000000, 0.8660254037844387076, 1.000000000000000000, 0.8660254037844387076, 1.000000000000000000, 0.8660254037844387076, 1.000000000000000000, 0.8660254037844387076, 1.000000000000000000, 0.8660254037844387076, 1.000000000000000000, 0.8660254037844387076, 1.000000000000000000, 0.8660254037844387076, 1.000000000000000000, 0.8660254037844387076, 1.000000000000000000, 0.8660254037844387076, 1.000000000000000000, 0.8660254037844387076, 1.000000000000000000, 0.8660254037844387076, 1.000000000000000000, 0.8660254037844387076, 1.000000000000000000, 0.8660254037844387076, 1.000000000000000000, 0.8660254037844387076, 1.000000000000000000, 0.8660254037844387076, 1.000000000000000000, 0.8660254037844387076, 1.000000000000000000, 0.8660254037844387076, 1.000000000000000000, 0.8660254037844387076, 1.000000000000000000, 0.8660254037844387076, 1.000000000000000000, 0.8660254037844387076, 1.000000000000000000, 0.8660254037844387076, 1.000000000000000000, 0.8660254037844387076, 1.000000000000000000, 0.8660254037844387076, 1.000000000000000000, 0.8660254037844387076, 1.000000000000000000, 0.8660254037844387076, 1.000000000000000000, 0.8660254037844387076, 1.000000000000000000, 0.8660254037844387076, 1.000000000000000000, 0.8660254037844387076, 1.000000000000000000) ) ) 
 REPRESENTATION_ITEM ( '' )  SURFACE ( )  );
#26258=CARTESIAN_POINT ( 'NONE',  ( 48.82187354100420151, 22.88065857334294861, 46.16985335424439540 ) ) ;
#26288=CARTESIAN_POINT ( 'NONE',  ( 44.09250526802607340, 29.45621246473837118, 46.89322480343881949 ) ) ;
#26291=ORIENTED_EDGE ( 'NONE', *, *, #3712, .T. ) ;
#26297=CARTESIAN_POINT ( 'NONE',  ( 48.91284552371730143, 25.33619643316631809, 46.12344667017377020 ) ) ;
#26300=FACE_OUTER_BOUND ( 'NONE', #762, .T. ) ;
#26305=VERTEX_POINT ( 'NONE', #7066 ) ;
#26309=LINE ( 'NONE', #3818, #13641 ) ;
#26313=CARTESIAN_POINT ( 'NONE',  ( 44.70507715278255034, 26.96291119454915020, 46.92503878583765697 ) ) ;
#26316=CARTESIAN_POINT ( 'NONE',  ( 48.75540398364718442, 22.86454579224779948, 48.16909669137300654 ) ) ;
#26346=DIRECTION ( 'NONE',  ( 0.9761574614375596592, 0.2110602665713100512, 0.05069688703093144788 ) ) ;
#26351=CARTESIAN_POINT ( 'NONE',  ( 46.59775284999513900, 22.99884124225578930, 45.72485089329623520 ) ) ;
#26375=ORIENTED_EDGE ( 'NONE', *, *, #12086, .T. ) ;
#26388=CARTESIAN_POINT ( 'NONE',  ( 46.99218062947583974, 27.20286309983298878, 49.08406571254116102 ) ) ;
#26397=CARTESIAN_POINT ( 'NONE',  ( 44.09250526802607340, 26.65621246473837402, 46.89322480343881949 ) ) ;
#26409=EDGE_CURVE ( 'NONE', #18170, #1048, #4598, .T. ) ;
#26418=VERTEX_POINT ( 'NONE', #24132 ) ;
#26422=( BOUNDED_CURVE ( )  B_SPLINE_CURVE ( 2, ( #31244, #1040, #14169, #1353, #6285, #13521, #21696, #29095, #26468 ),
 .UNSPECIFIED., .F., .F. ) 
 B_SPLINE_CURVE_WITH_KNOTS ( ( 3, 2, 2, 2, 3 ),
 ( 0.8214285725898440305, 0.8333333333333333703, 0.8571428571428570953, 0.8809523809523809312, 0.8928571440184154273 ),
 .UNSPECIFIED. ) 
 CURVE ( )  GEOMETRIC_REPRESENTATION_ITEM ( )  RATIONAL_B_SPLINE_CURVE ( ( 0.9330127018922200755, 0.9330127084266224280, 1.000000000000000000, 0.8660254037844388186, 1.000000000000000000, 0.8660254037844388186, 1.000000000000000000, 0.9330126953578163906, 0.9330127018922200755 ) ) 
 REPRESENTATION_ITEM ( '' )  );
#26425=EDGE_CURVE ( 'NONE', #19411, #18170, #17228, .T. ) ;
#26434=VERTEX_POINT ( 'NONE', #27243 ) ;
#26438=PLANE ( 'NONE',  #6220 ) ;
#26444=CARTESIAN_POINT ( 'NONE',  ( 45.46000861347822308, 28.17287913140503619, 49.57397645940629616 ) ) ;
#26455=DIRECTION ( 'NONE',  ( -0.5319835227803569877, -0.2110602665713105230, 0.8200287161831886218 ) ) ;
#26458=CARTESIAN_POINT ( 'NONE',  ( 48.40186567930498285, 28.91618040159426073, 45.03923535223908203 ) ) ;
#26468=CARTESIAN_POINT ( 'NONE',  ( 45.96182992765471909, 25.20087065737812182, 44.82232689504102296 ) ) ;
#26474=CARTESIAN_POINT ( 'NONE',  ( 45.79384627280941089, 29.17957786121581165, 49.05938063676249072 ) ) ;
#26479=ORIENTED_EDGE ( 'NONE', *, *, #12241, .T. ) ;
#26524=EDGE_CURVE ( 'NONE', #22685, #20447, #24802, .T. ) ;
#26528=PRODUCT_DEFINITION_FORMATION_WITH_SPECIFIED_SOURCE ( 'ANY', '', #7490, .NOT_KNOWN. ) ;
#26544=CARTESIAN_POINT ( 'NONE',  ( 46.02876340639226527, 27.61119643316632022, 44.95353858666495483 ) ) ;
#26546=ORIENTED_EDGE ( 'NONE', *, *, #28875, .T. ) ;
#26555=CARTESIAN_POINT ( 'NONE',  ( 46.96268396749378127, 25.43121246473837971, 49.65201805493727960 ) ) ;
#26562=CARTESIAN_POINT ( 'NONE',  ( 48.81241343884743600, 22.91413368675619111, 46.49136847324655974 ) ) ;
#26563=CARTESIAN_POINT ( 'NONE',  ( 49.98072202819531640, 25.54488759933319386, 47.19902993264913960 ) ) ;
#26564=ORIENTED_EDGE ( 'NONE', *, *, #30357, .T. ) ;
#26587=DIRECTION ( 'NONE',  ( -0.8907924397839086517, -1.100109291107993817E-16, 0.4544104193609908027 ) ) ;
#26615=CARTESIAN_POINT ( 'NONE',  ( 48.94625023931840246, 29.55784706826092645, 46.10640627770150246 ) ) ;
#26621=CARTESIAN_POINT ( 'NONE',  ( 46.96819297411687444, 26.76988759933318818, 49.54594323136014822 ) ) ;
#26624=DIRECTION ( 'NONE',  ( 0.7549115352271290602, -0.6546536707079775308, 0.03920644602090544995 ) ) ;
#26629=CIRCLE ( 'NONE', #446, 4.100000000000001421 ) ;
#26630=CARTESIAN_POINT ( 'NONE',  ( 45.35708200440645044, 26.20457786121582444, 45.92000246470680480 ) ) ;
#26633=CARTESIAN_POINT ( 'NONE',  ( 45.60118599681192109, 25.28986642951281638, 49.35635783644741537 ) ) ;
#26646=CARTESIAN_POINT ( 'NONE',  ( 46.61910388458303345, 22.93328494799376216, 45.39920705986084215 ) ) ;
#26679=ORIENTED_EDGE ( 'NONE', *, *, #16879, .T. ) ;
#26683=CYLINDRICAL_SURFACE ( 'NONE', #1495, 2.499999999999997335 ) ;
#26702=CARTESIAN_POINT ( 'NONE',  ( 46.02876340639226527, 29.71119643316631809, 44.95353858666495483 ) ) ;
#26705=VERTEX_POINT ( 'NONE', #969 ) ;
#26706=DIRECTION ( 'NONE',  ( -0.4441739386572048920, 0.2110602665713095516, -0.8707256032141200697 ) ) ;
#26717=CARTESIAN_POINT ( 'NONE',  ( 47.23302798462060537, 27.18121246473837616, 44.44659793406428605 ) ) ;
#26719=CARTESIAN_POINT ( 'NONE',  ( 47.45197874502928670, 22.98879437201065912, 48.47452853850663246 ) ) ;
#26726=CARTESIAN_POINT ( 'NONE',  ( 48.15243707092404435, 22.93807716476589675, 45.72078620869762489 ) ) ;
#26727=PLANE ( 'NONE',  #29316 ) ;
#26749=B_SPLINE_CURVE_WITH_KNOTS ( 'NONE', 3,
 ( #991, #5927, #8706, #3613 ),
 .UNSPECIFIED., .F., .F.,
 ( 4, 4 ),
 ( 0.000000000000000000, 1.000000000000000000 ),
 .UNSPECIFIED. ) ;
#26771=CARTESIAN_POINT ( 'NONE',  ( 45.46000861347822308, 25.37287913140504614, 49.57397645940629616 ) ) ;
#26780=CARTESIAN_POINT ( 'NONE',  ( 45.28286642839709231, 24.98619643316632732, 47.97516931882780966 ) ) ;
#26783=CARTESIAN_POINT ( 'NONE',  ( 47.09785597605719687, 15.77906836436399374, 47.04930799450078638 ) ) ;
#26811=CARTESIAN_POINT ( 'NONE',  ( 47.20547626766765603, 29.67451373492759004, 44.97710074790751378 ) ) ;
#26816=CARTESIAN_POINT ( 'NONE',  ( 46.19123036519361136, 29.39672067899820362, 49.13362621058115565 ) ) ;
#26818=ORIENTED_EDGE ( 'NONE', *, *, #7036, .T. ) ;
#26844=CARTESIAN_POINT ( 'NONE',  ( 48.96093869543725674, 24.76454579224779806, 50.70155699761480861 ) ) ;
#26853=ADVANCED_FACE ( 'NONE', ( #6701 ), #29350, .T. ) ;
#26856=EDGE_CURVE ( 'NONE', #16020, #5063, #25165, .T. ) ;
#26859=CIRCLE ( 'NONE', #31067, 2.499999999999997335 ) ;
#26867=CARTESIAN_POINT ( 'NONE',  ( 48.01680169312755453, 22.93807716476589675, 45.63279442905645311 ) ) ;
#26870=CARTESIAN_POINT ( 'NONE',  ( 48.37829923888483563, 29.59452976649964384, 45.07556196625585443 ) ) ;
#26881=CARTESIAN_POINT ( 'NONE',  ( 45.73035263060504718, 27.23954579807170262, 44.36855633853329550 ) ) ;
#26883=CARTESIAN_POINT ( 'NONE',  ( 46.74326305241309853, 23.03451764446789696, 48.20531202744201238 ) ) ;
#26900=AXIS2_PLACEMENT_3D ( 'NONE', #15563, #30352, #23438 ) ;
#26923=VERTEX_POINT ( 'NONE', #30936 ) ;
#26934=CARTESIAN_POINT ( 'NONE',  ( 50.10320668408830613, 25.60621246473838042, 47.20539118556276037 ) ) ;
#26943=CARTESIAN_POINT ( 'NONE',  ( 46.00908685603034343, 27.63284706826092929, 44.91496614357595263 ) ) ;
#26955=CARTESIAN_POINT ( 'NONE',  ( 45.75738744548056758, 22.91413368675619111, 45.84342743610336868 ) ) ;
#26958=CARTESIAN_POINT ( 'NONE',  ( 45.96182992765472619, 27.30087065737811969, 44.82232689504102296 ) ) ;
#26961=FACE_OUTER_BOUND ( 'NONE', #14859, .T. ) ;
#26978=EDGE_CURVE ( 'NONE', #2756, #2200, #11008, .T. ) ;
#27000=DIRECTION ( 'NONE',  ( 0.5932111027100931411, 0.7071067811865471286, 0.3848383915638819985 ) ) ;
#27002=DIRECTION ( 'NONE',  ( 1.234978253042719660E-16, -1.000000000000000000, -1.109335647967047851E-31 ) ) ;
#27008=ORIENTED_EDGE ( 'NONE', *, *, #27068, .F. ) ;
#27030=DIRECTION ( 'NONE',  ( 0.5442436726714897643, 1.289618226626749726E-16, -0.8389271868029121171 ) ) ;
#27042=CARTESIAN_POINT ( 'NONE',  ( 44.91142894931555674, 27.29787913140504330, 45.63089057098605394 ) ) ;
#27043=CARTESIAN_POINT ( 'NONE',  ( 47.22573328838134188, 23.12036939723557083, 47.29998918090146987 ) ) ;
#27044=CARTESIAN_POINT ( 'NONE',  ( 45.22719185251098395, 19.86454579224779948, 48.00356987515886686 ) ) ;
#27046=CARTESIAN_POINT ( 'NONE',  ( 47.14149656544282863, 29.59378199361933781, 44.97899958470305393 ) ) ;
#27068=EDGE_CURVE ( 'NONE', #18631, #13067, #11385, .T. ) ;
#27076=LINE ( 'NONE', #6412, #25813 ) ;
#27087=EDGE_LOOP ( 'NONE', ( #1098, #1097, #11430, #26291 ) ) ;
#27091=FACE_OUTER_BOUND ( 'NONE', #11880, .T. ) ;
#27095=( BOUNDED_CURVE ( )  B_SPLINE_CURVE ( 2, ( #19873, #29906, #4953, #2483, #12512, #30068, #8223, #31033, #8380 ),
 .UNSPECIFIED., .F., .F. ) 
 B_SPLINE_CURVE_WITH_KNOTS ( ( 3, 2, 2, 2, 3 ),
 ( 0.3214285725898440860, 0.3333333333333333148, 0.3571428571428571508, 0.3809523809523809312, 0.3928571440184155938 ),
 .UNSPECIFIED. ) 
 CURVE ( )  GEOMETRIC_REPRESENTATION_ITEM ( )  RATIONAL_B_SPLINE_CURVE ( ( 0.9330127018922200755, 0.9330127084266228721, 1.000000000000000000, 0.8660254037844388186, 1.000000000000000000, 0.8660254037844388186, 1.000000000000000000, 0.9330126953578155025, 0.9330127018922200755 ) ) 
 REPRESENTATION_ITEM ( '' )  );
#27102=CARTESIAN_POINT ( 'NONE',  ( 46.99023568444673060, 26.52451373492759856, 49.12151524109405898 ) ) ;
#27115=PRODUCT_DEFINITION_SHAPE ( 'NONE', 'NONE',  #18711 ) ;
#27130=ORIENTED_EDGE ( 'NONE', *, *, #7981, .F. ) ;
#27132=CARTESIAN_POINT ( 'NONE',  ( 44.70507715278255745, 29.84951373492758719, 46.92503878583764987 ) ) ;
#27137=CARTESIAN_POINT ( 'NONE',  ( 45.19905222922426447, 29.26819764828676895, 45.57955500106713487 ) ) ;
#27151=AXIS2_PLACEMENT_3D ( 'NONE', #4244, #6544, #28871 ) ;
#27156=DIRECTION ( 'NONE',  ( 1.234978253042719660E-16, -1.000000000000000000, -1.109335647967047851E-31 ) ) ;
#27192=DIRECTION ( 'NONE',  ( 1.234978253042719660E-16, -1.000000000000000000, -1.109335647967047851E-31 ) ) ;
#27195=CARTESIAN_POINT ( 'NONE',  ( 47.86511985000206693, 22.93807716476589320, 48.55339511290479493 ) ) ;
#27196=CARTESIAN_POINT ( 'NONE',  ( 46.31454563678332903, 22.93807716476589675, 48.55381333958629142 ) ) ;
#27200=CARTESIAN_POINT ( 'NONE',  ( 45.24946171279598417, 26.32124452788248803, 47.99220971130007030 ) ) ;
#27205=VERTEX_POINT ( 'NONE', #2511 ) ;
#27218=CARTESIAN_POINT ( 'NONE',  ( 45.38329851326696485, 22.91413368675619111, 47.60724751575505564 ) ) ;
#27224=ORIENTED_EDGE ( 'NONE', *, *, #17213, .T. ) ;
#27228=CARTESIAN_POINT ( 'NONE',  ( 49.98072202819530219, 26.36753733014356271, 47.19902993264913960 ) ) ;
#27229=CARTESIAN_POINT ( 'NONE',  ( 48.40186567930498285, 26.72957786121581947, 45.03923535223908203 ) ) ;
#27231=ORIENTED_EDGE ( 'NONE', *, *, #21792, .T. ) ;
#27238=CARTESIAN_POINT ( 'NONE',  ( 44.70507715278255034, 26.26291119454915091, 46.92503878583765697 ) ) ;
#27243=CARTESIAN_POINT ( 'NONE',  ( 48.04075769285628894, 25.09624452788247950, 48.89770225776209855 ) ) ;
#27246=CARTESIAN_POINT ( 'NONE',  ( 46.99023568444673060, 28.62451373492759643, 49.12151524109405898 ) ) ;
#27260=ORIENTED_EDGE ( 'NONE', *, *, #26011, .T. ) ;
#27265=B_SPLINE_CURVE_WITH_KNOTS ( 'NONE', 3,
 ( #27195, #12610, #21939, #24745, #29840, #22601 ),
 .UNSPECIFIED., .F., .F.,
 ( 4, 2, 4 ),
 ( 0.000000000000000000, 0.5000000000000000000, 1.000000000000000000 ),
 .UNSPECIFIED. ) ;
#27289=CARTESIAN_POINT ( 'NONE',  ( 49.84415473660248352, 24.82319976284615137, 47.19193729663540893 ) ) ;
#27291=CARTESIAN_POINT ( 'NONE',  ( 47.09785597605719687, 20.36454579224779948, 47.04930799450078638 ) ) ;
#27300=CARTESIAN_POINT ( 'NONE',  ( 46.00908685603034343, 29.03284706826092787, 44.91496614357595263 ) ) ;
#27373=CARTESIAN_POINT ( 'NONE',  ( 46.00908685603034343, 28.24624452788248163, 44.91496614357594552 ) ) ;
#27375=DIRECTION ( 'NONE',  ( 0.4544104193609900810, 0.000000000000000000, 0.8907924397839089847 ) ) ;
#27380=AXIS2_PLACEMENT_3D ( 'NONE', #30039, #15414, #7552 ) ;
#27388=B_SPLINE_CURVE_WITH_KNOTS ( 'NONE', 3,
 ( #23482, #3291, #8231, #6087 ),
 .UNSPECIFIED., .F., .F.,
 ( 4, 4 ),
 ( 0.000000000000000000, 1.000000000000000000 ),
 .UNSPECIFIED. ) ;
#27398=TOROIDAL_SURFACE ( 'NONE', #22132, 4.099999999999999645, 0.1000000000000002554 ) ;
#27403=CARTESIAN_POINT ( 'NONE',  ( 48.94625023931840957, 27.37124452788248874, 46.10640627770150246 ) ) ;
#27421=CARTESIAN_POINT ( 'NONE',  ( 44.70507715278255034, 27.74951373492759288, 46.92503878583765697 ) ) ;
#27436=CARTESIAN_POINT ( 'NONE',  ( 47.20547626766766314, 26.87451373492759643, 44.97710074790751378 ) ) ;
#27455=ORIENTED_EDGE ( 'NONE', *, *, #12400, .F. ) ;
#27460=CARTESIAN_POINT ( 'NONE',  ( 49.98072202819530219, 27.06753733014356555, 47.19902993264913960 ) ) ;
#27473=CARTESIAN_POINT ( 'NONE',  ( 45.50224332293416296, 29.25496114406801951, 45.23743444292109217 ) ) ;
#27474=ORIENTED_EDGE ( 'NONE', *, *, #28798, .T. ) ;
#27482=PLANE ( 'NONE',  #5551 ) ;
#27536=CARTESIAN_POINT ( 'NONE',  ( 45.79384627280941089, 29.17957786121581520, 49.05938063676249072 ) ) ;
#27556=CARTESIAN_POINT ( 'NONE',  ( 45.53481149911499415, 22.92747281079970278, 47.84664715514688282 ) ) ;
#27563=CARTESIAN_POINT ( 'NONE',  ( 45.38854177497844944, 29.02622849631042712, 45.94041160078741370 ) ) ;
#27571=CARTESIAN_POINT ( 'NONE',  ( 46.82137942583813128, 14.98691807112498964, 46.50732389770341513 ) ) ;
#27583=CARTESIAN_POINT ( 'NONE',  ( 45.79384627280941089, 29.26618040159426215, 49.05938063676249072 ) ) ;
#27595=CARTESIAN_POINT ( 'NONE',  ( 48.40186567930498285, 26.81618040159426641, 45.03923535223908203 ) ) ;
#27598=CARTESIAN_POINT ( 'NONE',  ( 45.96182992765471909, 27.17822092656774302, 44.82232689504102296 ) ) ;
#27601=CARTESIAN_POINT ( 'NONE',  ( 44.21498992391908445, 27.41753733014355987, 46.89958605635242606 ) ) ;
#27611=CARTESIAN_POINT ( 'NONE',  ( 48.80400426508809630, 25.05247065798242900, 45.18571335294186042 ) ) ;
#27626=CARTESIAN_POINT ( 'NONE',  ( 47.20547626766766314, 26.17451373492760069, 44.97710074790751378 ) ) ;
#27627=CARTESIAN_POINT ( 'NONE',  ( 44.86660686226233707, 22.74928388133296409, 45.96443597445600204 ) ) ;
#27640=ORIENTED_EDGE ( 'NONE', *, *, #8416, .T. ) ;
#27673=CARTESIAN_POINT ( 'NONE',  ( 44.87087493598345134, 25.95322093266652530, 48.18533415931919706 ) ) ;
#27688=ORIENTED_EDGE ( 'NONE', *, *, #26409, .F. ) ;
#27694=CARTESIAN_POINT ( 'NONE',  ( 47.20547626766766314, 28.88791119454915091, 44.97710074790751378 ) ) ;
#27720=ADVANCED_FACE ( 'NONE', ( #27091 ), #486, .T. ) ;
#27723=CARTESIAN_POINT ( 'NONE',  ( 49.44967724995736091, 29.25019814131313822, 46.48227884171557633 ) ) ;
#27724=CARTESIAN_POINT ( 'NONE',  ( 46.55854765242722948, 26.56960992152948364, 44.51792966461572831 ) ) ;
#27725=CARTESIAN_POINT ( 'NONE',  ( 45.79384627280941089, 25.67957786121582231, 49.05938063676249072 ) ) ;
#27735=CARTESIAN_POINT ( 'NONE',  ( 47.20547626766764893, 25.38791119454915801, 44.97710074790751378 ) ) ;
#27743=CARTESIAN_POINT ( 'NONE',  ( 49.49063479933183629, 28.79951373492759359, 47.17357720316391578 ) ) ;
#27745=CARTESIAN_POINT ( 'NONE',  ( 47.09785597605719687, 15.77906836436399374, 47.04930799450078638 ) ) ;
#27746=DIRECTION ( 'NONE',  ( 0.6298853748009116682, 0.7071067811865470176, -0.3213166889719796249 ) ) ;
#27763=CARTESIAN_POINT ( 'NONE',  ( 45.52675994804781112, 26.13420399681022843, 49.47108226228596806 ) ) ;
#27771=CARTESIAN_POINT ( 'NONE',  ( 50.10320668408830613, 29.10621246473837331, 47.20539118556276037 ) ) ;
#27789=CARTESIAN_POINT ( 'NONE',  ( 44.70507715278255745, 27.04951373492760069, 46.92503878583765697 ) ) ;
#27800=EDGE_LOOP ( 'NONE', ( #6621, #25200, #8086, #30089 ) ) ;
#27816=DIRECTION ( 'NONE',  ( 0.4544104193609903586, 0.000000000000000000, 0.8907924397839087627 ) ) ;
#27860=CARTESIAN_POINT ( 'NONE',  ( 46.99031239021303463, 23.10527865767145173, 46.47233026104575515 ) ) ;
#27864=CARTESIAN_POINT ( 'NONE',  ( 45.35708200440645044, 29.00457786121581805, 45.92000246470679770 ) ) ;
#27889=CARTESIAN_POINT ( 'NONE',  ( 47.94164539834608263, 29.49617064401329714, 45.04602341336960336 ) ) ;
#27891=CARTESIAN_POINT ( 'NONE',  ( 48.94625023931840957, 25.27124452788249442, 46.10640627770150246 ) ) ;
#27901=EDGE_CURVE ( 'NONE', #19268, #27205, #5264, .T. ) ;
#27908=CARTESIAN_POINT ( 'NONE',  ( 46.00908685603033632, 28.33284706826092503, 44.91496614357595263 ) ) ;
#27922=CARTESIAN_POINT ( 'NONE',  ( 48.79245099466763946, 22.93807716476589675, 46.97542197481624271 ) ) ;
#27937=CARTESIAN_POINT ( 'NONE',  ( 44.77625694075214824, 28.81454579807170546, 48.23360063142255427 ) ) ;
#27952=CARTESIAN_POINT ( 'NONE',  ( 45.79384627280941089, 28.56618040159425931, 49.05938063676249072 ) ) ;
#27953=FACE_OUTER_BOUND ( 'NONE', #31280, .T. ) ;
#27987=DIRECTION ( 'NONE',  ( 0.4544104193609913023, 0.000000000000000000, 0.8907924397839084296 ) ) ;
#27990=EDGE_CURVE ( 'NONE', #4649, #4406, #31504, .T. ) ;
#28019=CARTESIAN_POINT ( 'NONE',  ( 46.96997866373305186, 23.12036939723557083, 46.79862680810013131 ) ) ;
#28024=CARTESIAN_POINT ( 'NONE',  ( 44.21498992391907024, 28.69488759933318178, 46.89958605635244027 ) ) ;
#28026=VERTEX_POINT ( 'NONE', #8694 ) ;
#28050=CARTESIAN_POINT ( 'NONE',  ( 48.16694854572211426, 27.91789516297709284, 49.14507740233662503 ) ) ;
#28064=CARTESIAN_POINT ( 'NONE',  ( 46.00908685603032922, 25.44624452788248448, 44.91496614357595263 ) ) ;
#28070=CARTESIAN_POINT ( 'NONE',  ( 45.24946171279598417, 26.40784706826093498, 47.99220971130008451 ) ) ;
#28082=ORIENTED_EDGE ( 'NONE', *, *, #10040, .T. ) ;
#28106=ORIENTED_EDGE ( 'NONE', *, *, #9263, .F. ) ;
#28118=CARTESIAN_POINT ( 'NONE',  ( 48.18662509608405031, 25.18284706826093355, 49.18364984542562013 ) ) ;
#28120=CARTESIAN_POINT ( 'NONE',  ( 48.94625023931840246, 28.77124452788248377, 46.10640627770150246 ) ) ;
#28130=CARTESIAN_POINT ( 'NONE',  ( 45.96182992765471909, 26.60087065737812040, 44.82232689504102296 ) ) ;
#28131=CARTESIAN_POINT ( 'NONE',  ( 45.39969523643555505, 22.86454579224779948, 45.99212200068701861 ) ) ;
#28149=ORIENTED_EDGE ( 'NONE', *, *, #8447, .F. ) ;
#28156=DIRECTION ( 'NONE',  ( 1.234978253042719660E-16, -1.000000000000000000, -1.109335647967047851E-31 ) ) ;
#28160=ORIENTED_EDGE ( 'NONE', *, *, #26124, .T. ) ;
#28169=ORIENTED_EDGE ( 'NONE', *, *, #23977, .T. ) ;
#28186=CARTESIAN_POINT ( 'NONE',  ( 46.96819297411687444, 28.86988759933318249, 49.54594323136014822 ) ) ;
#28197=VECTOR ( 'NONE', #29523, 999.9999999999998863 ) ;
#28200=B_SPLINE_CURVE_WITH_KNOTS ( 'NONE', 3,
 ( #18390, #28420, #3458, #13647, #23649, #13486, #11181, #21166, #31205, #3780 ),
 .UNSPECIFIED., .F., .F.,
 ( 4, 2, 2, 2, 4 ),
 ( 0.01122971665427002254, 0.01185769113519980454, 0.01248566561612958481, 0.01311364009705936681, 0.01374161457798914882 ),
 .UNSPECIFIED. ) ;
#28205=CARTESIAN_POINT ( 'NONE',  ( 47.65130514356931002, 23.10527865767145173, 47.24466138387320768 ) ) ;
#28211=CARTESIAN_POINT ( 'NONE',  ( 48.80717017713595141, 26.57622849631043138, 48.15820438821415195 ) ) ;
#28212=ORIENTED_EDGE ( 'NONE', *, *, #5422, .T. ) ;
#28220=CARTESIAN_POINT ( 'NONE',  ( 47.09785597605719687, 20.36454579224779948, 47.04930799450078638 ) ) ;
#28223=LINE ( 'NONE', #3583, #10029 ) ;
#28230=CARTESIAN_POINT ( 'NONE',  ( 47.20547626766764893, 26.17451373492760069, 44.97710074790751378 ) ) ;
#28245=CARTESIAN_POINT ( 'NONE',  ( 48.78406556707242459, 22.93807716476589675, 47.13688154746046166 ) ) ;
#28262=MECHANICAL_DESIGN_GEOMETRIC_PRESENTATION_REPRESENTATION('',(#19864),#5719);
#28272=CARTESIAN_POINT ( 'NONE',  ( 48.83862994770794330, 28.74118040159426002, 48.17861352429476796 ) ) ;
#28273=CARTESIAN_POINT ( 'NONE',  ( 44.70507715278255745, 28.36291119454914877, 46.92503878583765697 ) ) ;
#28305=ORIENTED_EDGE ( 'NONE', *, *, #17896, .F. ) ;
#28306=CARTESIAN_POINT ( 'NONE',  ( 47.62584127360276653, 29.61482468817860436, 45.06378368935094869 ) ) ;
#28345=CARTESIAN_POINT ( 'NONE',  ( 47.73247023833965130, 22.99884124225578930, 45.78378261437761410 ) ) ;
#28373=CARTESIAN_POINT ( 'NONE',  ( 48.77568013947721681, 22.93807716476589675, 47.29834112010470903 ) ) ;
#28374=CARTESIAN_POINT ( 'NONE',  ( 47.17209261226641104, 29.58954579224849368, 44.97563639035409011 ) ) ;
#28376=CARTESIAN_POINT ( 'NONE',  ( 45.28286642839709231, 26.34289516297710065, 47.97516931882780966 ) ) ;
#28391=CARTESIAN_POINT ( 'NONE',  ( 45.24946171279598417, 25.70784706826093569, 47.99220971130007740 ) ) ;
#28406=CARTESIAN_POINT ( 'NONE',  ( 46.55854765242722237, 25.86960992152948435, 44.51792966461572831 ) ) ;
#28409=ORIENTED_EDGE ( 'NONE', *, *, #12036, .T. ) ;
#28420=CARTESIAN_POINT ( 'NONE',  ( 46.18024325840006838, 29.23016326080685445, 44.78457194432868960 ) ) ;
#28436=CARTESIAN_POINT ( 'NONE',  ( 45.79384627280941089, 25.06618040159426641, 49.05938063676249072 ) ) ;
#28460=ORIENTED_EDGE ( 'NONE', *, *, #24432, .T. ) ;
#28531=CARTESIAN_POINT ( 'NONE',  ( 47.65993751833249092, 23.10527845304106620, 47.07849978535075053 ) ) ;
#28534=CARTESIAN_POINT ( 'NONE',  ( 45.38854177497844944, 28.32622849631042783, 45.94041160078741370 ) ) ;
#28542=CARTESIAN_POINT ( 'NONE',  ( 49.20081590711968289, 22.84434098701873594, 47.48251420876358964 ) ) ;
#28546=FACE_OUTER_BOUND ( 'NONE', #3758, .T. ) ;
#28554=CARTESIAN_POINT ( 'NONE',  ( 48.27628129728358886, 23.03451764446789696, 46.77839245790816847 ) ) ;
#28556=CARTESIAN_POINT ( 'NONE',  ( 45.35708200440645044, 25.59118040159426855, 45.92000246470680480 ) ) ;
#28564=CARTESIAN_POINT ( 'NONE',  ( 47.22751897799751220, 25.84253733014356413, 44.55267275764142454 ) ) ;
#28572=ORIENTED_EDGE ( 'NONE', *, *, #31908, .T. ) ;
#28580=CARTESIAN_POINT ( 'NONE',  ( 45.96182992765471909, 25.20087065737812182, 44.82232689504102296 ) ) ;
#28591=CARTESIAN_POINT ( 'NONE',  ( 45.73035263060504718, 30.03954579807169978, 44.36855633853329550 ) ) ;
#28593=PLANE ( 'NONE',  #23782 ) ;
#28616=CARTESIAN_POINT ( 'NONE',  ( 48.77917452769285944, 19.86454579224779948, 50.34524002170125101 ) ) ;
#28624=CARTESIAN_POINT ( 'NONE',  ( 49.72013424640590529, 24.87319583719382976, 46.29665793277550279 ) ) ;
#28660=DIRECTION ( 'NONE',  ( 0.4544104193609915243, 0.000000000000000000, 0.8907924397839082076 ) ) ;
#28673=EDGE_CURVE ( 'NONE', #9336, #13719, #20367, .T. ) ;
#28677=VERTEX_POINT ( 'NONE', #20215 ) ;
#28683=CARTESIAN_POINT ( 'NONE',  ( 44.74832014356462651, 27.68456182964376566, 46.92728461490987257 ) ) ;
#28704=CARTESIAN_POINT ( 'NONE',  ( 45.35708200440645044, 26.99118040159426357, 45.92000246470680480 ) ) ;
#28716=CARTESIAN_POINT ( 'NONE',  ( 48.23388202445966044, 25.55087065737811969, 49.27628909396054979 ) ) ;
#28728=ORIENTED_EDGE ( 'NONE', *, *, #11051, .T. ) ;
#28745=CARTESIAN_POINT ( 'NONE',  ( 50.10320668408830613, 27.00621246473837544, 47.20539118556276037 ) ) ;
#28758=CARTESIAN_POINT ( 'NONE',  ( 48.40186567930498285, 29.61618040159425647, 45.03923535223908203 ) ) ;
#28760=DIRECTION ( 'NONE',  ( 0.4544104193609903586, 0.000000000000000000, 0.8907924397839087627 ) ) ;
#28765=CARTESIAN_POINT ( 'NONE',  ( 45.00053793792376666, 26.53655426599985745, 45.68869892245983522 ) ) ;
#28773=CARTESIAN_POINT ( 'NONE',  ( 46.99023568444673771, 27.13791119454915446, 49.12151524109405898 ) ) ;
#28789=CARTESIAN_POINT ( 'NONE',  ( 48.35060479220636154, 22.84434098701873950, 48.79307647092393552 ) ) ;
#28798=EDGE_CURVE ( 'NONE', #30715, #15904, #19319, .T. ) ;
#28821=LINE ( 'NONE', #25028, #10610 ) ;
#28830=EDGE_CURVE ( 'NONE', #30606, #8039, #5936, .T. ) ;
#28833=CARTESIAN_POINT ( 'NONE',  ( 45.96182992765471909, 25.20087065737812182, 44.82232689504102296 ) ) ;
#28853=CARTESIAN_POINT ( 'NONE',  ( 45.81741271322955100, 27.14452976649964810, 49.02305402274571122 ) ) ;
#28856=ORIENTED_EDGE ( 'NONE', *, *, #14987, .T. ) ;
#28865=CARTESIAN_POINT ( 'NONE',  ( 49.28428300279882990, 27.64787913140504116, 48.46772541801551171 ) ) ;
#28869=B_SPLINE_CURVE_WITH_KNOTS ( 'NONE', 3,
 ( #29116, #6631, #26646, #31744, #9254, #7287 ),
 .UNSPECIFIED., .F., .F.,
 ( 4, 2, 4 ),
 ( 0.000000000000000000, 0.5000000000000000000, 1.000000000000000000 ),
 .UNSPECIFIED. ) ;
#28871=DIRECTION ( 'NONE',  ( -0.4441739386572047255, 0.2110602665713113557, -0.8707256032141197366 ) ) ;
#28875=EDGE_CURVE ( 'NONE', #24589, #3003, #2137, .T. ) ;
#28904=CARTESIAN_POINT ( 'NONE',  ( 45.84097905237065618, 22.86454579224779948, 48.98672734302541443 ) ) ;
#28921=CARTESIAN_POINT ( 'NONE',  ( 44.09250526802607340, 30.15621246473836692, 46.89322480343881949 ) ) ;
#28928=CARTESIAN_POINT ( 'NONE',  ( 46.55854765242722237, 28.66960992152947085, 44.51792966461572121 ) ) ;
#28929=CARTESIAN_POINT ( 'NONE',  ( 47.20353132263855400, 26.15286309983298807, 45.01455027646041174 ) ) ;
#28940=CARTESIAN_POINT ( 'NONE',  ( 45.36511207810797686, 27.90948166895303117, 45.12672418911604666 ) ) ;
#28943=CARTESIAN_POINT ( 'NONE',  ( 48.94625023931840246, 25.97124452788249371, 46.10640627770148825 ) ) ;
#28992=VECTOR ( 'NONE', #12268, 1000.000000000000000 ) ;
#29011=CARTESIAN_POINT ( 'NONE',  ( 45.28286642839709231, 29.18619643316631240, 47.97516931882780966 ) ) ;
#29022=CARTESIAN_POINT ( 'NONE',  ( 44.77625694075214824, 28.11454579807170617, 48.23360063142255427 ) ) ;
#29023=EDGE_CURVE ( 'NONE', #19411, #13392, #11231, .T. ) ;
#29028=LINE ( 'NONE', #18675, #23409 ) ;
#29047=ORIENTED_EDGE ( 'NONE', *, *, #3931, .F. ) ;
#29069=CARTESIAN_POINT ( 'NONE',  ( 44.91142894931555674, 29.39787913140503761, 45.63089057098605394 ) ) ;
#29075=VECTOR ( 'NONE', #19967, 1000.000000000000114 ) ;
#29083=CARTESIAN_POINT ( 'NONE',  ( 45.79384627280941089, 29.26618040159425860, 49.05938063676249072 ) ) ;
#29095=CARTESIAN_POINT ( 'NONE',  ( 45.36511207810797686, 25.23213139976340713, 45.12672418911604666 ) ) ;
#29101=CARTESIAN_POINT ( 'NONE',  ( 48.40186567930497574, 27.42957786121582231, 45.03923535223907493 ) ) ;
#29116=CARTESIAN_POINT ( 'NONE',  ( 46.33059210211230550, 22.93807716476589675, 45.54522087609679204 ) ) ;
#29133=ORIENTED_EDGE ( 'NONE', *, *, #14063, .F. ) ;
#29150=FACE_OUTER_BOUND ( 'NONE', #17006, .T. ) ;
#29156=VERTEX_POINT ( 'NONE', #6377 ) ;
#29170=CARTESIAN_POINT ( 'NONE',  ( 49.44739180854976013, 28.77786309983298096, 47.17133137409169308 ) ) ;
#29173=EDGE_LOOP ( 'NONE', ( #25940, #15325, #26375, #22926, #16695, #11117 ) ) ;
#29174=PLANE ( 'NONE',  #20062 ) ;
#29175=ORIENTED_EDGE ( 'NONE', *, *, #23285, .F. ) ;
#29182=CARTESIAN_POINT ( 'NONE',  ( 45.73035263060504718, 25.13954579807171186, 44.36855633853329550 ) ) ;
#29183=CARTESIAN_POINT ( 'NONE',  ( 46.72376704384358703, 22.91413368675619111, 48.81312807415246624 ) ) ;
#29188=DIRECTION ( 'NONE',  ( 0.4544104193609903586, 0.000000000000000000, 0.8907924397839087627 ) ) ;
#29189=CARTESIAN_POINT ( 'NONE',  ( 48.01680169312756874, 22.93807716476589675, 45.63279442905646022 ) ) ;
#29201=( BOUNDED_CURVE ( )  B_SPLINE_CURVE ( 2, ( #2887, #17820, #23551, #1069, #5849, #25854, #3367, #18297, #21082 ),
 .UNSPECIFIED., .F., .F. ) 
 B_SPLINE_CURVE_WITH_KNOTS ( ( 3, 2, 2, 2, 3 ),
 ( 0.3214285702672988188, 0.3333333333333333703, 0.3571428571428570953, 0.3809523809523809312, 0.3928571416958702711 ),
 .UNSPECIFIED. ) 
 CURVE ( )  GEOMETRIC_REPRESENTATION_ITEM ( )  RATIONAL_B_SPLINE_CURVE ( ( 0.9330127018922199644, 0.9330126953578159466, 1.000000000000000000, 0.8660254037844387076, 1.000000000000000000, 0.8660254037844387076, 1.000000000000000000, 0.9330127084266224280, 0.9330127018922200755 ) ) 
 REPRESENTATION_ITEM ( '' )  );
#29204=EDGE_CURVE ( 'NONE', #26418, #27205, #28223, .T. ) ;
#29209=CARTESIAN_POINT ( 'NONE',  ( 45.75738744548056758, 22.91413368675619111, 45.84342743610336868 ) ) ;
#29224=DIRECTION ( 'NONE',  ( -0.4441739386572013393, -0.2110602665713099402, -0.8707256032141217350 ) ) ;
#29227=CARTESIAN_POINT ( 'NONE',  ( 45.96182992765472619, 26.47822092656774728, 44.82232689504103007 ) ) ;
#29231=CARTESIAN_POINT ( 'NONE',  ( 50.10320668408830613, 26.30621246473837616, 47.20539118556276037 ) ) ;
#29240=CARTESIAN_POINT ( 'NONE',  ( 45.35708200440645044, 28.39118040159425860, 45.92000246470679770 ) ) ;
#29251=CARTESIAN_POINT ( 'NONE',  ( 45.96182992765471909, 27.87822092656774231, 44.82232689504102296 ) ) ;
#29257=CARTESIAN_POINT ( 'NONE',  ( 44.35155721551191021, 25.17319976284614924, 46.90667869236616383 ) ) ;
#29260=CIRCLE ( 'NONE', #958, 1.799999999999998490 ) ;
#29262=FACE_OUTER_BOUND ( 'NONE', #29773, .T. ) ;
#29268=ORIENTED_EDGE ( 'NONE', *, *, #9260, .F. ) ;
#29270=DIRECTION ( 'NONE',  ( 0.4544104193609905806, -6.737912671758737363E-17, 0.8907924397839086517 ) ) ;
#29310=ADVANCED_FACE ( 'NONE', ( #9319 ), #6935, .T. ) ;
#29316=AXIS2_PLACEMENT_3D ( 'NONE', #11801, #31980, #19328 ) ;
#29317=ORIENTED_EDGE ( 'NONE', *, *, #22571, .T. ) ;
#29325=CARTESIAN_POINT ( 'NONE',  ( 47.71045395478045492, 23.04411619146718238, 46.10501571378621577 ) ) ;
#29329=CARTESIAN_POINT ( 'NONE',  ( 48.16694854572211426, 28.66119643316631738, 49.14507740233662503 ) ) ;
#29334=EDGE_LOOP ( 'NONE', ( #4520, #29175, #20475, #31275 ) ) ;
#29335=CARTESIAN_POINT ( 'NONE',  ( 48.63043294988131748, 29.48064476602542072, 48.61409888045912453 ) ) ;
#29342=CARTESIAN_POINT ( 'NONE',  ( 49.41945501136223839, 27.76454579807170830, 45.86501535757901848 ) ) ;
#29344=CARTESIAN_POINT ( 'NONE',  ( 47.20539956190135200, 23.10527865767145173, 47.62628572795583892 ) ) ;
#29350=CYLINDRICAL_SURFACE ( 'NONE', #6805, 2.499999999999997335 ) ;
#29352=CARTESIAN_POINT ( 'NONE',  ( 46.04844006429464542, 19.96454579224779380, 44.99211097489548905 ) ) ;
#29382=DIRECTION ( 'NONE',  ( 0.4544104193609903586, 0.000000000000000000, 0.8907924397839087627 ) ) ;
#29384=FILL_AREA_STYLE ('',( #6733 ) ) ;
#29388=DIRECTION ( 'NONE',  ( 0.9986540920324801229, 6.158269594508761132E-17, 0.05186525298099653458 ) ) ;
#29395=ORIENTED_EDGE ( 'NONE', *, *, #4298, .T. ) ;
#29403=CARTESIAN_POINT ( 'NONE',  ( 47.23302798462060537, 26.48121246473837687, 44.44659793406428605 ) ) ;
#29404=B_SPLINE_CURVE_WITH_KNOTS ( 'NONE', 3,
 ( #14251, #24246, #21448, #13166, #1765, #16208, #18986, #8825, #11783, #9313, #13928, #11300, #19311, #18819, #29335, #13767, #15607, #23164 ),
 .UNSPECIFIED., .F., .F.,
 ( 4, 2, 2, 2, 2, 2, 2, 2, 4 ),
 ( 0.000000000000000000, 0.0004968808153924961441, 0.0009937616307849922882, 0.001490642446177488541, 0.001987523261569984576, 0.002484404076962480612, 0.002981284892354977081, 0.003478165707747473117, 0.003975046523139969153 ),
 .UNSPECIFIED. ) ;
#29411=CARTESIAN_POINT ( 'NONE',  ( 45.81741271322955100, 25.74452976649965663, 49.02305402274571122 ) ) ;
#29421=CARTESIAN_POINT ( 'NONE',  ( 49.71782891623905698, 24.91911585698229814, 46.85208669721036046 ) ) ;
#29428=CARTESIAN_POINT ( 'NONE',  ( 45.70079091716032593, 22.99884124225578574, 46.82018145558027555 ) ) ;
#29443=CARTESIAN_POINT ( 'NONE',  ( 45.24946171279598417, 29.90784706826092076, 47.99220971130007030 ) ) ;
#29448=CARTESIAN_POINT ( 'NONE',  ( 44.96728230447946117, 29.28052639176819838, 45.96899605402243338 ) ) ;
#29470=CARTESIAN_POINT ( 'NONE',  ( 49.40414881150629611, 19.96454579224779380, 47.16908566558144855 ) ) ;
#29502=CARTESIAN_POINT ( 'NONE',  ( 47.09785597605719687, 23.12036939723557083, 47.04930799450080059 ) ) ;
#29503=DIRECTION ( 'NONE',  ( 0.8907924397839086517, 1.100109291107994064E-16, -0.4544104193609905251 ) ) ;
#29506=CARTESIAN_POINT ( 'NONE',  ( 48.91284552371730143, 28.13619643316631169, 46.12344667017377020 ) ) ;
#29516=CARTESIAN_POINT ( 'NONE',  ( 44.77625694075215534, 26.71454579807170759, 48.23360063142255427 ) ) ;
#29518=CARTESIAN_POINT ( 'NONE',  ( 47.60933809039193676, 23.04411619146718238, 48.05197954673941751 ) ) ;
#29519=LINE ( 'NONE', #27044, #177 ) ;
#29521=EDGE_CURVE ( 'NONE', #14398, #7056, #15586, .T. ) ;
#29523=DIRECTION ( 'NONE',  ( 0.4544104193609905806, -6.737912671758738596E-17, 0.8907924397839087627 ) ) ;
#29525=CARTESIAN_POINT ( 'NONE',  ( 48.66090045299940670, 22.92747281079970278, 46.25196883385470414 ) ) ;
#29551=CARTESIAN_POINT ( 'NONE',  ( 45.23477325667712989, 24.86454579224779593, 43.39705899138675704 ) ) ;
#29556=PRESENTATION_STYLE_ASSIGNMENT (( #19357 ) ) ;
#29569=CARTESIAN_POINT ( 'NONE',  ( 44.77625694075214824, 25.31454579807171257, 48.23360063142255427 ) ) ;
#29575=CARTESIAN_POINT ( 'NONE',  ( 45.84097905237065618, 22.80400562401890241, 48.98672734302541443 ) ) ;
#29576=CARTESIAN_POINT ( 'NONE',  ( 48.83862994770794330, 26.64118040159426570, 48.17861352429476796 ) ) ;
#29583=DIRECTION ( 'NONE',  ( 0.4544104193609937448, 0.000000000000000000, 0.8907924397839072084 ) ) ;
#29591=CARTESIAN_POINT ( 'NONE',  ( 45.69268131687783807, 22.99884124225578574, 46.97633003370108185 ) ) ;
#29593=DIRECTION ( 'NONE',  ( 1.234978253042719660E-16, -1.000000000000000000, -1.109335647967047851E-31 ) ) ;
#29595=ORIENTED_EDGE ( 'NONE', *, *, #19814, .F. ) ;
#29596=( BOUNDED_CURVE ( )  B_SPLINE_CURVE ( 3, ( #2091, #22600, #17350, #24411 ),
 .UNSPECIFIED., .F., .F. ) 
 B_SPLINE_CURVE_WITH_KNOTS ( ( 4, 4 ),
 ( 1.099063246724956588, 1.220321128156879542 ),
 .UNSPECIFIED. ) 
 CURVE ( )  GEOMETRIC_REPRESENTATION_ITEM ( )  RATIONAL_B_SPLINE_CURVE ( ( 1.000000000000000000, 0.9987750858034806223, 0.9987750858034806223, 1.000000000000000000 ) ) 
 REPRESENTATION_ITEM ( '' )  );
#29615=EDGE_CURVE ( 'NONE', #12307, #10357, #7427, .T. ) ;
#29634=FACE_OUTER_BOUND ( 'NONE', #13943, .T. ) ;
#29641=VERTEX_POINT ( 'NONE', #25881 ) ;
#29677=CARTESIAN_POINT ( 'NONE',  ( 48.18662509608405031, 29.29624452788248234, 49.18364984542562013 ) ) ;
#29678=CARTESIAN_POINT ( 'NONE',  ( 47.73724253767792192, 22.99884124225578219, 48.30271392650413276 ) ) ;
#29697=CARTESIAN_POINT ( 'NONE',  ( 45.96600969091793587, 23.04411657098542676, 47.14051579308762285 ) ) ;
#29705=CARTESIAN_POINT ( 'NONE',  ( 48.94625023931840957, 25.97124452788249371, 46.10640627770150246 ) ) ;
#29714=CARTESIAN_POINT ( 'NONE',  ( 46.99023568444673771, 26.43791119454915517, 49.12151524109405898 ) ) ;
#29738=CARTESIAN_POINT ( 'NONE',  ( 45.24946171279598417, 25.00784706826093640, 47.99220971130007030 ) ) ;
#29748=CARTESIAN_POINT ( 'NONE',  ( 49.32910508985204956, 22.74928388133296764, 48.13418001454558492 ) ) ;
#29757=FACE_OUTER_BOUND ( 'NONE', #14943, .T. ) ;
#29772=CIRCLE ( 'NONE', #29789, 0.2999999999999986011 ) ;
#29773=EDGE_LOOP ( 'NONE', ( #28460, #28169, #31782, #16122 ) ) ;
#29789=AXIS2_PLACEMENT_3D ( 'NONE', #22608, #2269, #7526 ) ;
#29815=VECTOR ( 'NONE', #18684, 1000.000000000000114 ) ;
#29819=TOROIDAL_SURFACE ( 'NONE', #5192, 3.700000000000000178, 0.5000000000000002220 ) ;
#29834=DIRECTION ( 'NONE',  ( -0.4441739386572048920, -0.2110602665713094683, -0.8707256032141200697 ) ) ;
#29840=CARTESIAN_POINT ( 'NONE',  ( 47.22573328838134188, 23.12036939723557083, 47.29998918090146987 ) ) ;
#29842=CARTESIAN_POINT ( 'NONE',  ( 45.35708200440645044, 26.90457786121582018, 45.92000246470679770 ) ) ;
#29847=CARTESIAN_POINT ( 'NONE',  ( 45.96182992765471909, 15.77906836436399374, 44.82232689504101586 ) ) ;
#29862=CARTESIAN_POINT ( 'NONE',  ( 46.94469835654546586, 23.12036939723557083, 47.28539358874152043 ) ) ;
#29870=CARTESIAN_POINT ( 'NONE',  ( 48.16694854572211426, 29.31789516297709142, 49.14507740233662503 ) ) ;
#29881=CARTESIAN_POINT ( 'NONE',  ( 49.49063479933183629, 27.31291119454915162, 47.17357720316391578 ) ) ;
#29890=CARTESIAN_POINT ( 'NONE',  ( 48.18662509608405742, 27.98284706826092716, 49.18364984542562013 ) ) ;
#29906=CARTESIAN_POINT ( 'NONE',  ( 46.55854765242722948, 27.96960992152947512, 44.51792966461572121 ) ) ;
#29911=DIRECTION ( 'NONE',  ( 1.234978253042719660E-16, -1.000000000000000000, -1.109335647967047851E-31 ) ) ;
#29924=ORIENTED_EDGE ( 'NONE', *, *, #23403, .F. ) ;
#29928=FACE_OUTER_BOUND ( 'NONE', #9921, .T. ) ;
#29937=CARTESIAN_POINT ( 'NONE',  ( 45.35708200440645044, 29.79118040159425718, 45.92000246470679770 ) ) ;
#29944=EDGE_CURVE ( 'NONE', #4981, #11362, #25036, .T. ) ;
#29992=DIRECTION ( 'NONE',  ( -0.8389271868029121171, -1.036056831587902747E-16, -0.5442436726714897643 ) ) ;
#30004=CARTESIAN_POINT ( 'NONE',  ( 44.79156314060809763, 19.96454579224779380, 46.92953032342012420 ) ) ;
#30007=CARTESIAN_POINT ( 'NONE',  ( 45.24946171279598417, 29.12124452788248163, 47.99220971130007030 ) ) ;
#30009=CARTESIAN_POINT ( 'NONE',  ( 45.82550680184641578, 24.86454579224779593, 44.55508916310584056 ) ) ;
#30011=LINE ( 'NONE', #30175, #28197 ) ;
#30019=VERTEX_POINT ( 'NONE', #16943 ) ;
#30025=CARTESIAN_POINT ( 'NONE',  ( 45.70756922570320313, 22.95310733321322161, 47.91958190782160898 ) ) ;
#30029=EDGE_CURVE ( 'NONE', #10913, #10357, #11725, .T. ) ;
#30036=CARTESIAN_POINT ( 'NONE',  ( 44.74832014356462651, 29.08456182964376069, 46.92728461490987257 ) ) ;
#30039=CARTESIAN_POINT ( 'NONE',  ( 47.09785597605719687, 15.77906836436399374, 47.04930799450078638 ) ) ;
#30068=CARTESIAN_POINT ( 'NONE',  ( 49.98072202819530219, 27.76753733014355774, 47.19902993264913960 ) ) ;
#30089=ORIENTED_EDGE ( 'NONE', *, *, #30029, .T. ) ;
#30094=ORIENTED_EDGE ( 'NONE', *, *, #8213, .F. ) ;
#30098=ADVANCED_FACE ( 'NONE', ( #31893 ), #1526, .F. ) ;
#30102=CARTESIAN_POINT ( 'NONE',  ( 47.20547626766766314, 26.87451373492759643, 44.97710074790751378 ) ) ;
#30128=CARTESIAN_POINT ( 'NONE',  ( 45.99457799031791438, 29.23661293962803143, 44.88652376508412090 ) ) ;
#30151=CARTESIAN_POINT ( 'NONE',  ( 45.96182992765471909, 25.77822092656774799, 44.82232689504102296 ) ) ;
#30160=CARTESIAN_POINT ( 'NONE',  ( 47.86511985000206693, 22.93807716476589320, 48.55339511290479493 ) ) ;
#30164=ORIENTED_EDGE ( 'NONE', *, *, #31028, .F. ) ;
#30168=CARTESIAN_POINT ( 'NONE',  ( 45.63968093275011029, 22.91413368675619111, 48.10984057092807831 ) ) ;
#30170=CARTESIAN_POINT ( 'NONE',  ( 48.40186567930498285, 28.82957786121581378, 45.03923535223908203 ) ) ;
#30175=CARTESIAN_POINT ( 'NONE',  ( 48.35473289974373756, 22.86454579224779948, 45.11188864597615833 ) ) ;
#30187=CARTESIAN_POINT ( 'NONE',  ( 46.79153437246152691, 23.10527845304106265, 47.52148899368456370 ) ) ;
#30191=DIRECTION ( 'NONE',  ( -0.9986540920324801229, -1.233316085972235327E-16, -0.05186525298099629866 ) ) ;
#30193=CARTESIAN_POINT ( 'NONE',  ( 46.00908685603034343, 26.84624452788248661, 44.91496614357595263 ) ) ;
#30227=CARTESIAN_POINT ( 'NONE',  ( 48.40186567930498285, 25.41618040159426783, 45.03923535223908203 ) ) ;
#30234=PLANE ( 'NONE',  #16468 ) ;
#30257=CARTESIAN_POINT ( 'NONE',  ( 44.70507715278255745, 26.34951373492759430, 46.92503878583765697 ) ) ;
#30265=( BOUNDED_CURVE ( )  B_SPLINE_CURVE ( 3, ( #28131, #31076, #20571, #30914 ),
 .UNSPECIFIED., .F., .F. ) 
 B_SPLINE_CURVE_WITH_KNOTS ( ( 4, 4 ),
 ( 1.099063246724960363, 1.220321128156882651 ),
 .UNSPECIFIED. ) 
 CURVE ( )  GEOMETRIC_REPRESENTATION_ITEM ( )  RATIONAL_B_SPLINE_CURVE ( ( 1.000000000000000000, 0.9987750858034806223, 0.9987750858034806223, 1.000000000000000000 ) ) 
 REPRESENTATION_ITEM ( '' )  );
#30275=VECTOR ( 'NONE', #26455, 1000.000000000000227 ) ;
#30322=CARTESIAN_POINT ( 'NONE',  ( 47.88116631533108603, 22.93807716476589675, 45.54480264941530265 ) ) ;
#30327=CARTESIAN_POINT ( 'NONE',  ( 48.83862994770794330, 27.95457786121581734, 48.17861352429476796 ) ) ;
#30333=ORIENTED_EDGE ( 'NONE', *, *, #15234, .T. ) ;
#30352=DIRECTION ( 'NONE',  ( 1.234978253042719660E-16, -1.000000000000000000, -1.109335647967047851E-31 ) ) ;
#30353=CARTESIAN_POINT ( 'NONE',  ( 46.00908685603034343, 25.44624452788248448, 44.91496614357595263 ) ) ;
#30357=EDGE_CURVE ( 'NONE', #7173, #27205, #6221, .T. ) ;
#30370=CARTESIAN_POINT ( 'NONE',  ( 47.20547626766765603, 27.57451373492759572, 44.97710074790751378 ) ) ;
#30371=EDGE_LOOP ( 'NONE', ( #22058, #21002, #4967, #12363 ) ) ;
#30381=ORIENTED_EDGE ( 'NONE', *, *, #30029, .F. ) ;
#30384=CARTESIAN_POINT ( 'NONE',  ( 48.81767175631193112, 22.89977464660286444, 46.33034145269077442 ) ) ;
#30389=CARTESIAN_POINT ( 'NONE',  ( 45.00053793792376666, 25.95920399681023127, 45.68869892245983522 ) ) ;
#30392=ADVANCED_FACE ( 'NONE', ( #25482 ), #12191, .T. ) ;
#30398=DIRECTION ( 'NONE',  ( 1.234978253042719660E-16, -1.000000000000000000, -1.109335647967047851E-31 ) ) ;
#30403=CARTESIAN_POINT ( 'NONE',  ( 48.78406556707242459, 22.93807716476589675, 47.13688154746046166 ) ) ;
#30405=ORIENTED_EDGE ( 'NONE', *, *, #7981, .T. ) ;
#30415=CARTESIAN_POINT ( 'NONE',  ( 48.78406556707242459, 22.93807716476589675, 47.13688154746047587 ) ) ;
#30420=CARTESIAN_POINT ( 'NONE',  ( 48.40186567930498285, 25.41618040159426783, 45.03923535223908203 ) ) ;
#30422=CARTESIAN_POINT ( 'NONE',  ( 45.35708200440645044, 28.30457786121581876, 45.92000246470679770 ) ) ;
#30458=FACE_OUTER_BOUND ( 'NONE', #4020, .T. ) ;
#30459=CARTESIAN_POINT ( 'NONE',  ( 49.32483701613094240, 29.10322093266652033, 45.91328182968236860 ) ) ;
#30470=( BOUNDED_CURVE ( )  B_SPLINE_CURVE ( 3, ( #15959, #25496, #15809, #30907 ),
 .UNSPECIFIED., .F., .F. ) 
 B_SPLINE_CURVE_WITH_KNOTS ( ( 4, 4 ),
 ( 1.099063246724954812, 1.220321128156879320 ),
 .UNSPECIFIED. ) 
 CURVE ( )  GEOMETRIC_REPRESENTATION_ITEM ( )  RATIONAL_B_SPLINE_CURVE ( ( 1.000000000000000000, 0.9987750858034805113, 0.9987750858034805113, 1.000000000000000000 ) ) 
 REPRESENTATION_ITEM ( '' )  );
#30474=LINE ( 'NONE', #587, #6309 ) ;
#30487=ORIENTED_EDGE ( 'NONE', *, *, #16555, .F. ) ;
#30489=FACE_OUTER_BOUND ( 'NONE', #24847, .T. ) ;
#30495=CARTESIAN_POINT ( 'NONE',  ( 45.24946171279598417, 24.92124452788249300, 47.99220971130007030 ) ) ;
#30504=EDGE_CURVE ( 'NONE', #27205, #4649, #19327, .T. ) ;
#30505=ORIENTED_EDGE ( 'NONE', *, *, #28875, .F. ) ;
#30507=EDGE_CURVE ( 'NONE', #24091, #13542, #5919, .T. ) ;
#30520=DIRECTION ( 'NONE',  ( 1.234978253042719660E-16, -1.000000000000000000, -1.109335647967047851E-31 ) ) ;
#30521=CARTESIAN_POINT ( 'NONE',  ( 48.91284552371730143, 28.09289516297709710, 46.12344667017377020 ) ) ;
#30526=ORIENTED_EDGE ( 'NONE', *, *, #12836, .F. ) ;
#30528=CARTESIAN_POINT ( 'NONE',  ( 45.84097905237065618, 19.96454579224779380, 48.98672734302541443 ) ) ;
#30533=CARTESIAN_POINT ( 'NONE',  ( 44.70507715278255034, 25.56291119454915872, 46.92503878583767118 ) ) ;
#30538=CARTESIAN_POINT ( 'NONE',  ( 49.49063479933183629, 26.69951373492759927, 47.17357720316391578 ) ) ;
#30552=ORIENTED_EDGE ( 'NONE', *, *, #13909, .F. ) ;
#30562=CARTESIAN_POINT ( 'NONE',  ( 48.34748475735720064, 24.86874180309281712, 49.49898713858203791 ) ) ;
#30567=B_SPLINE_SURFACE_WITH_KNOTS ( 'NONE', 3, 3, ( 
 ( #10749, #30764, #20898, #8275, #5818, #15822 ),
 ( #25828, #3342, #13371, #23369, #10900, #30927 ),
 ( #8437, #18430, #14174, #1847, #24167, #1684 ),
 ( #22023, #17100, #14496, #6939, #14333, #26955 ),
 ( #29591, #29428, #9568, #6615, #32054, #24001 ),
 ( #11539, #21531, #31569, #7101, #16937, #9401 ) ),
 .UNSPECIFIED., .F., .F., .F.,
 ( 4, 2, 4 ),
 ( 4, 2, 4 ),
 ( 0.000000000000000000, 0.5000000000000000000, 1.000000000000000000 ),
 ( 0.000000000000000000, 0.5000000000000000000, 1.000000000000000000 ),
 .UNSPECIFIED. ) ;
#30570=CARTESIAN_POINT ( 'NONE',  ( 49.28428300279882990, 28.34787913140504045, 48.46772541801551171 ) ) ;
#30579=CARTESIAN_POINT ( 'NONE',  ( 47.25101359556892078, 23.12036939723557083, 46.81322240026007364 ) ) ;
#30585=CARTESIAN_POINT ( 'NONE',  ( 49.49063479933183629, 25.29951373492760069, 47.17357720316391578 ) ) ;
#30586=CARTESIAN_POINT ( 'NONE',  ( 46.00908685603034343, 28.94624452788248092, 44.91496614357595263 ) ) ;
#30606=VERTEX_POINT ( 'NONE', #20474 ) ;
#30626=ORIENTED_EDGE ( 'NONE', *, *, #11437, .F. ) ;
#30634=DIRECTION ( 'NONE',  ( 0.5319835227803570987, 0.2110602665713104953, -0.8200287161831886218 ) ) ;
#30636=TOROIDAL_SURFACE ( 'NONE', #14919, 4.099999999999999645, 0.1000000000000002554 ) ;
#30651=CARTESIAN_POINT ( 'NONE',  ( 47.71045395478045492, 23.04411619146718238, 46.10501571378621577 ) ) ;
#30676=CARTESIAN_POINT ( 'NONE',  ( 49.49821893081623614, 29.23298080189710291, 46.63169638315567767 ) ) ;
#30680=CARTESIAN_POINT ( 'NONE',  ( 45.81741271322955100, 25.70122849631043849, 49.02305402274571122 ) ) ;
#30681=ORIENTED_EDGE ( 'NONE', *, *, #10774, .T. ) ;
#30698=EDGE_CURVE ( 'NONE', #14884, #22418, #20796, .T. ) ;
#30700=CARTESIAN_POINT ( 'NONE',  ( 49.49063479933183629, 25.29951373492760069, 47.17357720316391578 ) ) ;
#30711=CARTESIAN_POINT ( 'NONE',  ( 48.83059987400640978, 25.58213139976340855, 48.97189179988551899 ) ) ;
#30715=VERTEX_POINT ( 'NONE', #28833 ) ;
#30728=CARTESIAN_POINT ( 'NONE',  ( 44.91142894931555674, 29.39787913140503761, 45.63089057098605394 ) ) ;
#30744=CARTESIAN_POINT ( 'NONE',  ( 45.24946171279598417, 26.40784706826093498, 47.99220971130007030 ) ) ;
#30745=CARTESIAN_POINT ( 'NONE',  ( 48.94625023931840246, 29.47124452788248306, 46.10640627770150246 ) ) ;
#30764=CARTESIAN_POINT ( 'NONE',  ( 46.96997866373305186, 23.12036939723557083, 46.79862680810013131 ) ) ;
#30771=CARTESIAN_POINT ( 'NONE',  ( 49.71806030971111312, 24.89927402503721154, 46.59246371035801815 ) ) ;
#30779=EDGE_LOOP ( 'NONE', ( #31125, #1473, #5153, #17008, #2409, #973 ) ) ;
#30785=DIRECTION ( 'NONE',  ( 1.234978253042719660E-16, -1.000000000000000000, -1.109335647967047851E-31 ) ) ;
#30805=CARTESIAN_POINT ( 'NONE',  ( 46.17891025898683921, 22.93807716476589675, 48.46582155994513386 ) ) ;
#30812=CARTESIAN_POINT ( 'NONE',  ( 44.87087493598345134, 28.75322093266651891, 48.18533415931919706 ) ) ;
#30825=ADVANCED_BREP_SHAPE_REPRESENTATION ( '', ( #23129, #8172 ), #22330 ) ;
#30833=CARTESIAN_POINT ( 'NONE',  ( 48.58040715586306391, 22.89977464660286444, 48.17922887912574481 ) ) ;
#30836=CARTESIAN_POINT ( 'NONE',  ( 48.37829923888483563, 26.75122849631043209, 45.07556196625585443 ) ) ;
#30845=CARTESIAN_POINT ( 'NONE',  ( 48.79601671567883159, 22.86454579224779948, 48.10649398831456125 ) ) ;
#30856=CARTESIAN_POINT ( 'NONE',  ( 48.40186567930497574, 26.81618040159426641, 45.03923535223907493 ) ) ;
#30858=DIRECTION ( 'NONE',  ( 0.4544104193609905806, 5.611869858668448142E-17, 0.8907924397839087627 ) ) ;
#30877=ORIENTED_EDGE ( 'NONE', *, *, #16642, .F. ) ;
#30894=ORIENTED_EDGE ( 'NONE', *, *, #6446, .T. ) ;
#30895=FACE_BOUND ( 'NONE', #24285, .T. ) ;
#30898=CARTESIAN_POINT ( 'NONE',  ( 47.23302798462060537, 29.98121246473836976, 44.44659793406428605 ) ) ;
#30907=CARTESIAN_POINT ( 'NONE',  ( 48.14727188781975542, 22.80400562401890241, 49.10650501410607660 ) ) ;
#30914=CARTESIAN_POINT ( 'NONE',  ( 44.79156314060809763, 22.80400562401889530, 46.92953032342012420 ) ) ;
#30926=VECTOR ( 'NONE', #18598, 1000.000000000000000 ) ;
#30927=CARTESIAN_POINT ( 'NONE',  ( 46.18657129672061501, 22.93807716476589675, 45.61868866909985343 ) ) ;
#30933=CARTESIAN_POINT ( 'NONE',  ( 49.65144901789264509, 24.93175518340850161, 46.50564549375109635 ) ) ;
#30936=CARTESIAN_POINT ( 'NONE',  ( 49.51946345327874610, 19.86454579224779948, 47.17507454913548770 ) ) ;
#30955=CARTESIAN_POINT ( 'NONE',  ( 45.96182992765471909, 15.77906836436399374, 44.82232689504101586 ) ) ;
#30961=CARTESIAN_POINT ( 'NONE',  ( 47.09785597605719687, 23.12036939723557083, 47.04930799450080059 ) ) ;
#30962=FACE_OUTER_BOUND ( 'NONE', #12806, .T. ) ;
#30984=CARTESIAN_POINT ( 'NONE',  ( 48.34748475735720064, 24.70653309617948423, 49.49898713858203791 ) ) ;
#31000=CARTESIAN_POINT ( 'NONE',  ( 49.44739180854976013, 26.63456182964376850, 47.17133137409169308 ) ) ;
#31006=CARTESIAN_POINT ( 'NONE',  ( 49.66977585544405827, 24.86874180309281712, 46.07579470028509405 ) ) ;
#31018=CARTESIAN_POINT ( 'NONE',  ( 48.40186567930497574, 26.11618040159426357, 45.03923535223908203 ) ) ;
#31028=EDGE_CURVE ( 'NONE', #6052, #26923, #9785, .T. ) ;
#31033=CARTESIAN_POINT ( 'NONE',  ( 48.83059987400639557, 27.68213139976340642, 48.97189179988552610 ) ) ;
#31034=B_SPLINE_CURVE_WITH_KNOTS ( 'NONE', 3,
 ( #6160, #5523, #20614, #908, #15527, #30961 ),
 .UNSPECIFIED., .F., .F.,
 ( 4, 2, 4 ),
 ( 0.000000000000000000, 0.5000000000000000000, 1.000000000000000000 ),
 .UNSPECIFIED. ) ;
#31041=ORIENTED_EDGE ( 'NONE', *, *, #982, .F. ) ;
#31051=CIRCLE ( 'NONE', #21073, 0.1000000000000016431 ) ;
#31057=CARTESIAN_POINT ( 'NONE',  ( 49.32483701613094240, 28.40322093266652104, 45.91328182968236860 ) ) ;
#31060=CARTESIAN_POINT ( 'NONE',  ( 48.46535932150934656, 26.88954579807171186, 49.73005965046827015 ) ) ;
#31061=EDGE_CURVE ( 'NONE', #1048, #19411, #12250, .T. ) ;
#31066=B_SPLINE_CURVE_WITH_KNOTS ( 'NONE', 3,
 ( #18732, #25816, #3161, #8264, #6119, #20729 ),
 .UNSPECIFIED., .F., .F.,
 ( 4, 2, 4 ),
 ( 0.000000000000000000, 0.5000000000000000000, 1.000000000000000000 ),
 .UNSPECIFIED. ) ;
#31067=AXIS2_PLACEMENT_3D ( 'NONE', #32263, #27156, #14699 ) ;
#31073=VECTOR ( 'NONE', #15606, 1000.000000000000000 ) ;
#31076=CARTESIAN_POINT ( 'NONE',  ( 45.19785535133951271, 22.86454579224779948, 46.30324912166403806 ) ) ;
#31081=LINE ( 'NONE', #15968, #6274 ) ;
#31102=CARTESIAN_POINT ( 'NONE',  ( 49.19517401419062708, 28.98655426599985319, 48.40991706654173754 ) ) ;
#31113=EDGE_CURVE ( 'NONE', #29641, #4406, #3510, .T. ) ;
#31114=DIRECTION ( 'NONE',  ( -0.9986540920324801229, -1.233316085972235573E-16, -0.05186525298099663173 ) ) ;
#31125=ORIENTED_EDGE ( 'NONE', *, *, #5396, .F. ) ;
#31155=CARTESIAN_POINT ( 'NONE',  ( 47.73724253767792192, 22.99884124225578219, 48.30271392650413276 ) ) ;
#31158=CARTESIAN_POINT ( 'NONE',  ( 45.81741271322955100, 27.10122849631043351, 49.02305402274571122 ) ) ;
#31168=PLANE ( 'NONE',  #5433 ) ;
#31205=CARTESIAN_POINT ( 'NONE',  ( 48.22039229833278995, 29.17080963813146965, 44.81246039718205765 ) ) ;
#31225=CARTESIAN_POINT ( 'NONE',  ( 50.10320668408830613, 28.40621246473837402, 47.20539118556276037 ) ) ;
#31244=CARTESIAN_POINT ( 'NONE',  ( 48.23388202445966044, 25.55087065737811969, 49.27628909396054979 ) ) ;
#31248=CARTESIAN_POINT ( 'NONE',  ( 47.20547626766765603, 27.48791119454915233, 44.97710074790751378 ) ) ;
#31257=ORIENTED_EDGE ( 'NONE', *, *, #7905, .T. ) ;
#31263=CARTESIAN_POINT ( 'NONE',  ( 48.14727188781975542, 22.80400562401890241, 49.10650501410607660 ) ) ;
#31264=ORIENTED_EDGE ( 'NONE', *, *, #20818, .T. ) ;
#31270=LINE ( 'NONE', #25698, #18118 ) ;
#31275=ORIENTED_EDGE ( 'NONE', *, *, #9227, .F. ) ;
#31280=EDGE_LOOP ( 'NONE', ( #143, #4083, #7670, #16472 ) ) ;
#31287=CARTESIAN_POINT ( 'NONE',  ( 48.23388202445966755, 27.52822092656774089, 49.27628909396054979 ) ) ;
#31301=ORIENTED_EDGE ( 'NONE', *, *, #15561, .F. ) ;
#31304=EDGE_CURVE ( 'NONE', #10913, #19411, #28869, .T. ) ;
#31313=CARTESIAN_POINT ( 'NONE',  ( 47.35361591473682097, 23.10527845304106265, 47.55068078453451363 ) ) ;
#31316=CARTESIAN_POINT ( 'NONE',  ( 45.18933221474103590, 24.76454579224779806, 43.30797974740836764 ) ) ;
#31317=CARTESIAN_POINT ( 'NONE',  ( 49.44739180854976013, 27.37786309983298239, 47.17133137409169308 ) ) ;
#31347=CARTESIAN_POINT ( 'NONE',  ( 48.23388202445966755, 15.77906836436399374, 49.27628909396055690 ) ) ;
#31376=CARTESIAN_POINT ( 'NONE',  ( 44.09250526802607340, 28.05621246473836905, 46.89322480343881949 ) ) ;
#31387=CARTESIAN_POINT ( 'NONE',  ( 46.99218062947583974, 25.80286309983299375, 49.08406571254116102 ) ) ;
#31399=CARTESIAN_POINT ( 'NONE',  ( 48.23388202445966755, 26.82822092656774515, 49.27628909396054979 ) ) ;
#31406=CARTESIAN_POINT ( 'NONE',  ( 49.49063479933183629, 26.61291119454915233, 47.17357720316391578 ) ) ;
#31413=AXIS2_PLACEMENT_3D ( 'NONE', #27745, #10517, #3101 ) ;
#31422=CARTESIAN_POINT ( 'NONE',  ( 47.82620649179236949, 29.44832000455004462, 49.14791808304156717 ) ) ;
#31442=CARTESIAN_POINT ( 'NONE',  ( 49.65101332465108186, 24.93501648625822398, 46.52608845888364186 ) ) ;
#31476=CARTESIAN_POINT ( 'NONE',  ( 45.38854177497844944, 28.36952976649964597, 45.94041160078741370 ) ) ;
#31489=CARTESIAN_POINT ( 'NONE',  ( 45.73035263060504718, 25.83954579807171115, 44.36855633853329550 ) ) ;
#31504=LINE ( 'NONE', #3762, #7378 ) ;
#31506=ADVANCED_FACE ( 'NONE', ( #18563 ), #28593, .F. ) ;
#31514=( BOUNDED_CURVE ( )  B_SPLINE_CURVE ( 2, ( #30151, #7661, #22251, #17654, #27673, #5194, #25218, #2730, #20923 ),
 .UNSPECIFIED., .F., .F. ) 
 B_SPLINE_CURVE_WITH_KNOTS ( ( 3, 2, 2, 2, 3 ),
 ( 0.1071428559815845449, 0.1190476190476190688, 0.1428571428571429047, 0.1666666666666666297, 0.1785714274101558585 ),
 .UNSPECIFIED. ) 
 CURVE ( )  GEOMETRIC_REPRESENTATION_ITEM ( )  RATIONAL_B_SPLINE_CURVE ( ( 0.9330127018922200755, 0.9330126953578161686, 1.000000000000000000, 0.8660254037844387076, 1.000000000000000000, 0.8660254037844387076, 1.000000000000000000, 0.9330127084266230941, 0.9330127018922200755 ) ) 
 REPRESENTATION_ITEM ( '' )  );
#31521=CARTESIAN_POINT ( 'NONE',  ( 47.09785597605719687, 24.86454579224779593, 47.04930799450078638 ) ) ;
#31540=DIRECTION ( 'NONE',  ( -0.4544104193609905806, -5.611869858668448142E-17, -0.8907924397839087627 ) ) ;
#31544=CARTESIAN_POINT ( 'NONE',  ( 46.96268396749378127, 28.93121246473836905, 49.65201805493727960 ) ) ;
#31555=CARTESIAN_POINT ( 'NONE',  ( 46.99218062947583974, 25.10286309983299091, 49.08406571254116102 ) ) ;
#31557=DIRECTION ( 'NONE',  ( 0.4114095458597723520, -0.6546536707079779749, -0.6341693441061513337 ) ) ;
#31562=CARTESIAN_POINT ( 'NONE',  ( 45.77813520618632737, 19.86454579224779948, 49.08359831045164157 ) ) ;
#31569=CARTESIAN_POINT ( 'NONE',  ( 45.42945060211348363, 22.93328494799376216, 46.63886900051237916 ) ) ;
#31570=CARTESIAN_POINT ( 'NONE',  ( 48.40186567930497574, 26.02957786121582373, 45.03923535223908203 ) ) ;
#31578=CARTESIAN_POINT ( 'NONE',  ( 46.58637386172244277, 23.04411619146718238, 46.04663644226216945 ) ) ;
#31582=DIRECTION ( 'NONE',  ( 1.234978253042719660E-16, -1.000000000000000000, -1.109335647967047851E-31 ) ) ;
#31608=CARTESIAN_POINT ( 'NONE',  ( 46.86492225703624825, 23.03451764446789696, 45.86279067552989375 ) ) ;
#31642=CARTESIAN_POINT ( 'NONE',  ( 45.28286642839709231, 27.08619643316632519, 47.97516931882780966 ) ) ;
#31655=CARTESIAN_POINT ( 'NONE',  ( 44.77625694075215534, 26.01454579807171186, 48.23360063142255427 ) ) ;
#31656=CARTESIAN_POINT ( 'NONE',  ( 47.02134891529708938, 22.98765316579146756, 48.52243470084199117 ) ) ;
#31657=DIRECTION ( 'NONE',  ( 0.4544104193609903586, 0.000000000000000000, 0.8907924397839087627 ) ) ;
#31675=EDGE_CURVE ( 'NONE', #5398, #3842, #9548, .T. ) ;
#31681=AXIS2_PLACEMENT_3D ( 'NONE', #9394, #19554, #25862 ) ;
#31689=FACE_OUTER_BOUND ( 'NONE', #29173, .T. ) ;
#31713=CARTESIAN_POINT ( 'NONE',  ( 49.49063479933183629, 29.49951373492758933, 47.17357720316391578 ) ) ;
#31731=CARTESIAN_POINT ( 'NONE',  ( 47.25393916711946218, 25.08121246473836763, 44.04395728646968422 ) ) ;
#31734=CARTESIAN_POINT ( 'NONE',  ( 46.55854765242723659, 26.44696019071911053, 44.51792966461573542 ) ) ;
#31744=CARTESIAN_POINT ( 'NONE',  ( 46.90849534498374140, 22.91413368675619111, 45.25622507561872965 ) ) ;
#31748=ORIENTED_EDGE ( 'NONE', *, *, #9852, .F. ) ;
#31769=CARTESIAN_POINT ( 'NONE',  ( 48.35473289974373756, 19.96454579224779380, 45.11188864597615833 ) ) ;
#31782=ORIENTED_EDGE ( 'NONE', *, *, #6405, .F. ) ;
#31796=CARTESIAN_POINT ( 'NONE',  ( 48.91284552371730143, 27.43619643316631596, 46.12344667017377020 ) ) ;
#31808=CARTESIAN_POINT ( 'NONE',  ( 49.28428300279882990, 24.84787913140505111, 48.46772541801551171 ) ) ;
#31810=DIRECTION ( 'NONE',  ( 0.4441739386572013948, 0.2110602665713099679, 0.8707256032141218460 ) ) ;
#31815=CARTESIAN_POINT ( 'NONE',  ( 47.83611419692596911, 23.04411657098542676, 46.18653938413861226 ) ) ;
#31858=CARTESIAN_POINT ( 'NONE',  ( 45.73035263060504718, 25.83954579807171115, 44.36855633853329550 ) ) ;
#31870=CARTESIAN_POINT ( 'NONE',  ( 49.44739180854976013, 25.27786309983298807, 47.17133137409169308 ) ) ;
#31877=CARTESIAN_POINT ( 'NONE',  ( 44.87087493598345134, 26.65322093266652104, 48.18533415931919706 ) ) ;
#31883=ORIENTED_EDGE ( 'NONE', *, *, #7437, .F. ) ;
#31891=( BOUNDED_CURVE ( )  B_SPLINE_CURVE ( 2, ( #10596, #8125, #18121, #22886, #398, #10427, #20419, #31734, #23694 ),
 .UNSPECIFIED., .F., .F. ) 
 B_SPLINE_CURVE_WITH_KNOTS ( ( 3, 2, 2, 2, 3 ),
 ( 0.1785714274101558585, 0.1904761904761904656, 0.2142857142857143016, 0.2380952380952381375, 0.2499999988387273664 ),
 .UNSPECIFIED. ) 
 CURVE ( )  GEOMETRIC_REPRESENTATION_ITEM ( )  RATIONAL_B_SPLINE_CURVE ( ( 0.9330127018922200755, 0.9330126953578157245, 1.000000000000000000, 0.8660254037844387076, 1.000000000000000000, 0.8660254037844387076, 1.000000000000000000, 0.9330127084266226500, 0.9330127018922199644 ) ) 
 REPRESENTATION_ITEM ( '' )  );
#31893=FACE_OUTER_BOUND ( 'NONE', #1939, .T. ) ;
#31908=EDGE_CURVE ( 'NONE', #15214, #25764, #25230, .T. ) ;
#31920=CARTESIAN_POINT ( 'NONE',  ( 48.23388202445966755, 27.65087065737811756, 49.27628909396056400 ) ) ;
#31931=DIRECTION ( 'NONE',  ( 1.234978253042719660E-16, -1.000000000000000000, -1.109335647967047851E-31 ) ) ;
#31957=LINE ( 'NONE', #24733, #28992 ) ;
#31958=CARTESIAN_POINT ( 'NONE',  ( 47.20353132263855400, 29.65286309983298096, 45.01455027646041174 ) ) ;
#31967=CARTESIAN_POINT ( 'NONE',  ( 44.79156314060809763, 22.80400562401889530, 46.92953032342012420 ) ) ;
#31970=CARTESIAN_POINT ( 'NONE',  ( 49.28428300279882990, 25.54787913140504685, 48.46772541801551171 ) ) ;
#31972=CARTESIAN_POINT ( 'NONE',  ( 47.14231618896855025, 22.89977464660286444, 48.91282684219816446 ) ) ;
#31979=CARTESIAN_POINT ( 'NONE',  ( 48.68948053213853910, 22.89977464660286444, 46.07904489681320115 ) ) ;
#31980=DIRECTION ( 'NONE',  ( -0.2155021956183748588, 0.9702957262759968060, 0.1099318300320501068 ) ) ;
#32008=PLANE ( 'NONE',  #1707 ) ;
#32010=( NAMED_UNIT ( * ) SI_UNIT ( $, .STERADIAN. ) SOLID_ANGLE_UNIT ( ) );
#32036=CARTESIAN_POINT ( 'NONE',  ( 44.70507715278255745, 26.34951373492759430, 46.92503878583765697 ) ) ;
#32054=CARTESIAN_POINT ( 'NONE',  ( 45.62581776903441977, 22.92747281079970278, 46.09434135054691950 ) ) ;
#32056=EDGE_CURVE ( 'NONE', #16262, #23526, #8479, .T. ) ;
#32058=CARTESIAN_POINT ( 'NONE',  ( 49.66977585544405827, 24.86874180309281712, 46.07579470028509405 ) ) ;
#32067=PLANE ( 'NONE',  #7319 ) ;
#32097=ADVANCED_FACE ( 'NONE', ( #25546, #3051 ), #604, .F. ) ;
#32114=AXIS2_PLACEMENT_3D ( 'NONE', #9807, #19801, #29834 ) ;
#32124=CARTESIAN_POINT ( 'NONE',  ( 46.58650058836976626, 22.86454579224779593, 49.02544611800051655 ) ) ;
#32140=CARTESIAN_POINT ( 'NONE',  ( 45.46000861347822308, 24.67287913140504685, 49.57397645940629616 ) ) ;
#32143=CARTESIAN_POINT ( 'NONE',  ( 46.86983284546423079, 22.95310733321322161, 48.67358610625728232 ) ) ;
#32167=CARTESIAN_POINT ( 'NONE',  ( 49.49063479933183629, 25.21291119454915375, 47.17357720316391578 ) ) ;
#32180=CARTESIAN_POINT ( 'NONE',  ( 48.40186567930497574, 28.82957786121581378, 45.03923535223908203 ) ) ;
#32183=ORIENTED_EDGE ( 'NONE', *, *, #5669, .F. ) ;
#32189=CARTESIAN_POINT ( 'NONE',  ( 48.94625023931840246, 27.45784706826093213, 46.10640627770149536 ) ) ;
#32195=ORIENTED_EDGE ( 'NONE', *, *, #1149, .T. ) ;
#32213=PLANE ( 'NONE',  #12073 ) ;
#32227=ORIENTED_EDGE ( 'NONE', *, *, #26425, .T. ) ;
#32235=CARTESIAN_POINT ( 'NONE',  ( 49.49063479933183629, 29.49951373492758933, 47.17357720316391578 ) ) ;
#32263=CARTESIAN_POINT ( 'NONE',  ( 47.09785597605719687, 25.16454579224780019, 47.04930799450078638 ) ) ;
#32272=DIRECTION ( 'NONE',  ( -0.5319835227803600963, 0.2110602665713099124, 0.8200287161831868454 ) ) ;
#32287=PLANE ( 'NONE',  #8367 ) ;
#32292=EDGE_LOOP ( 'NONE', ( #7754, #2457, #19422, #4495 ) ) ;
#32304=CARTESIAN_POINT ( 'NONE',  ( 45.79384627280941089, 26.37957786121582160, 49.05938063676249072 ) ) ;
#32308=CARTESIAN_POINT ( 'NONE',  ( 47.12478250753322584, 29.59809144869074160, 44.98302815556229461 ) ) ;
#32320=ORIENTED_EDGE ( 'NONE', *, *, #27901, .T. ) ;
#32332=CARTESIAN_POINT ( 'NONE',  ( 47.20353132263855400, 29.60956182964376637, 45.01455027646041174 ) ) ;
#32333=ORIENTED_EDGE ( 'NONE', *, *, #29023, .F. ) ;
#32341=CARTESIAN_POINT ( 'NONE',  ( 46.00908685603033632, 28.24624452788248874, 44.91496614357595263 ) ) ;
#32347=CARTESIAN_POINT ( 'NONE',  ( 44.87087493598345134, 28.87587066347688847, 48.18533415931919706 ) ) ;
#32350=CARTESIAN_POINT ( 'NONE',  ( 45.79384627280941089, 28.56618040159425931, 49.05938063676249072 ) ) ;
#32355=CARTESIAN_POINT ( 'NONE',  ( 47.23302798462060537, 25.78121246473837758, 44.44659793406428605 ) ) ;
#32369=CARTESIAN_POINT ( 'NONE',  ( 48.14727188781975542, 19.96454579224779380, 49.10650501410607660 ) ) ;
#32373=CARTESIAN_POINT ( 'NONE',  ( 47.70546624744041253, 14.98691807112498964, 47.08086432685907852 ) ) ;
#32382=CARTESIAN_POINT ( 'NONE',  ( 49.19517401419062708, 27.00920399681022843, 48.40991706654173754 ) ) ;
#32383=ORIENTED_EDGE ( 'NONE', *, *, #21822, .F. ) ;
#32390=CARTESIAN_POINT ( 'NONE',  ( 48.35473289974373756, 22.86454579224779948, 45.11188864597615833 ) ) ;
#32395=CARTESIAN_POINT ( 'NONE',  ( 46.05267182906204226, 29.39183878387655824, 49.07307072161059835 ) ) ;
#32399=EDGE_CURVE ( 'NONE', #30019, #2146, #14961, .T. ) ;
#32412=FACE_OUTER_BOUND ( 'NONE', #14579, .T. ) ;
#32465=CARTESIAN_POINT ( 'NONE',  ( 47.20547626766766314, 26.08791119454915730, 44.97710074790751378 ) ) ;
#32468=VERTEX_POINT ( 'NONE', #15338 ) ;
#32484=CARTESIAN_POINT ( 'NONE',  ( 45.40326095744675428, 22.93807716476589675, 47.12319401418537268 ) ) ;
#32493=CARTESIAN_POINT ( 'NONE',  ( 45.28286642839709231, 29.14289516297709071, 47.97516931882780966 ) ) ;
#32537=COLOUR_RGB('Black',0.12,0.14,0.17);
#32538=FILL_AREA_STYLE_COLOUR('',#32537);
#32539=FILL_AREA_STYLE('',(#32538));
#32540=SURFACE_STYLE_FILL_AREA(#32539);
#32541=SURFACE_SIDE_STYLE('',(#32540));
#32542=SURFACE_STYLE_USAGE(.BOTH.,#32541);
#32543=PRESENTATION_STYLE_ASSIGNMENT((#32542));
ENDSEC;
END-ISO-10303-21;
